ISO-10303-21;
HEADER;
FILE_DESCRIPTION (('STEP AP214'),
    '1' );
FILE_NAME ( 'ISO 4162 M5x10 Hex Flange Bolt.step', '2026-10-04T02:08:54', ( '' ), ( '' ), 'STEP AP214', 'Unspecified', '' );
FILE_SCHEMA (( 'AUTOMOTIVE_DESIGN' ));
ENDSEC;
DATA;
#29=CARTESIAN_POINT ( 'NONE',  ( 0.1527640389977631963, -0.1337207259432456607, 0.04397945982240732826 ) ) ;
#33=CARTESIAN_POINT ( 'NONE',  ( 0.1619907858920772714, 0.1553500912766716535, 0.01195870310704324514 ) ) ;
#37=CARTESIAN_POINT ( 'NONE',  ( 0.1602931993194442739, 0.07955613945526338049, -0.1377952755905511861 ) ) ;
#48=CARTESIAN_POINT ( 'NONE',  ( 0.1588779435336318824, 0.09971251034084034626, -0.1082054717952101869 ) ) ;
#70=EDGE_CURVE ( 'NONE', #32405, #30831, #8652, .T. ) ;
#86=CIRCLE ( 'NONE', #1647, 0.09842519685039370636 ) ;
#92=EDGE_CURVE ( 'NONE', #27712, #6075, #1837, .T. ) ;
#103=CARTESIAN_POINT ( 'NONE',  ( 0.005425426062181716927, 0.05318853600681028998, 0.1377950977353498141 ) ) ;
#132=FACE_OUTER_BOUND ( 'NONE', #21236, .T. ) ;
#147=FACE_OUTER_BOUND ( 'NONE', #21139, .T. ) ;
#175=CARTESIAN_POINT ( 'NONE',  ( 0.1619971594100712287, 0.06735705997075436269, 0.1405166210180776309 ) ) ;
#189=ADVANCED_FACE ( 'NONE', ( #38682 ), #13369, .T. ) ;
#212=CARTESIAN_POINT ( 'NONE',  ( 0.4330708661417322913, 0.08090551181102362266, 0.000000000000000000 ) ) ;
#229=AXIS2_PLACEMENT_3D ( 'NONE', #33997, #1125, #15784 ) ;
#237=AXIS2_PLACEMENT_3D ( 'NONE', #26256, #7319, #29176 ) ;
#244=DIRECTION ( 'NONE',  ( 0.000000000000000000, 0.000000000000000000, 1.000000000000000000 ) ) ;
#246=CARTESIAN_POINT ( 'NONE',  ( 0.2698848154395015464, -3.032960542342102697E-32, 0.09842519685039370636 ) ) ;
#250=ORIENTED_EDGE ( 'NONE', *, *, #34224, .F. ) ;
#273=ORIENTED_EDGE ( 'NONE', *, *, #35074, .F. ) ;
#278=CARTESIAN_POINT ( 'NONE',  ( 0.1571385178022428053, 0.1097099440836636214, 0.09077329659527381966 ) ) ;
#281=CARTESIAN_POINT ( 'NONE',  ( 0.1640397255812384159, 0.08076041531236369253, -0.1398787134456308257 ) ) ;
#302=AXIS2_PLACEMENT_3D ( 'NONE', #11967, #8576, #23214 ) ;
#336=CARTESIAN_POINT ( 'NONE',  ( 0.5358894627757212481, 4.766607801171850497E-17, 0.000000000000000000 ) ) ;
#339=DIRECTION ( 'NONE',  ( 0.000000000000000000, 1.000000000000000000, 0.000000000000000000 ) ) ;
#375=CARTESIAN_POINT ( 'NONE',  ( 0.003837171311379782533, -0.04331820873536343375, 0.1377949924024825246 ) ) ;
#394=CARTESIAN_POINT ( 'NONE',  ( 0.1637325577037128943, 0.07820587237429499350, 0.1401340067785760701 ) ) ;
#417=DIRECTION ( 'NONE',  ( -1.000000000000000000, 0.000000000000000000, 0.000000000000000000 ) ) ;
#424=EDGE_CURVE ( 'NONE', #18854, #1825, #37750, .T. ) ;
#446=CARTESIAN_POINT ( 'NONE',  ( 0.01230737760510395781, 0.07955613945526338049, -0.1377952755905511861 ) ) ;
#447=CARTESIAN_POINT ( 'NONE',  ( 0.1645760670519675339, 0.08210188079435769282, -0.1405695449895551230 ) ) ;
#452=DIRECTION ( 'NONE',  ( 0.000000000000000000, -1.000000000000000000, 0.000000000000000000 ) ) ;
#470=CARTESIAN_POINT ( 'NONE',  ( 0.3604359965418638123, 4.466152701071653354E-17, 0.000000000000000000 ) ) ;
#493=CARTESIAN_POINT ( 'NONE',  ( 0.3849708276051176936, 1.205361022782824954E-17, -0.09842519685039370636 ) ) ;
#500=CARTESIAN_POINT ( 'NONE',  ( 0.4330708661417322913, 4.616380251121755931E-17, 0.000000000000000000 ) ) ;
#517=CARTESIAN_POINT ( 'NONE',  ( 0.1577586585109271855, 0.1377137394884521138, -0.04231661445875282285 ) ) ;
#522=ORIENTED_EDGE ( 'NONE', *, *, #12247, .F. ) ;
#573=CARTESIAN_POINT ( 'NONE',  ( 3.334775382890951728E-20, 0.003375231709989810237, 0.1377952755905512139 ) ) ;
#576=FACE_OUTER_BOUND ( 'NONE', #27675, .T. ) ;
#592=CARTESIAN_POINT ( 'NONE',  ( 0.004734662961546367427, 0.1434636420620040986, -0.02711672434608614068 ) ) ;
#623=EDGE_CURVE ( 'NONE', #39641, #16593, #45079, .T. ) ;
#624=AXIS2_PLACEMENT_3D ( 'NONE', #17137, #13103, #2740 ) ;
#626=PLANE ( 'NONE',  #7602 ) ;
#634=CONICAL_SURFACE ( 'NONE', #29824, 0.09842519685039370636, 0.9599310885968824758 ) ;
#648=ORIENTED_EDGE ( 'NONE', *, *, #45925, .T. ) ;
#649=VERTEX_POINT ( 'NONE', #2063 ) ;
#665=ORIENTED_EDGE ( 'NONE', *, *, #6692, .F. ) ;
#671=CARTESIAN_POINT ( 'NONE',  ( 0.3425196850393700809, 4.616380251121755931E-17, 0.000000000000000000 ) ) ;
#724=DIRECTION ( 'NONE',  ( 0.000000000000000000, -1.000000000000000000, 0.000000000000000000 ) ) ;
#725=CARTESIAN_POINT ( 'NONE',  ( 0.4934383202099732468, 0.08090551181102362266, 9.908067607274841931E-18 ) ) ;
#729=EDGE_CURVE ( 'NONE', #7655, #31223, #13710, .T. ) ;
#737=CARTESIAN_POINT ( 'NONE',  ( 0.1642211665453957858, 0.08093770371294724264, -0.1401839329144623780 ) ) ;
#755=ORIENTED_EDGE ( 'NONE', *, *, #13172, .T. ) ;
#760=CARTESIAN_POINT ( 'NONE',  ( 0.5962569168439626477, -3.032960542342102697E-32, 0.09842519685039370636 ) ) ;
#767=ORIENTED_EDGE ( 'NONE', *, *, #22825, .T. ) ;
#771=AXIS2_PLACEMENT_3D ( 'NONE', #44550, #8619, #18463 ) ;
#783=CARTESIAN_POINT ( 'NONE',  ( 0.5839895013123354017, 4.616380251121755931E-17, 0.000000000000000000 ) ) ;
#827=VERTEX_POINT ( 'NONE', #3995 ) ;
#829=VERTEX_POINT ( 'NONE', #7135 ) ;
#832=CYLINDRICAL_SURFACE ( 'NONE', #40644, 0.09842519685039370636 ) ;
#838=CIRCLE ( 'NONE', #29214, 0.09842519685039370636 ) ;
#856=CARTESIAN_POINT ( 'NONE',  ( 0.1608809465420318885, 0.1607368455565694743, -0.002813831971227472289 ) ) ;
#868=CONICAL_SURFACE ( 'NONE', #23889, 0.08090551181102362266, 0.9599310885968742602 ) ;
#880=CARTESIAN_POINT ( 'NONE',  ( 0.1594617487093260011, 0.04893254358519821129, 0.1404675734346356175 ) ) ;
#882=CARTESIAN_POINT ( 'NONE',  ( 0.5057057357416000487, 4.766607801171850497E-17, 0.000000000000000000 ) ) ;
#902=CARTESIAN_POINT ( 'NONE',  ( 0.1555687797274980522, 0.09281549603114055969, 0.1148293963254592570 ) ) ;
#915=CARTESIAN_POINT ( 'NONE',  ( 0.1641609177537618758, -0.08086997970899940935, -0.1400748931816458154 ) ) ;
#916=CARTESIAN_POINT ( 'NONE',  ( 0.5839895013123354017, 0.08090551181102362266, 9.908067607274841931E-18 ) ) ;
#921=AXIS2_PLACEMENT_3D ( 'NONE', #33497, #29461, #21978 ) ;
#922=CARTESIAN_POINT ( 'NONE',  ( 0.1645805171892397445, -0.08212597262126515585, -0.1405696315964612142 ) ) ;
#960=EDGE_CURVE ( 'NONE', #2888, #5683, #38491, .T. ) ;
#961=CARTESIAN_POINT ( 'NONE',  ( 0.000000000000000000, 0.000000000000000000, 0.000000000000000000 ) ) ;
#964=DIRECTION ( 'NONE',  ( -1.000000000000000000, 0.000000000000000000, 0.000000000000000000 ) ) ;
#968=CARTESIAN_POINT ( 'NONE',  ( 0.4632545931758527691, -0.08090551181102362266, 0.000000000000000000 ) ) ;
#1003=DIRECTION ( 'NONE',  ( 1.000000000000000000, 0.000000000000000000, 0.000000000000000000 ) ) ;
#1007=CARTESIAN_POINT ( 'NONE',  ( 0.1637370714319413278, -0.1604746447930043285, 0.002359686926949007297 ) ) ;
#1012=EDGE_CURVE ( 'NONE', #35936, #46714, #2060, .T. ) ;
#1020=AXIS2_PLACEMENT_3D ( 'NONE', #961, #29788, #33603 ) ;
#1031=DIRECTION ( 'NONE',  ( 0.000000000000000000, -1.000000000000000000, 0.000000000000000000 ) ) ;
#1049=CARTESIAN_POINT ( 'NONE',  ( 0.4208034506101054895, 1.205361022782824954E-17, -0.09842519685039370636 ) ) ;
#1067=VERTEX_POINT ( 'NONE', #37789 ) ;
#1078=DIRECTION ( 'NONE',  ( 0.000000000000000000, 0.000000000000000000, 1.000000000000000000 ) ) ;
#1087=CARTESIAN_POINT ( 'NONE',  ( 0.2397010884053811242, 4.466152701071653354E-17, 0.000000000000000000 ) ) ;
#1111=ORIENTED_EDGE ( 'NONE', *, *, #15990, .F. ) ;
#1117=AXIS2_PLACEMENT_3D ( 'NONE', #18428, #1630, #34961 ) ;
#1125=DIRECTION ( 'NONE',  ( -1.000000000000000000, 0.000000000000000000, 0.000000000000000000 ) ) ;
#1136=CARTESIAN_POINT ( 'NONE',  ( 0.5415383587465882886, 4.466152701071653354E-17, 0.000000000000000000 ) ) ;
#1143=DIRECTION ( 'NONE',  ( 0.000000000000000000, -1.000000000000000000, 0.000000000000000000 ) ) ;
#1193=EDGE_CURVE ( 'NONE', #46578, #5859, #11421, .T. ) ;
#1208=CIRCLE ( 'NONE', #21080, 0.09842519685039370636 ) ;
#1236=FACE_OUTER_BOUND ( 'NONE', #37991, .T. ) ;
#1245=CARTESIAN_POINT ( 'NONE',  ( 0.1645760587280559184, -0.08068587895603188120, -0.1413870478498926997 ) ) ;
#1294=CARTESIAN_POINT ( 'NONE',  ( 0.1587072800412973328, -0.1005018865549618251, 0.1068311739851083991 ) ) ;
#1308=EDGE_CURVE ( 'NONE', #46256, #9934, #25199, .T. ) ;
#1312=ORIENTED_EDGE ( 'NONE', *, *, #24514, .F. ) ;
#1329=DIRECTION ( 'NONE',  ( -1.000000000000000000, 0.000000000000000000, 0.000000000000000000 ) ) ;
#1359=PRODUCT_DEFINITION ( 'UNKNOWN', '', #8646, #32694 ) ;
#1361=CARTESIAN_POINT ( 'NONE',  ( 0.2204724409448818867, 0.000000000000000000, 0.000000000000000000 ) ) ;
#1369=DIRECTION ( 'NONE',  ( 0.000000000000000000, -1.000000000000000000, 0.000000000000000000 ) ) ;
#1381=ORIENTED_EDGE ( 'NONE', *, *, #11607, .T. ) ;
#1425=EDGE_LOOP ( 'NONE', ( #24710, #12215, #7861, #39524, #40146 ) ) ;
#1428=CIRCLE ( 'NONE', #47370, 0.09842519685039370636 ) ;
#1438=EDGE_CURVE ( 'NONE', #4911, #23956, #39418, .T. ) ;
#1446=DIRECTION ( 'NONE',  ( -1.000000000000000000, 0.000000000000000000, 0.000000000000000000 ) ) ;
#1475=CARTESIAN_POINT ( 'NONE',  ( 0.1596650774283281671, -0.09389790430994664205, -0.1183119828674929208 ) ) ;
#1482=EDGE_LOOP ( 'NONE', ( #18220, #20705 ) ) ;
#1483=B_SPLINE_CURVE_WITH_KNOTS ( 'NONE', 3,
 ( #27986, #3010, #17175, #24600, #42774, #24838, #16708, #5916, #39439, #2776, #31337, #5681, #42553, #35166, #27769, #2081 ),
 .UNSPECIFIED., .F., .F.,
 ( 4, 2, 2, 2, 2, 2, 2, 4 ),
 ( 0.000000000000000000, 0.2499999999999998335, 0.3749999999999996669, 0.4374999999999997224, 0.4999999999999997780, 0.6249999999999997780, 0.7499999999999998890, 1.000000000000000000 ),
 .UNSPECIFIED. ) ;
#1489=CARTESIAN_POINT ( 'NONE',  ( 0.006378642920537238789, -0.09116121678392095917, -0.1176987636585394986 ) ) ;
#1528=DIRECTION ( 'NONE',  ( -1.000000000000000000, 0.000000000000000000, 0.000000000000000000 ) ) ;
#1533=AXIS2_PLACEMENT_3D ( 'NONE', #32083, #18396, #33038 ) ;
#1541=EDGE_CURVE ( 'NONE', #34889, #31112, #8075, .T. ) ;
#1543=CARTESIAN_POINT ( 'NONE',  ( 0.5538057742782149795, -0.08090551181102362266, 1.098083891755157578E-17 ) ) ;
#1547=AXIS2_PLACEMENT_3D ( 'NONE', #38721, #20498, #26603 ) ;
#1563=CARTESIAN_POINT ( 'NONE',  ( 0.000000000000000000, 0.000000000000000000, 0.000000000000000000 ) ) ;
#1564=ADVANCED_FACE ( 'NONE', ( #4001, #18623 ), #626, .T. ) ;
#1568=AXIS2_PLACEMENT_3D ( 'NONE', #36016, #3175, #19208 ) ;
#1580=DIRECTION ( 'NONE',  ( -1.000000000000000000, 0.000000000000000000, 0.000000000000000000 ) ) ;
#1595=FACE_OUTER_BOUND ( 'NONE', #26190, .T. ) ;
#1604=( BOUNDED_SURFACE ( )  B_SPLINE_SURFACE ( 3, 2, ( 
 ( #21922, #6580, #35599 ),
 ( #46830, #47074, #47320 ),
 ( #24800, #2738, #2973 ),
 ( #32962, #20953, #28666 ),
 ( #32492, #39871, #25283 ),
 ( #32251, #36542, #10194 ) ),
 .UNSPECIFIED., .F., .F., .T. ) 
 B_SPLINE_SURFACE_WITH_KNOTS ( ( 4, 2, 4 ),
 ( 3, 3 ),
 ( 0.01651732063679904952, 0.01857756227444015001, 0.02063780391208129908 ),
 ( 0.000000000000000000, 1.000000000000000000 ),
 .UNSPECIFIED. ) 
 GEOMETRIC_REPRESENTATION_ITEM ( )  RATIONAL_B_SPLINE_SURFACE ( (
 ( 1.000000000000000000, 0.8047781231227479903, 1.000000000000000000),
 ( 1.000000000000000000, 0.8123782108661420365, 1.000000000000000000),
 ( 1.000000000000000000, 0.8190665102138239284, 1.000000000000000000),
 ( 1.000000000000000000, 0.8192358432839229598, 1.000000000000000000),
 ( 1.000000000000000000, 0.8126132624438909824, 1.000000000000000000),
 ( 1.000000000000000000, 0.8047712436238880773, 1.000000000000000000) ) ) 
 REPRESENTATION_ITEM ( '' )  SURFACE ( )  ) ;
#1606=ORIENTED_EDGE ( 'NONE', *, *, #27421, .T. ) ;
#1614=EDGE_CURVE ( 'NONE', #44803, #21841, #30633, .T. ) ;
#1624=CARTESIAN_POINT ( 'NONE',  ( 0.000000000000000000, 1.205361022782826802E-17, -0.09842519685039370636 ) ) ;
#1630=DIRECTION ( 'NONE',  ( -1.000000000000000000, 0.000000000000000000, 0.000000000000000000 ) ) ;
#1639=CONICAL_SURFACE ( 'NONE', #35330, 0.09842519685039370636, 0.9599310885968824758 ) ;
#1644=DIRECTION ( 'NONE',  ( 0.000000000000000000, 0.000000000000000000, -1.000000000000000000 ) ) ;
#1647=AXIS2_PLACEMENT_3D ( 'NONE', #13097, #20494, #12627 ) ;
#1670=ADVANCED_FACE ( 'NONE', ( #44953 ), #16006, .F. ) ;
#1672=AXIS2_PLACEMENT_3D ( 'NONE', #671, #18207, #43831 ) ;
#1674=ADVANCED_FACE ( 'NONE', ( #4949 ), #46634, .T. ) ;
#1688=CARTESIAN_POINT ( 'NONE',  ( 0.1583744855326524870, -0.03901141430315739622, 0.1404421906569240930 ) ) ;
#1695=CIRCLE ( 'NONE', #17780, 0.09842519685039370636 ) ;
#1704=CARTESIAN_POINT ( 'NONE',  ( 0.1583858528204731275, 0.1411902173418021211, -0.03633609477026231160 ) ) ;
#1711=PRODUCT ( 'ISO 4162 M5x10 Hex Flange Bolt', 'ISO 4162 M5x10 Hex Flange Bolt', '', ( #36993 ) ) ;
#1731=CARTESIAN_POINT ( 'NONE',  ( 0.01230737760510407577, 0.1591122789105269553, -1.502406898952441074E-18 ) ) ;
#1736=AXIS2_PLACEMENT_3D ( 'NONE', #14915, #22318, #30036 ) ;
#1739=CARTESIAN_POINT ( 'NONE',  ( 0.002770643200454896322, -0.03669440867518906219, -0.1377943639823349942 ) ) ;
#1793=ORIENTED_EDGE ( 'NONE', *, *, #46477, .T. ) ;
#1812=FACE_OUTER_BOUND ( 'NONE', #12611, .T. ) ;
#1825=VERTEX_POINT ( 'NONE', #7084 ) ;
#1837=B_SPLINE_CURVE_WITH_KNOTS ( 'NONE', 3,
 ( #37491, #573, #18339, #36558, #40819, #40589, #3718, #43727, #10930, #44651, #25551, #103, #11868, #14749 ),
 .UNSPECIFIED., .F., .F.,
 ( 4, 2, 2, 2, 2, 2, 4 ),
 ( 0.000000000000000000, 0.1250000000000001110, 0.2500000000000002220, 0.3750000000000004441, 0.4375000000000004441, 0.5000000000000004441, 1.000000000000000000 ),
 .UNSPECIFIED. ) ;
#1857=DIRECTION ( 'NONE',  ( 0.000000000000000000, 1.000000000000000000, 1.224646799147353947E-16 ) ) ;
#1879=CIRCLE ( 'NONE', #1117, 0.09842519685039370636 ) ;
#1892=EDGE_LOOP ( 'NONE', ( #25261, #10836, #6956, #14618 ) ) ;
#1913=EDGE_CURVE ( 'NONE', #45437, #5036, #32752, .T. ) ;
#1928=DIRECTION ( 'NONE',  ( -1.000000000000000000, 0.000000000000000000, 0.000000000000000000 ) ) ;
#1930=CARTESIAN_POINT ( 'NONE',  ( 0.5236220472440944462, 4.616380251121755931E-17, 0.000000000000000000 ) ) ;
#1937=ORIENTED_EDGE ( 'NONE', *, *, #42883, .T. ) ;
#1955=CARTESIAN_POINT ( 'NONE',  ( 0.000000000000000000, 0.000000000000000000, 0.000000000000000000 ) ) ;
#1970=ORIENTED_EDGE ( 'NONE', *, *, #42883, .F. ) ;
#1973=CARTESIAN_POINT ( 'NONE',  ( 0.008396861977782204417, 0.1523390671602133373, 0.01173154688194899542 ) ) ;
#2002=DIRECTION ( 'NONE',  ( -1.000000000000000000, 0.000000000000000000, 0.000000000000000000 ) ) ;
#2009=EDGE_LOOP ( 'NONE', ( #35399, #38692, #14943 ) ) ;
#2033=ORIENTED_EDGE ( 'NONE', *, *, #22550, .F. ) ;
#2060=LINE ( 'NONE', #30862, #32086 ) ;
#2063=CARTESIAN_POINT ( 'NONE',  ( 0.3425196850393700809, -0.08090551181102362266, 1.098083891755157578E-17 ) ) ;
#2078=ORIENTED_EDGE ( 'NONE', *, *, #29473, .F. ) ;
#2081=CARTESIAN_POINT ( 'NONE',  ( 0.000000000000000000, 0.000000000000000000, -0.1377952755905511861 ) ) ;
#2087=DIRECTION ( 'NONE',  ( 0.000000000000000000, -1.000000000000000000, 0.000000000000000000 ) ) ;
#2125=CARTESIAN_POINT ( 'NONE',  ( 0.1602931993194444682, 0.1591122789105269553, 0.000000000000000000 ) ) ;
#2148=ORIENTED_EDGE ( 'NONE', *, *, #3089, .F. ) ;
#2173=ORIENTED_EDGE ( 'NONE', *, *, #32989, .F. ) ;
#2176=DIRECTION ( 'NONE',  ( 0.000000000000000000, -1.000000000000000000, 0.000000000000000000 ) ) ;
#2185=DIRECTION ( 'NONE',  ( -1.000000000000000000, 0.000000000000000000, 0.000000000000000000 ) ) ;
#2252=ORIENTED_EDGE ( 'NONE', *, *, #6760, .T. ) ;
#2282=LINE ( 'NONE', #13545, #25142 ) ;
#2288=DIRECTION ( 'NONE',  ( -0.5735764363510518216, 0.8191520442889876907, 1.003171929053519693E-16 ) ) ;
#2300=ORIENTED_EDGE ( 'NONE', *, *, #18650, .F. ) ;
#2311=ORIENTED_EDGE ( 'NONE', *, *, #16420, .T. ) ;
#2319=AXIS2_PLACEMENT_3D ( 'NONE', #15882, #43971, #29427 ) ;
#2323=EDGE_CURVE ( 'NONE', #7079, #3732, #45911, .T. ) ;
#2342=CARTESIAN_POINT ( 'NONE',  ( 0.1555687797274980522, 0.05303742630350897352, 0.1377952755905511861 ) ) ;
#2344=ORIENTED_EDGE ( 'NONE', *, *, #21534, .F. ) ;
#2366=LINE ( 'NONE', #17236, #2940 ) ;
#2373=EDGE_CURVE ( 'NONE', #42760, #4911, #43923, .T. ) ;
#2383=DIRECTION ( 'NONE',  ( 1.000000000000000000, 0.000000000000000000, 0.000000000000000000 ) ) ;
#2388=CONICAL_SURFACE ( 'NONE', #29250, 0.08090551181102362266, 0.9599310885968742602 ) ;
#2425=CIRCLE ( 'NONE', #46038, 0.1377952755905511861 ) ;
#2428=EDGE_CURVE ( 'NONE', #9934, #46256, #25269, .T. ) ;
#2445=DIRECTION ( 'NONE',  ( 0.000000000000000000, 0.000000000000000000, 1.000000000000000000 ) ) ;
#2454=CIRCLE ( 'NONE', #29322, 0.09842519685039370636 ) ;
#2470=CARTESIAN_POINT ( 'NONE',  ( 0.4632545931758527691, 4.616380251121755931E-17, 0.000000000000000000 ) ) ;
#2482=DIRECTION ( 'NONE',  ( 0.000000000000000000, 0.000000000000000000, 1.000000000000000000 ) ) ;
#2491=ORIENTED_EDGE ( 'NONE', *, *, #37055, .T. ) ;
#2496=EDGE_CURVE ( 'NONE', #35936, #6499, #7675, .T. ) ;
#2501=AXIS2_PLACEMENT_3D ( 'NONE', #40743, #38067, #22556 ) ;
#2510=DIRECTION ( 'NONE',  ( -1.000000000000000000, 0.000000000000000000, 0.000000000000000000 ) ) ;
#2517=FACE_OUTER_BOUND ( 'NONE', #41883, .T. ) ;
#2522=DIRECTION ( 'NONE',  ( 0.000000000000000000, -1.000000000000000000, 0.000000000000000000 ) ) ;
#2576=CARTESIAN_POINT ( 'NONE',  ( 0.002317115957683009517, 0.1025658529673372232, -0.09794161051897268266 ) ) ;
#2579=CARTESIAN_POINT ( 'NONE',  ( 0.4934383202099732468, -0.08090551181102362266, 0.000000000000000000 ) ) ;
#2580=FACE_OUTER_BOUND ( 'NONE', #28325, .T. ) ;
#2586=CARTESIAN_POINT ( 'NONE',  ( 0.1608809465420316664, 0.07793157280922068109, -0.1406091075617787456 ) ) ;
#2609=ORIENTED_EDGE ( 'NONE', *, *, #8223, .F. ) ;
#2613=DIRECTION ( 'NONE',  ( -1.000000000000000000, 0.000000000000000000, 0.000000000000000000 ) ) ;
#2635=EDGE_CURVE ( 'NONE', #5875, #19741, #27333, .T. ) ;
#2660=ORIENTED_EDGE ( 'NONE', *, *, #34982, .T. ) ;
#2684=AXIS2_PLACEMENT_3D ( 'NONE', #41666, #8387, #15851 ) ;
#2698=CARTESIAN_POINT ( 'NONE',  ( 0.2204724409448818867, 0.000000000000000000, 0.2047244094488188948 ) ) ;
#2711=DIRECTION ( 'NONE',  ( 0.000000000000000000, 1.000000000000000000, 0.000000000000000000 ) ) ;
#2721=ORIENTED_EDGE ( 'NONE', *, *, #27894, .F. ) ;
#2724=CONICAL_SURFACE ( 'NONE', #18814, 0.2114570894355444486, 1.221730476396037490 ) ;
#2738=CARTESIAN_POINT ( 'NONE',  ( 0.1555216598441131470, -0.02857485583077736674, 0.1377952755905512416 ) ) ;
#2740=DIRECTION ( 'NONE',  ( 0.000000000000000000, -1.000000000000000000, 0.000000000000000000 ) ) ;
#2746=EDGE_CURVE ( 'NONE', #5495, #31112, #13627, .T. ) ;
#2763=ORIENTED_EDGE ( 'NONE', *, *, #5694, .T. ) ;
#2776=CARTESIAN_POINT ( 'NONE',  ( 0.002798995768878668067, 0.03701427616989226566, -0.1377952292137403223 ) ) ;
#2802=EDGE_CURVE ( 'NONE', #8667, #32919, #11851, .T. ) ;
#2808=CARTESIAN_POINT ( 'NONE',  ( 0.000000000000000000, 0.000000000000000000, 0.09842519685039370636 ) ) ;
#2810=CARTESIAN_POINT ( 'NONE',  ( 0.1571288672381035423, 0.02360035419903267623, -0.1403980133540707609 ) ) ;
#2817=FACE_OUTER_BOUND ( 'NONE', #42425, .T. ) ;
#2845=EDGE_CURVE ( 'NONE', #17977, #39669, #20793, .T. ) ;
#2853=CARTESIAN_POINT ( 'NONE',  ( 0.1577586585109236050, -0.1055041328676506324, -0.09810528961776883439 ) ) ;
#2861=AXIS2_PLACEMENT_3D ( 'NONE', #24245, #6007, #6478 ) ;
#2888=VERTEX_POINT ( 'NONE', #25999 ) ;
#2904=DIRECTION ( 'NONE',  ( -0.5735764363510518216, 0.8191520442889876907, 1.003171929053519693E-16 ) ) ;
#2917=CARTESIAN_POINT ( 'NONE',  ( 0.4151545546392377273, 4.766607801171850497E-17, 0.000000000000000000 ) ) ;
#2925=ORIENTED_EDGE ( 'NONE', *, *, #8325, .F. ) ;
#2940=VECTOR ( 'NONE', #17933, 39.37007874015748143 ) ;
#2960=VECTOR ( 'NONE', #34906, 39.37007874015748854 ) ;
#2973=CARTESIAN_POINT ( 'NONE',  ( 0.1564639344508098606, -0.02850229122252114292, 0.1403868508442179253 ) ) ;
#3000=ORIENTED_EDGE ( 'NONE', *, *, #13330, .F. ) ;
#3010=CARTESIAN_POINT ( 'NONE',  ( 0.01036003557126029262, 0.07281034877059977539, -0.1377952755905511306 ) ) ;
#3016=CARTESIAN_POINT ( 'NONE',  ( 0.4151545546392377273, 0.09842519685039370636, 0.000000000000000000 ) ) ;
#3089=EDGE_CURVE ( 'NONE', #43974, #17392, #15936, .T. ) ;
#3102=CARTESIAN_POINT ( 'NONE',  ( 0.1600714537641845792, -0.1485828198929936561, -0.02360507234447689617 ) ) ;
#3110=VECTOR ( 'NONE', #33947, 39.37007874015748143 ) ;
#3140=CIRCLE ( 'NONE', #18475, 0.09842519685039370636 ) ;
#3142=AXIS2_PLACEMENT_3D ( 'NONE', #8163, #26882, #19187 ) ;
#3149=CARTESIAN_POINT ( 'NONE',  ( 0.1638066842826735592, -0.1611410944699764314, 1.358467538918664965E-08 ) ) ;
#3158=CARTESIAN_POINT ( 'NONE',  ( 0.4755220087074803481, 0.09842519685039370636, 0.000000000000000000 ) ) ;
#3171=AXIS2_PLACEMENT_3D ( 'NONE', #38062, #5217, #38991 ) ;
#3175=DIRECTION ( 'NONE',  ( -1.000000000000000000, 0.000000000000000000, 0.000000000000000000 ) ) ;
#3211=FACE_OUTER_BOUND ( 'NONE', #29205, .T. ) ;
#3212=CONICAL_SURFACE ( 'NONE', #921, 0.1377952755905511861, 1.047197551196598297 ) ;
#3215=CARTESIAN_POINT ( 'NONE',  ( 0.2519685039370078705, 0.08090551181102362266, 0.000000000000000000 ) ) ;
#3223=DIRECTION ( 'NONE',  ( 0.000000000000000000, 0.000000000000000000, 1.000000000000000000 ) ) ;
#3247=ADVANCED_FACE ( 'NONE', ( #147 ), #3212, .T. ) ;
#3270=CIRCLE ( 'NONE', #23966, 0.09842519685039370636 ) ;
#3271=( NAMED_UNIT ( * ) PLANE_ANGLE_UNIT ( ) SI_UNIT ( $, .RADIAN. ) ) ;
#3272=ORIENTED_EDGE ( 'NONE', *, *, #2496, .T. ) ;
#3279=AXIS2_PLACEMENT_3D ( 'NONE', #15161, #44825, #30497 ) ;
#3285=DIRECTION ( 'NONE',  ( 0.000000000000000000, -1.000000000000000000, 0.000000000000000000 ) ) ;
#3297=ORIENTED_EDGE ( 'NONE', *, *, #11546, .F. ) ;
#3338=ADVANCED_FACE ( 'NONE', ( #1812 ), #19787, .F. ) ;
#3393=CARTESIAN_POINT ( 'NONE',  ( 0.1638905441107560423, -0.1612682469887707637, -2.622724073162300381E-07 ) ) ;
#3423=AXIS2_PLACEMENT_3D ( 'NONE', #33122, #6972, #40258 ) ;
#3427=CONICAL_SURFACE ( 'NONE', #33287, 0.09842519685039370636, 0.9599310885968824758 ) ;
#3445=ORIENTED_EDGE ( 'NONE', *, *, #12750, .F. ) ;
#3449=ORIENTED_EDGE ( 'NONE', *, *, #22998, .F. ) ;
#3456=VECTOR ( 'NONE', #11530, 39.37007874015748854 ) ;
#3458=VECTOR ( 'NONE', #44223, 39.37007874015748854 ) ;
#3468=ADVANCED_FACE ( 'NONE', ( #23632 ), #16285, .T. ) ;
#3471=DIRECTION ( 'NONE',  ( 0.5735764363510447161, 0.8191520442889925757, 0.000000000000000000 ) ) ;
#3533=LINE ( 'NONE', #17426, #25380 ) ;
#3537=LINE ( 'NONE', #15513, #9076 ) ;
#3546=CARTESIAN_POINT ( 'NONE',  ( 0.004280036809600739831, -0.1422536944054435537, 0.02921503453321950064 ) ) ;
#3548=CARTESIAN_POINT ( 'NONE',  ( 0.5660731898098425585, 4.766607801171850497E-17, 0.000000000000000000 ) ) ;
#3587=LINE ( 'NONE', #6698, #28632 ) ;
#3612=DIRECTION ( 'NONE',  ( 0.000000000000000000, -1.000000000000000000, 0.000000000000000000 ) ) ;
#3646=EDGE_LOOP ( 'NONE', ( #29664, #18189, #18677, #755, #45195 ) ) ;
#3653=CARTESIAN_POINT ( 'NONE',  ( 0.1641609508012460417, 0.08087345834217524176, -0.1400729584206018841 ) ) ;
#3662=CARTESIAN_POINT ( 'NONE',  ( 0.1619907858921093569, 0.08803158632528092220, -0.1285577739724623192 ) ) ;
#3684=CARTESIAN_POINT ( 'NONE',  ( 0.01230737760510409486, -0.1591122789105269553, -1.990515434288500257E-18 ) ) ;
#3693=EDGE_CURVE ( 'NONE', #23379, #46614, #31138, .T. ) ;
#3718=CARTESIAN_POINT ( 'NONE',  ( 0.001488155332080226502, 0.02696424538979726865, 0.1377975042921876780 ) ) ;
#3723=VERTEX_POINT ( 'NONE', #22315 ) ;
#3732=VERTEX_POINT ( 'NONE', #7701 ) ;
#3738=CARTESIAN_POINT ( 'NONE',  ( 0.003857550520859602799, 0.1410454915399580178, -0.03130963158115300515 ) ) ;
#3742=ORIENTED_EDGE ( 'NONE', *, *, #23227, .T. ) ;
#3760=DIRECTION ( 'NONE',  ( -1.000000000000000000, 0.000000000000000000, 0.000000000000000000 ) ) ;
#3775=ORIENTED_EDGE ( 'NONE', *, *, #13482, .F. ) ;
#3776=CARTESIAN_POINT ( 'NONE',  ( 0.2204724409448818867, 0.07955613945526338049, -0.1377952755905511861 ) ) ;
#3783=ADVANCED_FACE ( 'NONE', ( #23465 ), #27554, .T. ) ;
#3791=DIRECTION ( 'NONE',  ( 0.5735764363510447161, 0.8191520442889925757, 0.000000000000000000 ) ) ;
#3795=EDGE_CURVE ( 'NONE', #15794, #46578, #21638, .T. ) ;
#3801=CONICAL_SURFACE ( 'NONE', #46656, 0.08090551181102362266, 0.9599310885968742602 ) ;
#3818=VERTEX_POINT ( 'NONE', #16967 ) ;
#3847=DIRECTION ( 'NONE',  ( -1.000000000000000000, 0.000000000000000000, 0.000000000000000000 ) ) ;
#3873=CARTESIAN_POINT ( 'NONE',  ( 0.3246033735368759610, -0.09842519685039370636, 1.205361022782828805E-17 ) ) ;
#3881=CARTESIAN_POINT ( 'NONE',  ( 0.1564139474901022064, 0.1282476652663593897, 0.05864041697631208749 ) ) ;
#3884=CARTESIAN_POINT ( 'NONE',  ( 0.1643970176816420548, 0.08114889158698145033, -0.1405540032085720592 ) ) ;
#3909=VECTOR ( 'NONE', #25774, 39.37007874015748854 ) ;
#3966=CARTESIAN_POINT ( 'NONE',  ( 0.005686768416221401126, 0.1458881524273768215, -0.02291217744946314958 ) ) ;
#3967=CYLINDRICAL_SURFACE ( 'NONE', #45037, 0.09842519685039370636 ) ;
#3969=ORIENTED_EDGE ( 'NONE', *, *, #37217, .F. ) ;
#3973=CONICAL_SURFACE ( 'NONE', #33075, 0.08090551181102362266, 0.9599310885968742602 ) ;
#3995=CARTESIAN_POINT ( 'NONE',  ( 0.4755220087074803481, 1.205361022782824954E-17, -0.09842519685039370636 ) ) ;
#4001=FACE_BOUND ( 'NONE', #1482, .T. ) ;
#4005=CARTESIAN_POINT ( 'NONE',  ( 0.000000000000000000, 0.1193342091828950846, -0.06889763779527559306 ) ) ;
#4010=EDGE_CURVE ( 'NONE', #32338, #35869, #33163, .T. ) ;
#4025=ORIENTED_EDGE ( 'NONE', *, *, #7280, .T. ) ;
#4041=EDGE_CURVE ( 'NONE', #3723, #15821, #12497, .T. ) ;
#4060=CIRCLE ( 'NONE', #35456, 0.09842519685039370636 ) ;
#4106=FACE_OUTER_BOUND ( 'NONE', #1892, .T. ) ;
#4149=CARTESIAN_POINT ( 'NONE',  ( 0.002061874009640850183, -0.03163730233503504047, -0.1377906290935765887 ) ) ;
#4160=EDGE_CURVE ( 'NONE', #14831, #38424, #44591, .T. ) ;
#4177=CARTESIAN_POINT ( 'NONE',  ( 0.1600714537641758362, -0.09473400225499722938, 0.1168739604209794586 ) ) ;
#4186=ORIENTED_EDGE ( 'NONE', *, *, #24423, .F. ) ;
#4196=MECHANICAL_DESIGN_GEOMETRIC_PRESENTATION_REPRESENTATION('',(#6491),#44754);
#4199=DIRECTION ( 'NONE',  ( 0.000000000000000000, -1.000000000000000000, 0.000000000000000000 ) ) ;
#4216=CARTESIAN_POINT ( 'NONE',  ( 0.1608764814808671395, 0.07794373349925551309, 0.1405880446287834651 ) ) ;
#4226=CARTESIAN_POINT ( 'NONE',  ( 0.2204724409448818867, 0.1591122789105269553, 0.000000000000000000 ) ) ;
#4243=EDGE_CURVE ( 'NONE', #20918, #23956, #35192, .T. ) ;
#4251=CARTESIAN_POINT ( 'NONE',  ( 0.5358894627757212481, -3.032960542342102697E-32, 0.09842519685039370636 ) ) ;
#4271=ORIENTED_EDGE ( 'NONE', *, *, #16678, .T. ) ;
#4300=LINE ( 'NONE', #5270, #3456 ) ;
#4319=CARTESIAN_POINT ( 'NONE',  ( 0.2204724409448818867, -0.1591122789105269553, 0.000000000000000000 ) ) ;
#4324=CARTESIAN_POINT ( 'NONE',  ( 0.5113546317124669782, 1.205361022782824954E-17, -0.09842519685039370636 ) ) ;
#4326=CARTESIAN_POINT ( 'NONE',  ( 0.1587072800412982765, 0.1427694538647063249, 0.03362159989229027840 ) ) ;
#4352=CARTESIAN_POINT ( 'NONE',  ( 0.1555213372790614501, -0.1050481006241407722, -0.09364190366147240319 ) ) ;
#4357=ADVANCED_FACE ( 'NONE', ( #25697 ), #29564, .T. ) ;
#4366=CARTESIAN_POINT ( 'NONE',  ( 0.003457534521343415441, -0.09882139917207719004, -0.1044452803222859771 ) ) ;
#4377=CARTESIAN_POINT ( 'NONE',  ( 0.1602931993194442739, 0.07955613945526338049, 0.1377952755905511861 ) ) ;
#4405=CARTESIAN_POINT ( 'NONE',  ( 0.1583858528204782623, -0.1411902173418210782, 0.03633609477024421497 ) ) ;
#4409=ORIENTED_EDGE ( 'NONE', *, *, #4243, .T. ) ;
#4421=ORIENTED_EDGE ( 'NONE', *, *, #36897, .F. ) ;
#4475=FACE_OUTER_BOUND ( 'NONE', #37850, .T. ) ;
#4492=DIRECTION ( 'NONE',  ( 0.000000000000000000, -1.000000000000000000, 0.000000000000000000 ) ) ;
#4497=EDGE_CURVE ( 'NONE', #827, #6014, #27115, .T. ) ;
#4502=CARTESIAN_POINT ( 'NONE',  ( 0.1637370647600281393, -0.08228083545669484522, -0.1377952755905511584 ) ) ;
#4540=EDGE_CURVE ( 'NONE', #829, #21151, #16422, .T. ) ;
#4545=AXIS2_PLACEMENT_3D ( 'NONE', #16240, #35154, #45663 ) ;
#4556=DIRECTION ( 'NONE',  ( 0.000000000000000000, -1.000000000000000000, 0.000000000000000000 ) ) ;
#4574=EDGE_CURVE ( 'NONE', #19636, #4842, #20134, .T. ) ;
#4585=ORIENTED_EDGE ( 'NONE', *, *, #8223, .T. ) ;
#4589=CARTESIAN_POINT ( 'NONE',  ( 0.000000000000000000, 0.000000000000000000, 0.000000000000000000 ) ) ;
#4594=ADVANCED_FACE ( 'NONE', ( #26644 ), #41438, .T. ) ;
#4595=CARTESIAN_POINT ( 'NONE',  ( 0.1526809758745832635, -0.1331472126641777554, -0.04497281396056834746 ) ) ;
#4601=ORIENTED_EDGE ( 'NONE', *, *, #11577, .T. ) ;
#4604=AXIS2_PLACEMENT_3D ( 'NONE', #16171, #30805, #39125 ) ;
#4615=FACE_OUTER_BOUND ( 'NONE', #31841, .T. ) ;
#4671=ORIENTED_EDGE ( 'NONE', *, *, #17308, .F. ) ;
#4672=CARTESIAN_POINT ( 'NONE',  ( 0.01230737760510393873, -0.07955613945526318620, 0.1377952755905511861 ) ) ;
#4673=CARTESIAN_POINT ( 'NONE',  ( 0.5660731898098425585, 4.766607801171850497E-17, 0.000000000000000000 ) ) ;
#4702=EDGE_CURVE ( 'NONE', #39448, #17524, #41605, .T. ) ;
#4731=CIRCLE ( 'NONE', #26220, 0.09842519685039370636 ) ;
#4735=CARTESIAN_POINT ( 'NONE',  ( 0.1636882031642129531, -0.08048656780410663736, 0.1394067246032472951 ) ) ;
#4756=CARTESIAN_POINT ( 'NONE',  ( 0.1644020957507537628, 0.08115590401245532937, -0.1405661490837558925 ) ) ;
#4758=EDGE_CURVE ( 'NONE', #27223, #9016, #38819, .T. ) ;
#4771=ORIENTED_EDGE ( 'NONE', *, *, #4540, .T. ) ;
#4778=AXIS2_PLACEMENT_3D ( 'NONE', #37976, #1528, #23830 ) ;
#4791=ORIENTED_EDGE ( 'NONE', *, *, #5136, .T. ) ;
#4819=ORIENTED_EDGE ( 'NONE', *, *, #46847, .T. ) ;
#4842=VERTEX_POINT ( 'NONE', #13649 ) ;
#4886=VERTEX_POINT ( 'NONE', #4251 ) ;
#4894=CARTESIAN_POINT ( 'NONE',  ( 0.1619907858920848209, -0.08803158632533415739, 0.1285577739723440804 ) ) ;
#4906=CARTESIAN_POINT ( 'NONE',  ( 0.2397010884053811242, 1.205361022782824954E-17, -0.09842519685039370636 ) ) ;
#4911=VERTEX_POINT ( 'NONE', #39734 ) ;
#4926=DIRECTION ( 'NONE',  ( 0.000000000000000000, -1.000000000000000000, 0.000000000000000000 ) ) ;
#4932=CARTESIAN_POINT ( 'NONE',  ( 0.000000000000000000, 1.478656101119254046E-17, 0.1377952755905511861 ) ) ;
#4949=FACE_OUTER_BOUND ( 'NONE', #20467, .T. ) ;
#4977=ADVANCED_FACE ( 'NONE', ( #11727 ), #31705, .T. ) ;
#4980=DIRECTION ( 'NONE',  ( -1.000000000000000000, 0.000000000000000000, 0.000000000000000000 ) ) ;
#4981=CARTESIAN_POINT ( 'NONE',  ( 0.1626913500753331410, -0.07997641687420671552, 0.1385231884448369366 ) ) ;
#4993=VERTEX_POINT ( 'NONE', #25860 ) ;
#4998=DIRECTION ( 'NONE',  ( -1.000000000000000000, 0.000000000000000000, 0.000000000000000000 ) ) ;
#5032=FACE_OUTER_BOUND ( 'NONE', #38704, .T. ) ;
#5036=VERTEX_POINT ( 'NONE', #40906 ) ;
#5037=ORIENTED_EDGE ( 'NONE', *, *, #424, .F. ) ;
#5105=ORIENTED_EDGE ( 'NONE', *, *, #46473, .T. ) ;
#5107=ORIENTED_EDGE ( 'NONE', *, *, #46612, .T. ) ;
#5114=ADVANCED_FACE ( 'NONE', ( #30201 ), #32568, .T. ) ;
#5136=EDGE_CURVE ( 'NONE', #40935, #12702, #19361, .T. ) ;
#5153=EDGE_CURVE ( 'NONE', #5859, #27600, #43219, .T. ) ;
#5199=DIRECTION ( 'NONE',  ( -1.000000000000000000, 0.000000000000000000, 0.000000000000000000 ) ) ;
#5209=CARTESIAN_POINT ( 'NONE',  ( 0.1624141299425573837, -0.07987878989917683581, 0.1383517943471609946 ) ) ;
#5217=DIRECTION ( 'NONE',  ( -1.000000000000000000, 0.000000000000000000, 0.000000000000000000 ) ) ;
#5235=EDGE_CURVE ( 'NONE', #17977, #3732, #31823, .T. ) ;
#5270=CARTESIAN_POINT ( 'NONE',  ( 0.6141732283464567121, 0.000000000000000000, 0.08090551181102362266 ) ) ;
#5273=AXIS2_PLACEMENT_3D ( 'NONE', #42105, #9312, #23935 ) ;
#5281=VECTOR ( 'NONE', #27506, 39.37007874015748143 ) ;
#5285=CARTESIAN_POINT ( 'NONE',  ( 0.1644020957507537628, -0.08115590401245532937, 0.1405661490837558925 ) ) ;
#5309=ORIENTED_EDGE ( 'NONE', *, *, #9903, .T. ) ;
#5321=CARTESIAN_POINT ( 'NONE',  ( 0.4934383202099732468, 4.616380251121755931E-17, 0.000000000000000000 ) ) ;
#5323=CARTESIAN_POINT ( 'NONE',  ( 0.0005737749932554291705, 0.1277779173640709587, 0.05427780112446529276 ) ) ;
#5349=DIRECTION ( 'NONE',  ( 0.000000000000000000, -1.000000000000000000, 0.000000000000000000 ) ) ;
#5351=MANIFOLD_SOLID_BREP ( 'ISO 4162 M5x10 Hex Flange Bolt', #25620 ) ;
#5365=EDGE_CURVE ( 'NONE', #40174, #12403, #17417, .T. ) ;
#5377=CONICAL_SURFACE ( 'NONE', #771, 0.09842519685039370636, 0.9599310885968824758 ) ;
#5385=ORIENTED_EDGE ( 'NONE', *, *, #12905, .T. ) ;
#5388=DIRECTION ( 'NONE',  ( 0.000000000000000000, 1.000000000000000000, 0.000000000000000000 ) ) ;
#5402=CARTESIAN_POINT ( 'NONE',  ( 0.1638905297737256739, -0.08063388607515166451, -0.1396625121104124179 ) ) ;
#5417=CARTESIAN_POINT ( 'NONE',  ( 0.01035225325188679837, -0.1557259041956392809, 0.005865373059643922728 ) ) ;
#5428=VERTEX_POINT ( 'NONE', #43320 ) ;
#5469=DIRECTION ( 'NONE',  ( 0.000000000000000000, 0.000000000000000000, 1.000000000000000000 ) ) ;
#5495=VERTEX_POINT ( 'NONE', #4005 ) ;
#5506=LINE ( 'NONE', #41663, #28999 ) ;
#5509=DIRECTION ( 'NONE',  ( 0.5735764363510447161, -0.8191520442889925757, 1.003171929053525486E-16 ) ) ;
#5510=LINE ( 'NONE', #34064, #13428 ) ;
#5538=ORIENTED_EDGE ( 'NONE', *, *, #7094, .T. ) ;
#5543=AXIS2_PLACEMENT_3D ( 'NONE', #5321, #30771, #16372 ) ;
#5566=EDGE_LOOP ( 'NONE', ( #14617, #8675, #21485, #2033, #25518 ) ) ;
#5568=CARTESIAN_POINT ( 'NONE',  ( 0.003062405574123812976, 0.1386494127069827775, 0.03544276884527174792 ) ) ;
#5593=CARTESIAN_POINT ( 'NONE',  ( 0.3604359965418638123, 4.466152701071653354E-17, 0.000000000000000000 ) ) ;
#5602=EDGE_LOOP ( 'NONE', ( #14159, #21326, #42089, #25238, #11299 ) ) ;
#5610=AXIS2_PLACEMENT_3D ( 'NONE', #38827, #38354, #24687 ) ;
#5619=DIRECTION ( 'NONE',  ( 0.000000000000000000, -1.000000000000000000, 0.000000000000000000 ) ) ;
#5665=DIRECTION ( 'NONE',  ( -1.000000000000000000, 0.000000000000000000, 0.000000000000000000 ) ) ;
#5679=ORIENTED_EDGE ( 'NONE', *, *, #41245, .F. ) ;
#5680=DIRECTION ( 'NONE',  ( 0.000000000000000000, -1.000000000000000000, 0.000000000000000000 ) ) ;
#5681=CARTESIAN_POINT ( 'NONE',  ( 0.001488395362858443375, 0.02696616380223046047, -0.1377975526281502716 ) ) ;
#5683=VERTEX_POINT ( 'NONE', #32877 ) ;
#5687=CARTESIAN_POINT ( 'NONE',  ( 0.2519685039370078705, 4.616380251121755931E-17, 0.000000000000000000 ) ) ;
#5689=DIRECTION ( 'NONE',  ( 0.000000000000000000, -1.000000000000000000, 0.000000000000000000 ) ) ;
#5694=EDGE_CURVE ( 'NONE', #16593, #38424, #33353, .T. ) ;
#5703=LINE ( 'NONE', #1624, #27682 ) ;
#5707=CARTESIAN_POINT ( 'NONE',  ( 0.1639941039450801552, -0.08071844585390765270, -0.1398101989048133320 ) ) ;
#5769=CARTESIAN_POINT ( 'NONE',  ( 0.006378642920439305843, 0.09116121678403278639, 0.1176987636582383229 ) ) ;
#5777=ORIENTED_EDGE ( 'NONE', *, *, #29916, .F. ) ;
#5793=ORIENTED_EDGE ( 'NONE', *, *, #16423, .F. ) ;
#5800=DIRECTION ( 'NONE',  ( 0.000000000000000000, 0.000000000000000000, -1.000000000000000000 ) ) ;
#5810=LINE ( 'NONE', #19942, #38422 ) ;
#5840=DIRECTION ( 'NONE',  ( -1.000000000000000000, 0.000000000000000000, 0.000000000000000000 ) ) ;
#5849=DIRECTION ( 'NONE',  ( -1.000000000000000000, 0.000000000000000000, 0.000000000000000000 ) ) ;
#5853=CYLINDRICAL_SURFACE ( 'NONE', #22042, 0.09842519685039370636 ) ;
#5859=VERTEX_POINT ( 'NONE', #28048 ) ;
#5875=VERTEX_POINT ( 'NONE', #32347 ) ;
#5915=CARTESIAN_POINT ( 'NONE',  ( 0.4509871776442260227, 4.466152701071653354E-17, 0.000000000000000000 ) ) ;
#5916=CARTESIAN_POINT ( 'NONE',  ( 0.003880704729684991260, 0.04358867701646648718, -0.1377950254940095709 ) ) ;
#5973=VERTEX_POINT ( 'NONE', #44730 ) ;
#5975=ORIENTED_EDGE ( 'NONE', *, *, #32989, .T. ) ;
#5983=LINE ( 'NONE', #35705, #10973 ) ;
#6007=DIRECTION ( 'NONE',  ( -1.000000000000000000, 0.000000000000000000, 0.000000000000000000 ) ) ;
#6014=VERTEX_POINT ( 'NONE', #27044 ) ;
#6040=FACE_OUTER_BOUND ( 'NONE', #19507, .T. ) ;
#6058=ORIENTED_EDGE ( 'NONE', *, *, #28100, .T. ) ;
#6067=DIRECTION ( 'NONE',  ( 1.000000000000000000, 0.000000000000000000, 0.000000000000000000 ) ) ;
#6075=VERTEX_POINT ( 'NONE', #25321 ) ;
#6076=DIRECTION ( 'NONE',  ( 0.000000000000000000, -1.000000000000000000, 0.000000000000000000 ) ) ;
#6083=VERTEX_POINT ( 'NONE', #17643 ) ;
#6091=EDGE_CURVE ( 'NONE', #45437, #40610, #36353, .T. ) ;
#6103=CARTESIAN_POINT ( 'NONE',  ( 0.2944196465027555387, 4.766607801171850497E-17, 0.000000000000000000 ) ) ;
#6120=AXIS2_PLACEMENT_3D ( 'NONE', #33768, #7849, #11000 ) ;
#6138=EDGE_LOOP ( 'NONE', ( #6952, #31631, #22767, #34065, #20754 ) ) ;
#6139=DIRECTION ( 'NONE',  ( -1.000000000000000000, 0.000000000000000000, 0.000000000000000000 ) ) ;
#6140=CARTESIAN_POINT ( 'NONE',  ( 0.3906197235759846786, 4.466152701071653354E-17, 0.000000000000000000 ) ) ;
#6144=ORIENTED_EDGE ( 'NONE', *, *, #24253, .T. ) ;
#6163=EDGE_CURVE ( 'NONE', #14042, #5036, #40960, .T. ) ;
#6170=ORIENTED_EDGE ( 'NONE', *, *, #17127, .F. ) ;
#6172=CARTESIAN_POINT ( 'NONE',  ( 0.000000000000000000, 0.000000000000000000, 0.000000000000000000 ) ) ;
#6174=EDGE_LOOP ( 'NONE', ( #2173, #15667, #25106, #39078, #21116 ) ) ;
#6175=CARTESIAN_POINT ( 'NONE',  ( 0.001477421097710441547, 0.1058998750574050018, -0.09216900433233464474 ) ) ;
#6219=CARTESIAN_POINT ( 'NONE',  ( 0.4811709046783464450, -0.09842519685039370636, 0.000000000000000000 ) ) ;
#6222=CARTESIAN_POINT ( 'NONE',  ( 0.1599045142068430958, -0.09467125711648119446, -0.1169792578046013332 ) ) ;
#6226=DIRECTION ( 'NONE',  ( 0.000000000000000000, -1.000000000000000000, 0.000000000000000000 ) ) ;
#6244=ORIENTED_EDGE ( 'NONE', *, *, #43925, .T. ) ;
#6258=ORIENTED_EDGE ( 'NONE', *, *, #8880, .T. ) ;
#6270=EDGE_CURVE ( 'NONE', #22975, #5495, #40297, .T. ) ;
#6285=ORIENTED_EDGE ( 'NONE', *, *, #19244, .T. ) ;
#6287=AXIS2_PLACEMENT_3D ( 'NONE', #17800, #38894, #21148 ) ;
#6293=DIRECTION ( 'NONE',  ( 1.000000000000000000, 0.000000000000000000, 0.000000000000000000 ) ) ;
#6315=CARTESIAN_POINT ( 'NONE',  ( 0.5962569168439626477, 1.205361022782824954E-17, -0.09842519685039370636 ) ) ;
#6317=EDGE_LOOP ( 'NONE', ( #36359, #15533, #3449, #13894 ) ) ;
#6340=CARTESIAN_POINT ( 'NONE',  ( 0.1620125744594652917, -0.07969860776396833768, -0.1380421452775067170 ) ) ;
#6356=LINE ( 'NONE', #46145, #23134 ) ;
#6405=DIRECTION ( 'NONE',  ( 1.000000000000000000, 0.000000000000000000, 0.000000000000000000 ) ) ;
#6408=CARTESIAN_POINT ( 'NONE',  ( 0.3849708276051176936, -0.09842519685039370636, 1.205361022782828805E-17 ) ) ;
#6419=DIRECTION ( 'NONE',  ( -1.000000000000000000, 0.000000000000000000, 0.000000000000000000 ) ) ;
#6449=CARTESIAN_POINT ( 'NONE',  ( 0.000000000000000000, 1.205361022782826802E-17, -0.09842519685039370636 ) ) ;
#6461=CARTESIAN_POINT ( 'NONE',  ( 0.1605229034655418219, -0.1502651944782444349, -0.02070802253792816683 ) ) ;
#6468=DIRECTION ( 'NONE',  ( -1.000000000000000000, 0.000000000000000000, 0.000000000000000000 ) ) ;
#6478=DIRECTION ( 'NONE',  ( 0.000000000000000000, -1.000000000000000000, 0.000000000000000000 ) ) ;
#6490=CONICAL_SURFACE ( 'NONE', #31018, 0.08090551181102362266, 0.9599310885968742602 ) ;
#6491=STYLED_ITEM ( 'NONE', ( #43289 ), #5351 ) ;
#6492=ORIENTED_EDGE ( 'NONE', *, *, #2496, .F. ) ;
#6499=VERTEX_POINT ( 'NONE', #1543 ) ;
#6522=B_SPLINE_CURVE_WITH_KNOTS ( 'NONE', 3,
 ( #41729, #38160, #41962, #15907, #5323, #19711, #23785, #34829, #16601, #38398, #5568, #34577, #1973, #1731 ),
 .UNSPECIFIED., .F., .F.,
 ( 4, 2, 2, 2, 2, 2, 4 ),
 ( 0.000000000000000000, 0.1250000000000001110, 0.2500000000000002220, 0.3750000000000003331, 0.4375000000000003886, 0.5000000000000004441, 1.000000000000000000 ),
 .UNSPECIFIED. ) ;
#6524=VECTOR ( 'NONE', #43023, 39.37007874015748143 ) ;
#6580=CARTESIAN_POINT ( 'NONE',  ( 0.1637325492971695717, -0.08225662854574337934, 0.1377952755905512972 ) ) ;
#6601=CARTESIAN_POINT ( 'NONE',  ( 0.1600813888244884409, -0.05392405859257631134, -0.1404791960284777486 ) ) ;
#6629=SURFACE_STYLE_USAGE ( .BOTH. , #10003 ) ;
#6649=CARTESIAN_POINT ( 'NONE',  ( 0.1633669211800945209, 0.08028805200495257866, 0.1390640086940820308 ) ) ;
#6653=FACE_OUTER_BOUND ( 'NONE', #5602, .T. ) ;
#6685=CARTESIAN_POINT ( 'NONE',  ( 0.5660731898098425585, -0.09842519685039370636, 1.205361022782828805E-17 ) ) ;
#6692=EDGE_CURVE ( 'NONE', #42489, #28106, #22537, .T. ) ;
#6698=CARTESIAN_POINT ( 'NONE',  ( 0.4755220087074803481, -0.09842519685039370636, 1.205361022782828805E-17 ) ) ;
#6699=DIRECTION ( 'NONE',  ( 0.000000000000000000, -1.000000000000000000, 0.000000000000000000 ) ) ;
#6701=EDGE_CURVE ( 'NONE', #19636, #19079, #41734, .T. ) ;
#6737=CARTESIAN_POINT ( 'NONE',  ( 0.000000000000000000, 0.000000000000000000, 0.09842519685039370636 ) ) ;
#6747=DIRECTION ( 'NONE',  ( -1.000000000000000000, 0.000000000000000000, 0.000000000000000000 ) ) ;
#6755=LINE ( 'NONE', #14206, #22297 ) ;
#6758=CARTESIAN_POINT ( 'NONE',  ( 0.1619802298550984954, 0.1595109072953912188, 2.917077808306172296E-06 ) ) ;
#6760=EDGE_CURVE ( 'NONE', #26132, #32405, #45568, .T. ) ;
#6799=CARTESIAN_POINT ( 'NONE',  ( 7.107660667885412143E-05, -0.1226968624036212790, -0.06307306040149587845 ) ) ;
#6804=EDGE_CURVE ( 'NONE', #4911, #18221, #47369, .T. ) ;
#6807=CARTESIAN_POINT ( 'NONE',  ( 0.4453382816733590377, 1.205361022782824954E-17, -0.09842519685039370636 ) ) ;
#6843=AXIS2_PLACEMENT_3D ( 'NONE', #20930, #35572, #46096 ) ;
#6848=DIRECTION ( 'NONE',  ( 0.000000000000000000, -1.000000000000000000, 0.000000000000000000 ) ) ;
#6872=CARTESIAN_POINT ( 'NONE',  ( 0.5236220472440944462, -0.08090551181102362266, 1.098083891755157578E-17 ) ) ;
#6873=EDGE_CURVE ( 'NONE', #38091, #29608, #21238, .T. ) ;
#6912=VECTOR ( 'NONE', #30881, 39.37007874015748143 ) ;
#6915=ADVANCED_FACE ( 'NONE', ( #18365 ), #2724, .T. ) ;
#6938=CARTESIAN_POINT ( 'NONE',  ( 0.1583858528204715732, -0.1020630898162695754, -0.1041062675987072944 ) ) ;
#6952=ORIENTED_EDGE ( 'NONE', *, *, #27421, .F. ) ;
#6956=ORIENTED_EDGE ( 'NONE', *, *, #4243, .F. ) ;
#6967=ORIENTED_EDGE ( 'NONE', *, *, #26978, .F. ) ;
#6972=DIRECTION ( 'NONE',  ( -1.000000000000000000, 0.000000000000000000, 0.000000000000000000 ) ) ;
#6973=ORIENTED_EDGE ( 'NONE', *, *, #24367, .F. ) ;
#6995=DIRECTION ( 'NONE',  ( -1.000000000000000000, 0.000000000000000000, 0.000000000000000000 ) ) ;
#6998=CARTESIAN_POINT ( 'NONE',  ( 0.1637019648151215312, 0.1609904454352970582, 5.735411161861398686E-09 ) ) ;
#7041=EDGE_CURVE ( 'NONE', #16843, #27712, #43697, .T. ) ;
#7045=DIRECTION ( 'NONE',  ( 0.000000000000000000, -1.000000000000000000, 0.000000000000000000 ) ) ;
#7059=CARTESIAN_POINT ( 'NONE',  ( 0.1602931993194442739, 0.07955613945526338049, -0.1377952755905511861 ) ) ;
#7079=VERTEX_POINT ( 'NONE', #43995 ) ;
#7082=CIRCLE ( 'NONE', #4778, 0.09842519685039370636 ) ;
#7084=CARTESIAN_POINT ( 'NONE',  ( 0.4632545931758527691, -0.08090551181102362266, 1.098083891755157578E-17 ) ) ;
#7094=EDGE_CURVE ( 'NONE', #12359, #10722, #7569, .T. ) ;
#7101=EDGE_LOOP ( 'NONE', ( #18028, #41010, #12496, #19859, #3742 ) ) ;
#7102=CARTESIAN_POINT ( 'NONE',  ( 0.5236220472440944462, 4.616380251121755931E-17, 0.000000000000000000 ) ) ;
#7104=DIRECTION ( 'NONE',  ( 0.5735764363510447161, 0.8191520442889925757, 0.000000000000000000 ) ) ;
#7120=AXIS2_PLACEMENT_3D ( 'NONE', #43599, #8541, #44947 ) ;
#7130=CARTESIAN_POINT ( 'NONE',  ( 0.4028871391076110364, -0.08090551181102362266, 0.000000000000000000 ) ) ;
#7133=LINE ( 'NONE', #2808, #37528 ) ;
#7134=B_SPLINE_CURVE_WITH_KNOTS ( 'NONE', 3,
 ( #14481, #43694, #6799, #36301, #46815, #21176, #24785, #21906, #36528, #17122, #35811, #32236, #28653, #13530 ),
 .UNSPECIFIED., .F., .F.,
 ( 4, 2, 2, 2, 2, 2, 4 ),
 ( 0.000000000000000000, 0.1249999999999997502, 0.2499999999999995004, 0.3749999999999992228, 0.4374999999999993894, 0.4999999999999995559, 1.000000000000000000 ),
 .UNSPECIFIED. ) ;
#7135=CARTESIAN_POINT ( 'NONE',  ( 0.4208034506101054895, -3.032960542342102697E-32, 0.09842519685039370636 ) ) ;
#7159=VECTOR ( 'NONE', #14374, 39.37007874015748143 ) ;
#7182=CARTESIAN_POINT ( 'NONE',  ( 0.3604359965418638123, 4.466152701071653354E-17, 0.000000000000000000 ) ) ;
#7185=ORIENTED_EDGE ( 'NONE', *, *, #41907, .T. ) ;
#7196=ORIENTED_EDGE ( 'NONE', *, *, #9960, .T. ) ;
#7199=ORIENTED_EDGE ( 'NONE', *, *, #31190, .T. ) ;
#7207=CARTESIAN_POINT ( 'NONE',  ( 0.003062405574123280416, -0.1000190445539560907, 0.1023525292014032806 ) ) ;
#7224=DIRECTION ( 'NONE',  ( -1.000000000000000000, 0.000000000000000000, 0.000000000000000000 ) ) ;
#7247=EDGE_CURVE ( 'NONE', #9117, #3818, #12732, .T. ) ;
#7252=CARTESIAN_POINT ( 'NONE',  ( 0.1571168540705091266, 0.1349219317376052774, 0.04713923310955830254 ) ) ;
#7263=AXIS2_PLACEMENT_3D ( 'NONE', #1136, #44972, #1369 ) ;
#7268=CARTESIAN_POINT ( 'NONE',  ( 0.2397010884053811242, 4.466152701071653354E-17, 0.000000000000000000 ) ) ;
#7280=EDGE_CURVE ( 'NONE', #34218, #7655, #7134, .T. ) ;
#7290=CIRCLE ( 'NONE', #14933, 0.09842519685039370636 ) ;
#7319=DIRECTION ( 'NONE',  ( -1.000000000000000000, 0.000000000000000000, 0.000000000000000000 ) ) ;
#7329=DIRECTION ( 'NONE',  ( 0.000000000000000000, -1.000000000000000000, 0.000000000000000000 ) ) ;
#7330=ORIENTED_EDGE ( 'NONE', *, *, #11662, .F. ) ;
#7345=ORIENTED_EDGE ( 'NONE', *, *, #21362, .T. ) ;
#7370=EDGE_CURVE ( 'NONE', #9016, #19819, #39356, .T. ) ;
#7375=EDGE_LOOP ( 'NONE', ( #12548, #10542, #25317 ) ) ;
#7386=VERTEX_POINT ( 'NONE', #39621 ) ;
#7390=DIRECTION ( 'NONE',  ( -1.000000000000000000, 0.000000000000000000, 0.000000000000000000 ) ) ;
#7403=DIRECTION ( 'NONE',  ( 0.000000000000000000, 1.000000000000000000, 0.000000000000000000 ) ) ;
#7439=FACE_OUTER_BOUND ( 'NONE', #1425, .T. ) ;
#7445=ORIENTED_EDGE ( 'NONE', *, *, #20397, .F. ) ;
#7452=ORIENTED_EDGE ( 'NONE', *, *, #38778, .T. ) ;
#7470=CARTESIAN_POINT ( 'NONE',  ( 0.1558458267876807191, -0.09164332750980157261, 0.1168596517594511774 ) ) ;
#7473=CARTESIAN_POINT ( 'NONE',  ( 0.5057057357416000487, 1.205361022782824954E-17, -0.09842519685039370636 ) ) ;
#7486=CARTESIAN_POINT ( 'NONE',  ( 0.3906197235759846786, 4.466152701071653354E-17, 0.000000000000000000 ) ) ;
#7508=CARTESIAN_POINT ( 'NONE',  ( 0.000000000000000000, 1.205361022782826802E-17, -0.09842519685039370636 ) ) ;
#7511=EDGE_CURVE ( 'NONE', #9744, #20867, #41631, .T. ) ;
#7519=CARTESIAN_POINT ( 'NONE',  ( 0.1602931993194442739, -0.07955613945526318620, 0.1377952755905511861 ) ) ;
#7523=EDGE_CURVE ( 'NONE', #7079, #27600, #43936, .T. ) ;
#7540=CARTESIAN_POINT ( 'NONE',  ( 0.5717220857807087109, 0.09842519685039370636, 1.205361022782828805E-17 ) ) ;
#7546=CARTESIAN_POINT ( 'NONE',  ( 0.1618536817988697474, -0.1553100982366859006, 0.01202753685200385302 ) ) ;
#7554=ORIENTED_EDGE ( 'NONE', *, *, #41843, .T. ) ;
#7561=CARTESIAN_POINT ( 'NONE',  ( 0.003583035186818364637, 0.1402401972141572029, -0.03270545601320399426 ) ) ;
#7569=LINE ( 'NONE', #26037, #24837 ) ;
#7602=AXIS2_PLACEMENT_3D ( 'NONE', #4226, #18855, #33512 ) ;
#7624=ORIENTED_EDGE ( 'NONE', *, *, #40079, .F. ) ;
#7627=AXIS2_PLACEMENT_3D ( 'NONE', #46738, #32640, #14410 ) ;
#7630=DIRECTION ( 'NONE',  ( 1.000000000000000000, 0.000000000000000000, 0.000000000000000000 ) ) ;
#7653=DIRECTION ( 'NONE',  ( 0.000000000000000000, -1.000000000000000000, 0.000000000000000000 ) ) ;
#7655=VERTEX_POINT ( 'NONE', #3684 ) ;
#7668=CARTESIAN_POINT ( 'NONE',  ( 0.0005737749932833635311, -0.1108949133173220275, 0.08352002191787535890 ) ) ;
#7675=CIRCLE ( 'NONE', #13804, 0.08090551181102362266 ) ;
#7677=CARTESIAN_POINT ( 'NONE',  ( 0.3425196850393700809, 4.616380251121755931E-17, 0.000000000000000000 ) ) ;
#7680=EDGE_LOOP ( 'NONE', ( #32414, #12904, #31395, #10232, #28916, #42307 ) ) ;
#7687=AXIS2_PLACEMENT_3D ( 'NONE', #32427, #6747, #39571 ) ;
#7701=CARTESIAN_POINT ( 'NONE',  ( 0.3000685424736224127, -0.09842519685039370636, 0.000000000000000000 ) ) ;
#7709=EDGE_CURVE ( 'NONE', #32411, #22975, #6522, .T. ) ;
#7720=CARTESIAN_POINT ( 'NONE',  ( 0.1571385178022536022, 0.1334669528786600612, -0.04962495032650500459 ) ) ;
#7748=LINE ( 'NONE', #25528, #44482 ) ;
#7757=CARTESIAN_POINT ( 'NONE',  ( 0.5358894627757212481, 4.766607801171850497E-17, 0.000000000000000000 ) ) ;
#7787=CARTESIAN_POINT ( 'NONE',  ( 0.5962569168439626477, -0.09842519685039370636, 1.205361022782828805E-17 ) ) ;
#7807=CIRCLE ( 'NONE', #8553, 0.09842519685039370636 ) ;
#7814=DIRECTION ( 'NONE',  ( 0.000000000000000000, 0.000000000000000000, 1.000000000000000000 ) ) ;
#7827=CARTESIAN_POINT ( 'NONE',  ( 0.1554371429169571495, 0.1330479920330144283, 0.04514466913490206706 ) ) ;
#7849=DIRECTION ( 'NONE',  ( -1.000000000000000000, 0.000000000000000000, 0.000000000000000000 ) ) ;
#7857=VECTOR ( 'NONE', #37893, 39.37007874015748143 ) ;
#7861=ORIENTED_EDGE ( 'NONE', *, *, #34177, .F. ) ;
#7864=AXIS2_PLACEMENT_3D ( 'NONE', #31844, #38071, #42363 ) ;
#7883=CARTESIAN_POINT ( 'NONE',  ( 0.1555210144364655711, 0.02856957593376195301, -0.1377952755905573479 ) ) ;
#7944=ORIENTED_EDGE ( 'NONE', *, *, #18516, .F. ) ;
#7948=CARTESIAN_POINT ( 'NONE',  ( 0.1594510458733777170, 0.1460701887063883264, 0.02793386226028452338 ) ) ;
#7955=DIRECTION ( 'NONE',  ( 0.000000000000000000, -1.000000000000000000, 0.000000000000000000 ) ) ;
#7979=EDGE_LOOP ( 'NONE', ( #27343, #3272, #28805, #7445, #43825 ) ) ;
#8037=VECTOR ( 'NONE', #34710, 39.37007874015748854 ) ;
#8041=DIRECTION ( 'NONE',  ( -1.000000000000000000, 0.000000000000000000, 0.000000000000000000 ) ) ;
#8047=DIRECTION ( 'NONE',  ( -0.5735764363510518216, 0.8191520442889876907, 1.003171929053519693E-16 ) ) ;
#8061=CARTESIAN_POINT ( 'NONE',  ( 0.1586955767088203406, 0.1469626601063697413, 0.02104375706135626356 ) ) ;
#8064=ORIENTED_EDGE ( 'NONE', *, *, #14890, .F. ) ;
#8068=CARTESIAN_POINT ( 'NONE',  ( 0.003857550520839538987, -0.1410454915399121656, 0.03130963158119893369 ) ) ;
#8075=LINE ( 'NONE', #3776, #29859 ) ;
#8098=VERTEX_POINT ( 'NONE', #9096 ) ;
#8105=CARTESIAN_POINT ( 'NONE',  ( 0.1644020957507537628, -0.08115590401245532937, 0.1405661490837558925 ) ) ;
#8118=ORIENTED_EDGE ( 'NONE', *, *, #13747, .F. ) ;
#8119=CARTESIAN_POINT ( 'NONE',  ( 0.1586952649960582662, -0.05525522230752598352, -0.1377952755905511306 ) ) ;
#8149=EDGE_LOOP ( 'NONE', ( #30196, #26286, #17746, #7185, #35437 ) ) ;
#8163=CARTESIAN_POINT ( 'NONE',  ( 0.5057057357416000487, 4.766607801171850497E-17, 0.000000000000000000 ) ) ;
#8176=CIRCLE ( 'NONE', #35001, 0.09842519685039370636 ) ;
#8188=CARTESIAN_POINT ( 'NONE',  ( 0.3123359580052492146, 4.616380251121755931E-17, 0.000000000000000000 ) ) ;
#8194=ORIENTED_EDGE ( 'NONE', *, *, #23654, .F. ) ;
#8202=LINE ( 'NONE', #22826, #28707 ) ;
#8203=CARTESIAN_POINT ( 'NONE',  ( 0.1558458267876820791, -0.1470250908559870007, -0.02093562383110287445 ) ) ;
#8223=EDGE_CURVE ( 'NONE', #43350, #36523, #47061, .T. ) ;
#8238=CARTESIAN_POINT ( 'NONE',  ( 0.3849708276051176936, 4.766607801171850497E-17, 0.000000000000000000 ) ) ;
#8247=ORIENTED_EDGE ( 'NONE', *, *, #15074, .T. ) ;
#8258=CARTESIAN_POINT ( 'NONE',  ( 0.1602931993194442739, 0.07955613945526338049, -0.1377952755905511861 ) ) ;
#8275=CARTESIAN_POINT ( 'NONE',  ( 0.005667817494309996054, -0.05302691243377098684, 0.1377926283226260096 ) ) ;
#8278=AXIS2_PLACEMENT_3D ( 'NONE', #43532, #6405, #21017 ) ;
#8281=VECTOR ( 'NONE', #12721, 39.37007874015748143 ) ;
#8290=DIRECTION ( 'NONE',  ( 0.000000000000000000, -0.8660254037844384856, 0.5000000000000003331 ) ) ;
#8294=DIRECTION ( 'NONE',  ( 1.000000000000000000, 0.000000000000000000, 0.000000000000000000 ) ) ;
#8319=DIRECTION ( 'NONE',  ( 0.000000000000000000, -1.000000000000000000, 0.000000000000000000 ) ) ;
#8325=EDGE_CURVE ( 'NONE', #649, #29529, #26428, .T. ) ;
#8340=CARTESIAN_POINT ( 'NONE',  ( 0.1555687797274982465, 0.1458529223346498038, 0.02296587926509188748 ) ) ;
#8358=VERTEX_POINT ( 'NONE', #246 ) ;
#8384=EDGE_CURVE ( 'NONE', #46509, #9744, #31012, .T. ) ;
#8387=DIRECTION ( 'NONE',  ( 1.000000000000000000, 0.000000000000000000, 0.000000000000000000 ) ) ;
#8388=ORIENTED_EDGE ( 'NONE', *, *, #7280, .F. ) ;
#8429=ORIENTED_EDGE ( 'NONE', *, *, #21536, .T. ) ;
#8430=FACE_OUTER_BOUND ( 'NONE', #41982, .T. ) ;
#8471=DIRECTION ( 'NONE',  ( 0.000000000000000000, 0.000000000000000000, -1.000000000000000000 ) ) ;
#8481=EDGE_LOOP ( 'NONE', ( #25324, #21341, #648, #44306, #43812 ) ) ;
#8515=FACE_OUTER_BOUND ( 'NONE', #31429, .T. ) ;
#8524=DIRECTION ( 'NONE',  ( 0.000000000000000000, -1.000000000000000000, 0.000000000000000000 ) ) ;
#8541=DIRECTION ( 'NONE',  ( 1.000000000000000000, 0.000000000000000000, 0.000000000000000000 ) ) ;
#8547=ADVANCED_FACE ( 'NONE', ( #5032 ), #11135, .T. ) ;
#8552=AXIS2_PLACEMENT_3D ( 'NONE', #39561, #7224, #32888 ) ;
#8553=AXIS2_PLACEMENT_3D ( 'NONE', #43303, #40170, #14562 ) ;
#8558=DIRECTION ( 'NONE',  ( -1.000000000000000000, 0.000000000000000000, 0.000000000000000000 ) ) ;
#8574=CARTESIAN_POINT ( 'NONE',  ( 0.1611065205236515141, -0.07959249327126025064, 0.1378515872677678056 ) ) ;
#8576=DIRECTION ( 'NONE',  ( -1.000000000000000000, 0.000000000000000000, 0.000000000000000000 ) ) ;
#8619=DIRECTION ( 'NONE',  ( 1.000000000000000000, 0.000000000000000000, 0.000000000000000000 ) ) ;
#8627=EDGE_LOOP ( 'NONE', ( #23487, #11973, #4025 ) ) ;
#8633=EDGE_CURVE ( 'NONE', #44803, #42642, #4300, .T. ) ;
#8646=PRODUCT_DEFINITION_FORMATION_WITH_SPECIFIED_SOURCE ( 'ANY', '', #1711, .NOT_KNOWN. ) ;
#8652=CIRCLE ( 'NONE', #237, 0.09842519685039370636 ) ;
#8667=VERTEX_POINT ( 'NONE', #12245 ) ;
#8668=CARTESIAN_POINT ( 'NONE',  ( 0.3000685424736224127, 4.466152701071653354E-17, 0.000000000000000000 ) ) ;
#8675=ORIENTED_EDGE ( 'NONE', *, *, #20352, .T. ) ;
#8679=CARTESIAN_POINT ( 'NONE',  ( 0.1637325577037128943, -0.07820587237429522942, -0.1401340067785763199 ) ) ;
#8701=CYLINDRICAL_SURFACE ( 'NONE', #42969, 0.09842519685039370636 ) ;
#8724=VERTEX_POINT ( 'NONE', #42392 ) ;
#8759=DIRECTION ( 'NONE',  ( 0.000000000000000000, -1.000000000000000000, 0.000000000000000000 ) ) ;
#8817=CONICAL_SURFACE ( 'NONE', #14966, 0.08090551181102362266, 0.9599310885968742602 ) ;
#8880=EDGE_CURVE ( 'NONE', #44147, #34498, #45506, .T. ) ;
#8887=FACE_OUTER_BOUND ( 'NONE', #45002, .T. ) ;
#8933=CARTESIAN_POINT ( 'NONE',  ( 0.5962569168439626477, 4.766607801171850497E-17, 0.000000000000000000 ) ) ;
#8976=ORIENTED_EDGE ( 'NONE', *, *, #7523, .F. ) ;
#8983=ORIENTED_EDGE ( 'NONE', *, *, #34003, .T. ) ;
#8984=AXIS2_PLACEMENT_3D ( 'NONE', #43956, #15218, #33684 ) ;
#8988=EDGE_LOOP ( 'NONE', ( #3445, #40701, #1381, #17064, #2300, #42339 ) ) ;
#8990=EDGE_LOOP ( 'NONE', ( #22295, #33327, #31614, #27327 ) ) ;
#9016=VERTEX_POINT ( 'NONE', #14827 ) ;
#9022=DIRECTION ( 'NONE',  ( 1.000000000000000000, 0.000000000000000000, 0.000000000000000000 ) ) ;
#9027=CARTESIAN_POINT ( 'NONE',  ( 0.2821522309711287368, 4.616380251121755931E-17, 0.000000000000000000 ) ) ;
#9031=VERTEX_POINT ( 'NONE', #36169 ) ;
#9041=AXIS2_PLACEMENT_3D ( 'NONE', #29977, #19133, #11740 ) ;
#9043=CARTESIAN_POINT ( 'NONE',  ( 0.3000685424736224127, 0.09842519685039370636, 1.205361022782828805E-17 ) ) ;
#9057=DIRECTION ( 'NONE',  ( 0.000000000000000000, -1.000000000000000000, 0.000000000000000000 ) ) ;
#9061=CARTESIAN_POINT ( 'NONE',  ( 0.2204724409448818867, 0.07955613945526338049, 0.1377952755905511861 ) ) ;
#9076=VECTOR ( 'NONE', #40627, 39.37007874015748143 ) ;
#9096=CARTESIAN_POINT ( 'NONE',  ( 0.4208034506101054895, -0.09842519685039370636, 0.000000000000000000 ) ) ;
#9104=CARTESIAN_POINT ( 'NONE',  ( 0.2944196465027555387, -0.09842519685039370636, 1.205361022782828805E-17 ) ) ;
#9117=VERTEX_POINT ( 'NONE', #21532 ) ;
#9119=CIRCLE ( 'NONE', #35900, 0.09842519685039370636 ) ;
#9129=CARTESIAN_POINT ( 'NONE',  ( 0.000000000000000000, 0.1193342091828950846, 0.06889763779527559306 ) ) ;
#9233=ORIENTED_EDGE ( 'NONE', *, *, #44717, .T. ) ;
#9243=DIRECTION ( 'NONE',  ( -1.000000000000000000, 0.000000000000000000, 0.000000000000000000 ) ) ;
#9254=DIRECTION ( 'NONE',  ( -1.000000000000000000, 0.000000000000000000, 0.000000000000000000 ) ) ;
#9290=DIRECTION ( 'NONE',  ( 0.000000000000000000, -1.000000000000000000, 0.000000000000000000 ) ) ;
#9291=AXIS2_PLACEMENT_3D ( 'NONE', #25082, #39674, #39920 ) ;
#9312=DIRECTION ( 'NONE',  ( 1.000000000000000000, 0.000000000000000000, 0.000000000000000000 ) ) ;
#9317=DIRECTION ( 'NONE',  ( -1.000000000000000000, 0.000000000000000000, 0.000000000000000000 ) ) ;
#9321=CARTESIAN_POINT ( 'NONE',  ( 0.3425196850393700809, 4.616380251121755931E-17, 0.000000000000000000 ) ) ;
#9325=CIRCLE ( 'NONE', #27719, 0.09842519685039370636 ) ;
#9362=CARTESIAN_POINT ( 'NONE',  ( 0.4208034506101054895, 4.466152701071653354E-17, 0.000000000000000000 ) ) ;
#9382=PLANE ( 'NONE',  #21599 ) ;
#9389=CIRCLE ( 'NONE', #26999, 0.08090551181102362266 ) ;
#9404=ORIENTED_EDGE ( 'NONE', *, *, #12026, .T. ) ;
#9413=AXIS2_PLACEMENT_3D ( 'NONE', #20140, #34786, #45763 ) ;
#9419=DIRECTION ( 'NONE',  ( -1.000000000000000000, 0.000000000000000000, 0.000000000000000000 ) ) ;
#9437=EDGE_LOOP ( 'NONE', ( #4819, #14648, #41256, #14511, #33723 ) ) ;
#9460=DIRECTION ( 'NONE',  ( 0.000000000000000000, -1.000000000000000000, 0.000000000000000000 ) ) ;
#9524=FACE_OUTER_BOUND ( 'NONE', #43286, .T. ) ;
#9529=EDGE_LOOP ( 'NONE', ( #20596, #40473, #7345, #33549, #13880 ) ) ;
#9564=VECTOR ( 'NONE', #8047, 39.37007874015748143 ) ;
#9580=LINE ( 'NONE', #45494, #8281 ) ;
#9595=EDGE_CURVE ( 'NONE', #42642, #11723, #41070, .T. ) ;
#9607=EDGE_CURVE ( 'NONE', #32653, #5495, #38053, .T. ) ;
#9612=CARTESIAN_POINT ( 'NONE',  ( 0.003857550520849534464, 0.09763768210239696932, 0.1064941629722592487 ) ) ;
#9638=VERTEX_POINT ( 'NONE', #15185 ) ;
#9670=CARTESIAN_POINT ( 'NONE',  ( 0.1602931993194444682, 0.1591122789105269553, 0.000000000000000000 ) ) ;
#9683=ORIENTED_EDGE ( 'NONE', *, *, #4574, .F. ) ;
#9695=ORIENTED_EDGE ( 'NONE', *, *, #3795, .F. ) ;
#9709=ORIENTED_EDGE ( 'NONE', *, *, #25272, .T. ) ;
#9724=FACE_OUTER_BOUND ( 'NONE', #8988, .T. ) ;
#9744=VERTEX_POINT ( 'NONE', #28458 ) ;
#9764=VERTEX_POINT ( 'NONE', #760 ) ;
#9767=DIRECTION ( 'NONE',  ( -1.000000000000000000, 0.000000000000000000, 0.000000000000000000 ) ) ;
#9786=DIRECTION ( 'NONE',  ( 0.000000000000000000, -1.000000000000000000, 0.000000000000000000 ) ) ;
#9797=CARTESIAN_POINT ( 'NONE',  ( -9.870935133357111912E-18, 0.1176498932187669128, -0.07181495862114489759 ) ) ;
#9806=CARTESIAN_POINT ( 'NONE',  ( 0.1645760587280559184, 0.1627877146821090915, 0.0008175030223464901328 ) ) ;
#9814=ADVANCED_FACE ( 'NONE', ( #33647 ), #40386, .F. ) ;
#9839=CIRCLE ( 'NONE', #37389, 0.09842519685039370636 ) ;
#9842=CYLINDRICAL_SURFACE ( 'NONE', #29404, 0.09842519685039370636 ) ;
#9843=CARTESIAN_POINT ( 'NONE',  ( 0.1564139474900951288, -0.1282476652664072125, -0.05864041697619068461 ) ) ;
#9856=EDGE_LOOP ( 'NONE', ( #26678, #40769, #33923, #32439, #35317 ) ) ;
#9865=AXIS2_PLACEMENT_3D ( 'NONE', #44234, #3760, #29462 ) ;
#9867=EDGE_LOOP ( 'NONE', ( #18578, #37880, #46875, #24819, #35262, #26001 ) ) ;
#9903=EDGE_CURVE ( 'NONE', #43974, #18113, #34244, .T. ) ;
#9904=VERTEX_POINT ( 'NONE', #10149 ) ;
#9911=LINE ( 'NONE', #32448, #34646 ) ;
#9918=VERTEX_POINT ( 'NONE', #18440 ) ;
#9934=VERTEX_POINT ( 'NONE', #212 ) ;
#9942=DIRECTION ( 'NONE',  ( 0.000000000000000000, -1.000000000000000000, 0.000000000000000000 ) ) ;
#9960=EDGE_CURVE ( 'NONE', #21404, #25167, #8176, .T. ) ;
#9976=CIRCLE ( 'NONE', #36756, 0.09842519685039370636 ) ;
#9981=ORIENTED_EDGE ( 'NONE', *, *, #1438, .T. ) ;
#9986=ORIENTED_EDGE ( 'NONE', *, *, #33414, .T. ) ;
#10003=SURFACE_SIDE_STYLE ('',( #35180 ) ) ;
#10019=CARTESIAN_POINT ( 'NONE',  ( 0.1555687797274980522, -0.05303742630350873760, 0.1377952755905511861 ) ) ;
#10035=FACE_OUTER_BOUND ( 'NONE', #3646, .T. ) ;
#10052=ADVANCED_FACE ( 'NONE', ( #12217 ), #32715, .T. ) ;
#10073=CARTESIAN_POINT ( 'NONE',  ( 0.1644020957507539848, -0.1623118080249112138, 7.560884646099310910E-18 ) ) ;
#10076=ORIENTED_EDGE ( 'NONE', *, *, #44341, .F. ) ;
#10095=CIRCLE ( 'NONE', #1672, 0.08090551181102362266 ) ;
#10118=CARTESIAN_POINT ( 'NONE',  ( 0.1610681406152271733, -0.1591122530826964421, -4.473511402309723835E-08 ) ) ;
#10121=EDGE_CURVE ( 'NONE', #40935, #23379, #10503, .T. ) ;
#10149=CARTESIAN_POINT ( 'NONE',  ( 0.4453382816733590377, 0.09842519685039370636, 0.000000000000000000 ) ) ;
#10155=DIRECTION ( 'NONE',  ( -1.000000000000000000, 0.000000000000000000, 0.000000000000000000 ) ) ;
#10171=CIRCLE ( 'NONE', #26266, 0.09842519685039370636 ) ;
#10181=DIRECTION ( 'NONE',  ( -1.000000000000000000, 0.000000000000000000, 0.000000000000000000 ) ) ;
#10193=AXIS2_PLACEMENT_3D ( 'NONE', #33375, #26885, #4556 ) ;
#10194=CARTESIAN_POINT ( 'NONE',  ( 0.1645805304145094572, 0.08212604421147362554, 0.1405696318538273704 ) ) ;
#10217=ORIENTED_EDGE ( 'NONE', *, *, #34003, .F. ) ;
#10219=CARTESIAN_POINT ( 'NONE',  ( 0.5236220472440944462, 4.616380251121755931E-17, 0.000000000000000000 ) ) ;
#10220=ORIENTED_EDGE ( 'NONE', *, *, #42560, .T. ) ;
#10232=ORIENTED_EDGE ( 'NONE', *, *, #10750, .F. ) ;
#10236=DIRECTION ( 'NONE',  ( 0.000000000000000000, -1.000000000000000000, 0.000000000000000000 ) ) ;
#10242=B_SPLINE_CURVE_WITH_KNOTS ( 'NONE', 3,
 ( #39959, #44489, #175, #33054, #22001, #880, #36404, #25844, #10772, #36858, #18175, #29943 ),
 .UNSPECIFIED., .F., .F.,
 ( 4, 2, 2, 2, 2, 4 ),
 ( 0.000000000000000000, 0.2500000000000002220, 0.3750000000000004441, 0.4375000000000005551, 0.5000000000000006661, 1.000000000000000000 ),
 .UNSPECIFIED. ) ;
#10247=DIRECTION ( 'NONE',  ( -1.000000000000000000, 0.000000000000000000, 0.000000000000000000 ) ) ;
#10266=CARTESIAN_POINT ( 'NONE',  ( 0.1564216623530369499, 0.006801955215764789002, -0.1403857474672217109 ) ) ;
#10297=ADVANCED_FACE ( 'NONE', ( #2580 ), #20337, .T. ) ;
#10302=ADVANCED_FACE ( 'NONE', ( #42588 ), #28156, .T. ) ;
#10305=DIRECTION ( 'NONE',  ( -1.000000000000000000, 0.000000000000000000, 0.000000000000000000 ) ) ;
#10350=AXIS2_PLACEMENT_3D ( 'NONE', #44745, #4980, #9057 ) ;
#10364=CARTESIAN_POINT ( 'NONE',  ( 0.1643592525012025352, -0.1621847908751006817, -1.511614865314615023E-06 ) ) ;
#10461=DIRECTION ( 'NONE',  ( -1.000000000000000000, 0.000000000000000000, 0.000000000000000000 ) ) ;
#10463=B_SPLINE_CURVE_WITH_KNOTS ( 'NONE', 3,
 ( #26318, #44247, #40874, #37796, #15055 ),
 .UNSPECIFIED., .F., .F.,
 ( 4, 1, 4 ),
 ( 0.000000000000000000, 0.002020725942163689639, 0.004041451884327384482 ),
 .UNSPECIFIED. ) ;
#10478=FACE_OUTER_BOUND ( 'NONE', #8990, .T. ) ;
#10503=CIRCLE ( 'NONE', #25025, 0.08090551181102362266 ) ;
#10508=CARTESIAN_POINT ( 'NONE',  ( 0.1637019648159556695, 0.08049521775124826584, 0.1394218183822737434 ) ) ;
#10538=CONICAL_SURFACE ( 'NONE', #8984, 0.08090551181102362266, 0.9599310885968742602 ) ;
#10542=ORIENTED_EDGE ( 'NONE', *, *, #6270, .T. ) ;
#10564=EDGE_CURVE ( 'NONE', #10722, #27975, #38096, .T. ) ;
#10603=CARTESIAN_POINT ( 'NONE',  ( 0.2944196465027555387, -3.032960542342102697E-32, 0.09842519685039370636 ) ) ;
#10623=DIRECTION ( 'NONE',  ( -1.000000000000000000, 0.000000000000000000, 0.000000000000000000 ) ) ;
#10633=ORIENTED_EDGE ( 'NONE', *, *, #30492, .F. ) ;
#10653=ORIENTED_EDGE ( 'NONE', *, *, #1913, .F. ) ;
#10665=AXIS2_PLACEMENT_3D ( 'NONE', #20000, #45152, #12369 ) ;
#10692=EDGE_LOOP ( 'NONE', ( #2925, #17829, #35491, #8429, #28059 ) ) ;
#10694=EDGE_CURVE ( 'NONE', #5036, #9764, #29693, .T. ) ;
#10716=DIRECTION ( 'NONE',  ( -1.000000000000000000, 0.000000000000000000, 0.000000000000000000 ) ) ;
#10722=VERTEX_POINT ( 'NONE', #11155 ) ;
#10730=ORIENTED_EDGE ( 'NONE', *, *, #3795, .T. ) ;
#10750=EDGE_CURVE ( 'NONE', #9904, #26132, #18182, .T. ) ;
#10752=DIRECTION ( 'NONE',  ( 1.000000000000000000, 0.000000000000000000, 0.000000000000000000 ) ) ;
#10772=CARTESIAN_POINT ( 'NONE',  ( 0.1587185860253795822, 0.04237460976003461915, 0.1404529029258638206 ) ) ;
#10779=VECTOR ( 'NONE', #21921, 39.37007874015748854 ) ;
#10806=CARTESIAN_POINT ( 'NONE',  ( 0.2642359194686346169, -3.032960542342102697E-32, 0.09842519685039370636 ) ) ;
#10816=ORIENTED_EDGE ( 'NONE', *, *, #9607, .F. ) ;
#10823=CARTESIAN_POINT ( 'NONE',  ( 9.848703297471225088E-18, -0.1176498932187602098, 0.07181495862115655493 ) ) ;
#10833=AXIS2_PLACEMENT_3D ( 'NONE', #29514, #44060, #25868 ) ;
#10835=DIRECTION ( 'NONE',  ( 1.000000000000000000, 0.000000000000000000, 0.000000000000000000 ) ) ;
#10836=ORIENTED_EDGE ( 'NONE', *, *, #26096, .F. ) ;
#10854=ADVANCED_FACE ( 'NONE', ( #36549 ), #10538, .T. ) ;
#10857=DIRECTION ( 'NONE',  ( 0.000000000000000000, -1.000000000000000000, 0.000000000000000000 ) ) ;
#10898=ORIENTED_EDGE ( 'NONE', *, *, #14082, .T. ) ;
#10930=CARTESIAN_POINT ( 'NONE',  ( 0.002334186094749960728, 0.03366073001697469924, 0.1377957753753820402 ) ) ;
#10937=CARTESIAN_POINT ( 'NONE',  ( 0.1605321103696192298, -0.05726506528273173774, -0.1404876550525108458 ) ) ;
#10939=ORIENTED_EDGE ( 'NONE', *, *, #26804, .F. ) ;
#10943=ORIENTED_EDGE ( 'NONE', *, *, #17127, .T. ) ;
#10947=AXIS2_PLACEMENT_3D ( 'NONE', #6172, #28019, #27322 ) ;
#10952=VECTOR ( 'NONE', #40512, 39.37007874015748143 ) ;
#10973=VECTOR ( 'NONE', #14135, 39.37007874015748854 ) ;
#11000=DIRECTION ( 'NONE',  ( 0.000000000000000000, -1.000000000000000000, 0.000000000000000000 ) ) ;
#11059=CARTESIAN_POINT ( 'NONE',  ( 7.107660667886486858E-05, -0.1159713038039308503, 0.07472206960544050536 ) ) ;
#11062=ORIENTED_EDGE ( 'NONE', *, *, #7709, .F. ) ;
#11065=ADVANCED_FACE ( 'NONE', ( #576 ), #32506, .T. ) ;
#11072=TOROIDAL_SURFACE ( 'NONE', #22540, 0.2047244094488188948, 0.01968503937007873988 ) ;
#11078=DIRECTION ( 'NONE',  ( 0.000000000000000000, -1.000000000000000000, 0.000000000000000000 ) ) ;
#11092=CARTESIAN_POINT ( 'NONE',  ( 0.1564216623530370331, 8.908831420875236139E-13, 0.1403857474672218497 ) ) ;
#11098=DIRECTION ( 'NONE',  ( -0.5735764363510518216, -0.8191520442889876907, 0.000000000000000000 ) ) ;
#11111=CARTESIAN_POINT ( 'NONE',  ( 0.1571168540704948324, 0.1082847392564992711, -0.09327620385769608280 ) ) ;
#11125=ORIENTED_EDGE ( 'NONE', *, *, #24244, .T. ) ;
#11135=CONICAL_SURFACE ( 'NONE', #2684, 0.09842519685039370636, 0.9599310885968824758 ) ;
#11140=CARTESIAN_POINT ( 'NONE',  ( 0.3547871005709968273, -0.09842519685039370636, 1.205361022782828805E-17 ) ) ;
#11155=CARTESIAN_POINT ( 'NONE',  ( 0.5660731898098425585, -3.032960542342102697E-32, 0.09842519685039370636 ) ) ;
#11168=DIRECTION ( 'NONE',  ( -1.000000000000000000, 0.000000000000000000, 0.000000000000000000 ) ) ;
#11169=DIRECTION ( 'NONE',  ( -1.000000000000000000, 0.000000000000000000, 0.000000000000000000 ) ) ;
#11216=CARTESIAN_POINT ( 'NONE',  ( 0.003583035186807825324, -0.1402401972141327779, 0.03270545601322783630 ) ) ;
#11218=CARTESIAN_POINT ( 'NONE',  ( 0.3246033735368759610, 4.766607801171850497E-17, 0.000000000000000000 ) ) ;
#11234=CARTESIAN_POINT ( 'NONE',  ( 0.3302522695077432791, 4.466152701071653354E-17, 0.000000000000000000 ) ) ;
#11240=LINE ( 'NONE', #29010, #33309 ) ;
#11246=VERTEX_POINT ( 'NONE', #15949 ) ;
#11299=ORIENTED_EDGE ( 'NONE', *, *, #12527, .F. ) ;
#11330=CARTESIAN_POINT ( 'NONE',  ( 0.1620125769272121319, 0.07969870020048158699, -0.1380420919957745518 ) ) ;
#11347=ADVANCED_FACE ( 'NONE', ( #35567 ), #13982, .F. ) ;
#11363=CARTESIAN_POINT ( 'NONE',  ( 0.001106411046829887477, -0.1060985490479111754, -0.09184399599051619456 ) ) ;
#11368=ADVANCED_FACE ( 'NONE', ( #24768 ), #5853, .T. ) ;
#11391=ORIENTED_EDGE ( 'NONE', *, *, #29238, .T. ) ;
#11396=CARTESIAN_POINT ( 'NONE',  ( 0.1573602050224713056, -0.1351575695123996834, 0.04671412196467249894 ) ) ;
#11399=ORIENTED_EDGE ( 'NONE', *, *, #40917, .T. ) ;
#11412=CARTESIAN_POINT ( 'NONE',  ( 0.5415383587465882886, 4.466152701071653354E-17, 0.000000000000000000 ) ) ;
#11416=VERTEX_POINT ( 'NONE', #36732 ) ;
#11421=CIRCLE ( 'NONE', #17526, 0.09842519685039370636 ) ;
#11429=DIRECTION ( 'NONE',  ( -1.000000000000000000, 0.000000000000000000, 0.000000000000000000 ) ) ;
#11442=CARTESIAN_POINT ( 'NONE',  ( 0.1527640389977631963, 0.1049476924225429125, 0.09381581576814683465 ) ) ;
#11452=ORIENTED_EDGE ( 'NONE', *, *, #35074, .T. ) ;
#11475=EDGE_CURVE ( 'NONE', #46256, #8098, #28872, .T. ) ;
#11491=LINE ( 'NONE', #22497, #21277 ) ;
#11521=CARTESIAN_POINT ( 'NONE',  ( 0.5415383587465882886, -0.09842519685039370636, 0.000000000000000000 ) ) ;
#11530=DIRECTION ( 'NONE',  ( -0.7071067811865454633, 0.000000000000000000, 0.7071067811865494601 ) ) ;
#11539=DIRECTION ( 'NONE',  ( -1.000000000000000000, 0.000000000000000000, 0.000000000000000000 ) ) ;
#11546=EDGE_CURVE ( 'NONE', #16593, #4842, #15957, .T. ) ;
#11553=LINE ( 'NONE', #4319, #42971 ) ;
#11577=EDGE_CURVE ( 'NONE', #19741, #11246, #35342, .T. ) ;
#11583=CONICAL_SURFACE ( 'NONE', #39868, 0.09842519685039370636, 0.9599310885968824758 ) ;
#11590=ORIENTED_EDGE ( 'NONE', *, *, #34224, .T. ) ;
#11601=CARTESIAN_POINT ( 'NONE',  ( 0.01230737760510134012, -0.07955613945526751607, -0.1377952755905511861 ) ) ;
#11607=EDGE_CURVE ( 'NONE', #26601, #31651, #21245, .T. ) ;
#11653=VECTOR ( 'NONE', #18017, 39.37007874015748854 ) ;
#11654=CONICAL_SURFACE ( 'NONE', #13924, 0.08090551181102362266, 0.9599310885968742602 ) ;
#11662=EDGE_CURVE ( 'NONE', #46614, #42394, #23558, .T. ) ;
#11663=EDGE_LOOP ( 'NONE', ( #41281, #15030, #23544, #30924, #14040 ) ) ;
#11723=VERTEX_POINT ( 'NONE', #25897 ) ;
#11724=CONICAL_SURFACE ( 'NONE', #7864, 0.08090551181102362266, 0.7853981633974511656 ) ;
#11727=FACE_OUTER_BOUND ( 'NONE', #44189, .T. ) ;
#11740=DIRECTION ( 'NONE',  ( 0.000000000000000000, -1.000000000000000000, 0.000000000000000000 ) ) ;
#11744=CARTESIAN_POINT ( 'NONE',  ( 0.1596648500867438869, 0.05551101047364393609, -0.1404739575301623966 ) ) ;
#11753=DIRECTION ( 'NONE',  ( -1.000000000000000000, 0.000000000000000000, 0.000000000000000000 ) ) ;
#11754=CONICAL_SURFACE ( 'NONE', #37744, 0.2114570894355444486, 1.221730476396037490 ) ;
#11755=ORIENTED_EDGE ( 'NONE', *, *, #18650, .T. ) ;
#11795=DIRECTION ( 'NONE',  ( 0.000000000000000000, -1.000000000000000000, 0.000000000000000000 ) ) ;
#11800=DIRECTION ( 'NONE',  ( 0.000000000000000000, -1.000000000000000000, 0.000000000000000000 ) ) ;
#11824=CARTESIAN_POINT ( 'NONE',  ( 0.1586955767088446545, -0.1469626601063630800, -0.02104375706137109892 ) ) ;
#11839=ORIENTED_EDGE ( 'NONE', *, *, #34177, .T. ) ;
#11851=B_SPLINE_CURVE_WITH_KNOTS ( 'NONE', 3,
 ( #19856, #10019, #34738, #2342, #34483 ),
 .UNSPECIFIED., .F., .F.,
 ( 4, 1, 4 ),
 ( 0.000000000000000000, 0.002020725942163684868, 0.004041451884327374941 ),
 .UNSPECIFIED. ) ;
#11868=CARTESIAN_POINT ( 'NONE',  ( 0.008412300615072984891, 0.06606319696301089783, 0.1377952755905512139 ) ) ;
#11872=CARTESIAN_POINT ( 'NONE',  ( 0.1577586585109163331, -0.1377137394883627131, 0.04231661445894344120 ) ) ;
#11898=CARTESIAN_POINT ( 'NONE',  ( 0.006360881761561069936, -0.05628132561868937761, 0.1377921049841277779 ) ) ;
#11899=DIRECTION ( 'NONE',  ( 0.000000000000000000, 0.000000000000000000, 1.000000000000000000 ) ) ;
#11927=CARTESIAN_POINT ( 'NONE',  ( 9.037241287634464769E-18, -0.1260561954211091296, 0.05725481610291012491 ) ) ;
#11934=ORIENTED_EDGE ( 'NONE', *, *, #29473, .T. ) ;
#11959=ORIENTED_EDGE ( 'NONE', *, *, #33254, .F. ) ;
#11965=CARTESIAN_POINT ( 'NONE',  ( 0.1602931993194442739, -0.07955613945526318620, 0.1377952755905511861 ) ) ;
#11967=CARTESIAN_POINT ( 'NONE',  ( 0.3727034120734909473, 4.616380251121755931E-17, 0.000000000000000000 ) ) ;
#11973=ORIENTED_EDGE ( 'NONE', *, *, #33362, .T. ) ;
#11984=CARTESIAN_POINT ( 'NONE',  ( 0.4934383202099732468, 4.616380251121755931E-17, 0.000000000000000000 ) ) ;
#11991=ORIENTED_EDGE ( 'NONE', *, *, #16294, .T. ) ;
#12026=EDGE_CURVE ( 'NONE', #16941, #8098, #36591, .T. ) ;
#12064=ORIENTED_EDGE ( 'NONE', *, *, #29800, .T. ) ;
#12076=CARTESIAN_POINT ( 'NONE',  ( 0.005379252439919633005, -0.05299006067052474539, -0.1377950963417848562 ) ) ;
#12091=CARTESIAN_POINT ( 'NONE',  ( 0.1644020957507537628, -0.08115590401245532937, 0.1405661490837558925 ) ) ;
#12116=VERTEX_POINT ( 'NONE', #34989 ) ;
#12136=ADVANCED_FACE ( 'NONE', ( #34506 ), #39023, .T. ) ;
#12148=CARTESIAN_POINT ( 'NONE',  ( 0.2642359194686346169, 4.766607801171850497E-17, 0.000000000000000000 ) ) ;
#12150=DIRECTION ( 'NONE',  ( -1.000000000000000000, 0.000000000000000000, 0.000000000000000000 ) ) ;
#12164=CARTESIAN_POINT ( 'NONE',  ( 0.2204724409448818867, -0.07955613945526357478, -0.1377952755905511861 ) ) ;
#12180=DIRECTION ( 'NONE',  ( 0.000000000000000000, -1.000000000000000000, 0.000000000000000000 ) ) ;
#12189=EDGE_CURVE ( 'NONE', #17392, #8358, #18245, .T. ) ;
#12215=ORIENTED_EDGE ( 'NONE', *, *, #16423, .T. ) ;
#12217=FACE_OUTER_BOUND ( 'NONE', #40358, .T. ) ;
#12245=CARTESIAN_POINT ( 'NONE',  ( 0.1602931993194442739, -0.07955613945526318620, 0.1377952755905511861 ) ) ;
#12246=VERTEX_POINT ( 'NONE', #13626 ) ;
#12247=EDGE_CURVE ( 'NONE', #28970, #23848, #9580, .T. ) ;
#12249=EDGE_LOOP ( 'NONE', ( #28262, #46662, #17289, #13117, #41411 ) ) ;
#12275=DIRECTION ( 'NONE',  ( -1.000000000000000000, 0.000000000000000000, 0.000000000000000000 ) ) ;
#12279=DIRECTION ( 'NONE',  ( 0.000000000000000000, -1.000000000000000000, 0.000000000000000000 ) ) ;
#12312=ADVANCED_FACE ( 'NONE', ( #36687 ), #40019, .T. ) ;
#12315=DIRECTION ( 'NONE',  ( 1.000000000000000000, 0.000000000000000000, 0.000000000000000000 ) ) ;
#12316=CARTESIAN_POINT ( 'NONE',  ( 0.004734662961589819648, -0.09521559318209203704, -0.1106847963722246697 ) ) ;
#12321=CARTESIAN_POINT ( 'NONE',  ( 0.003028377451660003734, -0.03839001012990030104, -0.1377950774391751565 ) ) ;
#12333=DIRECTION ( 'NONE',  ( -1.000000000000000000, 0.000000000000000000, 0.000000000000000000 ) ) ;
#12336=DIRECTION ( 'NONE',  ( 0.000000000000000000, -1.000000000000000000, 0.000000000000000000 ) ) ;
#12339=DIRECTION ( 'NONE',  ( -1.000000000000000000, 0.000000000000000000, 0.000000000000000000 ) ) ;
#12359=VERTEX_POINT ( 'NONE', #33589 ) ;
#12369=DIRECTION ( 'NONE',  ( 0.000000000000000000, -1.000000000000000000, 0.000000000000000000 ) ) ;
#12380=VECTOR ( 'NONE', #32639, 39.37007874015748143 ) ;
#12403=VERTEX_POINT ( 'NONE', #26392 ) ;
#12421=AXIS2_PLACEMENT_3D ( 'NONE', #19972, #5840, #30561 ) ;
#12438=CARTESIAN_POINT ( 'NONE',  ( 0.5057057357416000487, -0.09842519685039370636, 1.205361022782828805E-17 ) ) ;
#12496=ORIENTED_EDGE ( 'NONE', *, *, #6873, .T. ) ;
#12497=CIRCLE ( 'NONE', #46116, 0.09842519685039370636 ) ;
#12511=DIRECTION ( 'NONE',  ( 0.000000000000000000, 0.000000000000000000, 1.000000000000000000 ) ) ;
#12515=CONICAL_SURFACE ( 'NONE', #7120, 0.1377952755905511861, 1.047197551196598297 ) ;
#12527=EDGE_CURVE ( 'NONE', #35936, #27975, #5506, .T. ) ;
#12531=FACE_OUTER_BOUND ( 'NONE', #27623, .T. ) ;
#12548=ORIENTED_EDGE ( 'NONE', *, *, #7709, .T. ) ;
#12555=CARTESIAN_POINT ( 'NONE',  ( 0.5538057742782149795, -0.08090551181102362266, 0.000000000000000000 ) ) ;
#12560=( BOUNDED_SURFACE ( )  B_SPLINE_SURFACE ( 3, 2, ( 
 ( #15159, #21628, #36262 ),
 ( #18497, #32675, #21382 ),
 ( #29, #40285, #29353 ),
 ( #43895, #25716, #29803 ),
 ( #7470, #22090, #44350 ),
 ( #33154, #14919, #38129 ) ),
 .UNSPECIFIED., .F., .F., .F. ) 
 B_SPLINE_SURFACE_WITH_KNOTS ( ( 4, 2, 4 ),
 ( 3, 3 ),
 ( 0.01651999345535504898, 0.01858032176739835006, 0.02064065007944164767 ),
 ( 0.000000000000000000, 1.000000000000000000 ),
 .UNSPECIFIED. ) 
 GEOMETRIC_REPRESENTATION_ITEM ( )  RATIONAL_B_SPLINE_SURFACE ( (
 ( 1.000000000000000000, 0.8047781103519390244, 1.000000000000000000),
 ( 1.000000000000000000, 0.8123785825609630695, 1.000000000000000000),
 ( 1.000000000000000000, 0.8190671539781260169, 1.000000000000000000),
 ( 1.000000000000000000, 0.8192352254841890336, 1.000000000000000000),
 ( 1.000000000000000000, 0.8126129677206329616, 1.000000000000000000),
 ( 1.000000000000000000, 0.8047712537969730073, 1.000000000000000000) ) ) 
 REPRESENTATION_ITEM ( '' )  SURFACE ( )  ) ;
#12563=DIRECTION ( 'NONE',  ( -1.000000000000000000, 0.000000000000000000, 0.000000000000000000 ) ) ;
#12611=EDGE_LOOP ( 'NONE', ( #10076, #34340, #17706, #21844, #24523 ) ) ;
#12616=DIRECTION ( 'NONE',  ( 0.000000000000000000, 1.000000000000000000, 0.000000000000000000 ) ) ;
#12618=AXIS2_PLACEMENT_3D ( 'NONE', #21962, #14780, #32299 ) ;
#12627=DIRECTION ( 'NONE',  ( 0.000000000000000000, -1.000000000000000000, 0.000000000000000000 ) ) ;
#12644=CARTESIAN_POINT ( 'NONE',  ( 0.01230737760510409486, -0.1591122789105269553, -1.990515434288500257E-18 ) ) ;
#12646=EDGE_CURVE ( 'NONE', #29582, #15059, #17486, .T. ) ;
#12650=CIRCLE ( 'NONE', #41782, 0.09842519685039370636 ) ;
#12658=VECTOR ( 'NONE', #45025, 39.37007874015748143 ) ;
#12663=LINE ( 'NONE', #16249, #6912 ) ;
#12677=CARTESIAN_POINT ( 'NONE',  ( 0.1642909303726545756, -0.08091908006343519200, 0.1401559281493469367 ) ) ;
#12690=DIRECTION ( 'NONE',  ( -1.000000000000000000, 0.000000000000000000, 0.000000000000000000 ) ) ;
#12702=VERTEX_POINT ( 'NONE', #31408 ) ;
#12713=EDGE_LOOP ( 'NONE', ( #11959, #32452, #16975, #25153 ) ) ;
#12721=DIRECTION ( 'NONE',  ( -1.000000000000000000, 0.000000000000000000, 0.000000000000000000 ) ) ;
#12732=CIRCLE ( 'NONE', #30981, 0.09842519685039370636 ) ;
#12737=DIRECTION ( 'NONE',  ( 0.000000000000000000, -1.000000000000000000, 0.000000000000000000 ) ) ;
#12748=CARTESIAN_POINT ( 'NONE',  ( 0.01035225325190847548, 0.08294251417010607697, 0.1319299025309686735 ) ) ;
#12750=EDGE_CURVE ( 'NONE', #42394, #827, #2366, .T. ) ;
#12767=DIRECTION ( 'NONE',  ( 0.000000000000000000, 1.000000000000000000, 0.000000000000000000 ) ) ;
#12780=ORIENTED_EDGE ( 'NONE', *, *, #15074, .F. ) ;
#12808=ORIENTED_EDGE ( 'NONE', *, *, #6701, .F. ) ;
#12838=CARTESIAN_POINT ( 'NONE',  ( 0.000000000000000000, 0.000000000000000000, 0.09842519685039370636 ) ) ;
#12853=ORIENTED_EDGE ( 'NONE', *, *, #22552, .F. ) ;
#12904=ORIENTED_EDGE ( 'NONE', *, *, #37158, .T. ) ;
#12905=EDGE_CURVE ( 'NONE', #5683, #24890, #9839, .T. ) ;
#12909=LINE ( 'NONE', #20774, #18771 ) ;
#12975=CARTESIAN_POINT ( 'NONE',  ( 0.1564216623530370331, 8.908831420875236139E-13, 0.1403857474672218497 ) ) ;
#12982=AXIS2_PLACEMENT_3D ( 'NONE', #1930, #6468, #43602 ) ;
#13006=ORIENTED_EDGE ( 'NONE', *, *, #22350, .T. ) ;
#13012=EDGE_CURVE ( 'NONE', #27963, #23901, #22470, .T. ) ;
#13016=VECTOR ( 'NONE', #27338, 39.37007874015748854 ) ;
#13023=DIRECTION ( 'NONE',  ( 0.5735764363510447161, 0.8191520442889925757, 0.000000000000000000 ) ) ;
#13026=CIRCLE ( 'NONE', #35997, 0.09842519685039370636 ) ;
#13029=CARTESIAN_POINT ( 'NONE',  ( 0.5660731898098425585, 4.766607801171850497E-17, 0.000000000000000000 ) ) ;
#13050=EDGE_LOOP ( 'NONE', ( #19829, #2078, #34637, #40438, #36100 ) ) ;
#13090=CONICAL_SURFACE ( 'NONE', #24554, 0.08090551181102362266, 0.9599310885968742602 ) ;
#13097=CARTESIAN_POINT ( 'NONE',  ( 0.5717220857807087109, 4.466152701071653354E-17, 0.000000000000000000 ) ) ;
#13103=DIRECTION ( 'NONE',  ( -1.000000000000000000, 0.000000000000000000, 0.000000000000000000 ) ) ;
#13115=CARTESIAN_POINT ( 'NONE',  ( 0.008625679036560286728, -0.1524122562640881362, 0.01160289892419911692 ) ) ;
#13117=ORIENTED_EDGE ( 'NONE', *, *, #29800, .F. ) ;
#13142=CYLINDRICAL_SURFACE ( 'NONE', #16946, 0.09842519685039370636 ) ;
#13158=VERTEX_POINT ( 'NONE', #9043 ) ;
#13172=EDGE_CURVE ( 'NONE', #23076, #23848, #1428, .T. ) ;
#13222=CIRCLE ( 'NONE', #33938, 0.09842519685039370636 ) ;
#13231=VECTOR ( 'NONE', #45769, 39.37007874015748143 ) ;
#13256=VECTOR ( 'NONE', #46558, 39.37007874015748143 ) ;
#13263=CARTESIAN_POINT ( 'NONE',  ( 0.5113546317124669782, 4.466152701071653354E-17, 0.000000000000000000 ) ) ;
#13281=DIRECTION ( 'NONE',  ( 0.000000000000000000, -1.000000000000000000, 0.000000000000000000 ) ) ;
#13283=VERTEX_POINT ( 'NONE', #44731 ) ;
#13308=ORIENTED_EDGE ( 'NONE', *, *, #1438, .F. ) ;
#13315=EDGE_LOOP ( 'NONE', ( #44383, #38974, #19729, #33181, #9683 ) ) ;
#13324=DIRECTION ( 'NONE',  ( 0.000000000000000000, 0.000000000000000000, 1.000000000000000000 ) ) ;
#13325=CARTESIAN_POINT ( 'NONE',  ( 0.000000000000000000, 1.205361022782826802E-17, -0.09842519685039370636 ) ) ;
#13326=CARTESIAN_POINT ( 'NONE',  ( 0.1630380172108122638, -0.08011826877085716225, -0.1387687780145144545 ) ) ;
#13330=EDGE_CURVE ( 'NONE', #31112, #32653, #1483, .T. ) ;
#13345=ORIENTED_EDGE ( 'NONE', *, *, #31190, .F. ) ;
#13363=CIRCLE ( 'NONE', #31766, 0.1377952755905511861 ) ;
#13369=CONICAL_SURFACE ( 'NONE', #19467, 0.08090551181102362266, 0.9599310885968742602 ) ;
#13390=CARTESIAN_POINT ( 'NONE',  ( 0.4934383202099732468, 0.08090551181102362266, 0.000000000000000000 ) ) ;
#13412=DIRECTION ( 'NONE',  ( 0.000000000000000000, -1.000000000000000000, 0.000000000000000000 ) ) ;
#13428=VECTOR ( 'NONE', #37630, 39.37007874015748143 ) ;
#13439=FACE_OUTER_BOUND ( 'NONE', #26043, .T. ) ;
#13440=DIRECTION ( 'NONE',  ( -1.000000000000000000, 0.000000000000000000, 0.000000000000000000 ) ) ;
#13450=ORIENTED_EDGE ( 'NONE', *, *, #43336, .T. ) ;
#13476=ADVANCED_FACE ( 'NONE', ( #9524 ), #634, .T. ) ;
#13481=CARTESIAN_POINT ( 'NONE',  ( 0.1631287816244539335, -0.1603246120961979437, 5.150759842524385501E-07 ) ) ;
#13482=EDGE_CURVE ( 'NONE', #25167, #46714, #9119, .T. ) ;
#13495=CARTESIAN_POINT ( 'NONE',  ( 0.01230737760510407577, 0.1591122789105269553, -1.502406898952441074E-18 ) ) ;
#13514=CARTESIAN_POINT ( 'NONE',  ( 0.2821522309711287368, 0.08090551181102362266, 9.908067607274841931E-18 ) ) ;
#13518=ORIENTED_EDGE ( 'NONE', *, *, #6692, .T. ) ;
#13525=EDGE_LOOP ( 'NONE', ( #34874, #24093, #16663, #44854, #34630 ) ) ;
#13527=ORIENTED_EDGE ( 'NONE', *, *, #960, .F. ) ;
#13530=CARTESIAN_POINT ( 'NONE',  ( 0.01230737760510409486, -0.1591122789105269553, -1.990515434288500257E-18 ) ) ;
#13532=ADVANCED_FACE ( 'NONE', ( #36355 ), #3967, .T. ) ;
#13543=CARTESIAN_POINT ( 'NONE',  ( 0.4028871391076110364, -0.08090551181102362266, 1.098083891755157578E-17 ) ) ;
#13545=CARTESIAN_POINT ( 'NONE',  ( 0.000000000000000000, 0.000000000000000000, 0.09842519685039370636 ) ) ;
#13554=ORIENTED_EDGE ( 'NONE', *, *, #14082, .F. ) ;
#13563=CARTESIAN_POINT ( 'NONE',  ( 0.1644020957507539848, -0.08115590401245571794, -0.1405661490837558925 ) ) ;
#13598=DIRECTION ( 'NONE',  ( 0.000000000000000000, 1.000000000000000000, 0.000000000000000000 ) ) ;
#13626=CARTESIAN_POINT ( 'NONE',  ( 0.5113546317124669782, -0.09842519685039370636, 0.000000000000000000 ) ) ;
#13627=B_SPLINE_CURVE_WITH_KNOTS ( 'NONE', 3,
 ( #28025, #9797, #20798, #24406, #28742, #39008, #6175, #39472, #2576, #35439, #17215, #31850, #46429, #446 ),
 .UNSPECIFIED., .F., .F.,
 ( 4, 2, 2, 2, 2, 2, 4 ),
 ( 0.000000000000000000, 0.1249999999999994449, 0.2499999999999991673, 0.3749999999999988898, 0.4374999999999987232, 0.4999999999999985567, 1.000000000000000000 ),
 .UNSPECIFIED. ) ;
#13644=ORIENTED_EDGE ( 'NONE', *, *, #42513, .F. ) ;
#13649=CARTESIAN_POINT ( 'NONE',  ( 0.2397010884053811242, -0.09842519685039370636, 0.000000000000000000 ) ) ;
#13662=EDGE_LOOP ( 'NONE', ( #45052, #25788, #10730, #43452, #1111 ) ) ;
#13675=DIRECTION ( 'NONE',  ( 0.000000000000000000, -1.000000000000000000, 0.000000000000000000 ) ) ;
#13685=AXIS2_PLACEMENT_3D ( 'NONE', #38541, #24396, #9786 ) ;
#13710=B_SPLINE_CURVE_WITH_KNOTS ( 'NONE', 3,
 ( #12644, #5417, #13115, #34215, #27748, #15277, #3546, #8068, #11216, #44014, #33034, #11927, #32798 ),
 .UNSPECIFIED., .F., .F.,
 ( 4, 2, 2, 1, 2, 2, 4 ),
 ( 0.000000000000000000, 0.2500000000000013323, 0.3750000000000019984, 0.4375000000000021649, 0.4687500000000021649, 0.5000000000000021094, 1.000000000000000000 ),
 .UNSPECIFIED. ) ;
#13726=CONICAL_SURFACE ( 'NONE', #31375, 0.09842519685039370636, 0.9599310885968824758 ) ;
#13747=EDGE_CURVE ( 'NONE', #649, #15059, #45398, .T. ) ;
#13750=ADVANCED_FACE ( 'NONE', ( #19293 ), #40493, .T. ) ;
#13755=VECTOR ( 'NONE', #37180, 39.37007874015748143 ) ;
#13756=DIRECTION ( 'NONE',  ( 0.000000000000000000, -1.000000000000000000, 0.000000000000000000 ) ) ;
#13775=CARTESIAN_POINT ( 'NONE',  ( 0.1610681367838507072, -0.07955608858867080357, -0.1377952755905511584 ) ) ;
#13789=AXIS2_PLACEMENT_3D ( 'NONE', #24337, #38936, #19552 ) ;
#13804=AXIS2_PLACEMENT_3D ( 'NONE', #45715, #24184, #19862 ) ;
#13829=CARTESIAN_POINT ( 'NONE',  ( 0.3849708276051176936, 0.09842519685039370636, 0.000000000000000000 ) ) ;
#13880=ORIENTED_EDGE ( 'NONE', *, *, #7041, .F. ) ;
#13885=EDGE_CURVE ( 'NONE', #22837, #3723, #42030, .T. ) ;
#13894=ORIENTED_EDGE ( 'NONE', *, *, #46906, .F. ) ;
#13921=AXIS2_PLACEMENT_3D ( 'NONE', #19722, #31243, #45820 ) ;
#13924=AXIS2_PLACEMENT_3D ( 'NONE', #9321, #42582, #31145 ) ;
#13949=CARTESIAN_POINT ( 'NONE',  ( 0.4028871391076110364, 0.08090551181102362266, 9.908067607274841931E-18 ) ) ;
#13982=PLANE ( 'NONE',  #43447 ) ;
#13995=AXIS2_PLACEMENT_3D ( 'NONE', #41526, #44901, #23368 ) ;
#14002=ORIENTED_EDGE ( 'NONE', *, *, #10121, .F. ) ;
#14028=CARTESIAN_POINT ( 'NONE',  ( 0.5962569168439626477, 4.766607801171850497E-17, 0.000000000000000000 ) ) ;
#14034=CIRCLE ( 'NONE', #30895, 0.2047244094488188948 ) ;
#14040=ORIENTED_EDGE ( 'NONE', *, *, #28100, .F. ) ;
#14042=VERTEX_POINT ( 'NONE', #6315 ) ;
#14067=CONICAL_SURFACE ( 'NONE', #30929, 0.09842519685039370636, 0.9599310885968824758 ) ;
#14082=EDGE_CURVE ( 'NONE', #12702, #27624, #39704, .T. ) ;
#14132=DIRECTION ( 'NONE',  ( 0.000000000000000000, -1.000000000000000000, 0.000000000000000000 ) ) ;
#14135=DIRECTION ( 'NONE',  ( 0.5735764363510447161, -0.8191520442889925757, 1.003171929053525486E-16 ) ) ;
#14158=ORIENTED_EDGE ( 'NONE', *, *, #28652, .T. ) ;
#14159=ORIENTED_EDGE ( 'NONE', *, *, #35720, .F. ) ;
#14191=CARTESIAN_POINT ( 'NONE',  ( 0.1634463062180389892, -0.1606610259913433258, 5.268451237904698604E-07 ) ) ;
#14206=CARTESIAN_POINT ( 'NONE',  ( 0.6141732283464567121, 9.908067607274841931E-18, -0.08090551181102362266 ) ) ;
#14287=CARTESIAN_POINT ( 'NONE',  ( 0.1564216623530370054, -0.01359171937732193448, -0.1403857474672217664 ) ) ;
#14309=EDGE_CURVE ( 'NONE', #5973, #20673, #28646, .T. ) ;
#14317=CARTESIAN_POINT ( 'NONE',  ( 0.002396928536207490728, -0.03415735691519130451, -0.1377928489248547994 ) ) ;
#14350=ADVANCED_FACE ( 'NONE', ( #40545 ), #22903, .T. ) ;
#14374=DIRECTION ( 'NONE',  ( -1.000000000000000000, 0.000000000000000000, 0.000000000000000000 ) ) ;
#14381=CARTESIAN_POINT ( 'NONE',  ( 0.1643592241977981927, -0.08109105093932868213, -0.1404568431685181695 ) ) ;
#14384=DIRECTION ( 'NONE',  ( 0.000000000000000000, 0.000000000000000000, 1.000000000000000000 ) ) ;
#14397=ORIENTED_EDGE ( 'NONE', *, *, #2323, .F. ) ;
#14408=CARTESIAN_POINT ( 'NONE',  ( 0.2204724409448818867, 0.07955613945526338049, 0.1377952755905511861 ) ) ;
#14410=DIRECTION ( 'NONE',  ( 0.000000000000000000, 0.000000000000000000, 1.000000000000000000 ) ) ;
#14422=ORIENTED_EDGE ( 'NONE', *, *, #13012, .T. ) ;
#14481=CARTESIAN_POINT ( 'NONE',  ( 0.000000000000000000, -0.1193342091828950846, -0.06889763779527559306 ) ) ;
#14484=AXIS2_PLACEMENT_3D ( 'NONE', #2917, #25224, #32674 ) ;
#14511=ORIENTED_EDGE ( 'NONE', *, *, #20013, .F. ) ;
#14543=ORIENTED_EDGE ( 'NONE', *, *, #18190, .F. ) ;
#14562=DIRECTION ( 'NONE',  ( 0.000000000000000000, -1.000000000000000000, 0.000000000000000000 ) ) ;
#14591=CIRCLE ( 'NONE', #1568, 0.09842519685039370636 ) ;
#14615=ADVANCED_FACE ( 'NONE', ( #10035 ), #13726, .T. ) ;
#14617=ORIENTED_EDGE ( 'NONE', *, *, #1308, .T. ) ;
#14618=ORIENTED_EDGE ( 'NONE', *, *, #39156, .F. ) ;
#14631=EDGE_LOOP ( 'NONE', ( #5975, #35684, #26323, #46704, #18224 ) ) ;
#14639=CARTESIAN_POINT ( 'NONE',  ( 0.002317115957668979941, -0.1025658529674488839, 0.09794161051882110947 ) ) ;
#14648=ORIENTED_EDGE ( 'NONE', *, *, #36692, .F. ) ;
#14720=AXIS2_PLACEMENT_3D ( 'NONE', #30202, #1857, #16265 ) ;
#14727=CARTESIAN_POINT ( 'NONE',  ( 0.1602931993194444682, -0.1591122789105269553, 0.000000000000000000 ) ) ;
#14734=LINE ( 'NONE', #37003, #37384 ) ;
#14749=CARTESIAN_POINT ( 'NONE',  ( 0.01230737760510397689, 0.07955613945526338049, 0.1377952755905511861 ) ) ;
#14773=CARTESIAN_POINT ( 'NONE',  ( 0.003457534521343477024, 0.1398629656505299135, -0.03335920195937951138 ) ) ;
#14780=DIRECTION ( 'NONE',  ( -1.000000000000000000, 0.000000000000000000, 0.000000000000000000 ) ) ;
#14810=CARTESIAN_POINT ( 'NONE',  ( 0.2204724409448818867, 1.205361022782826802E-17, -0.09842519685039370636 ) ) ;
#14812=B_SPLINE_CURVE_WITH_KNOTS ( 'NONE', 3,
 ( #33786, #902, #15563, #8340, #32307 ),
 .UNSPECIFIED., .F., .F.,
 ( 4, 1, 4 ),
 ( 0.000000000000000000, 0.002020725942163689639, 0.004041451884327384482 ),
 .UNSPECIFIED. ) ;
#14814=DIRECTION ( 'NONE',  ( -1.000000000000000000, 0.000000000000000000, 0.000000000000000000 ) ) ;
#14817=CARTESIAN_POINT ( 'NONE',  ( 0.2204724409448818867, 0.000000000000000000, 0.09842519685039370636 ) ) ;
#14827=CARTESIAN_POINT ( 'NONE',  ( 0.3547871005709968273, 1.205361022782824954E-17, -0.09842519685039370636 ) ) ;
#14831=VERTEX_POINT ( 'NONE', #14817 ) ;
#14859=CIRCLE ( 'NONE', #39323, 0.09842519685039370636 ) ;
#14890=EDGE_CURVE ( 'NONE', #27963, #45437, #37464, .T. ) ;
#14898=VECTOR ( 'NONE', #40221, 39.37007874015748143 ) ;
#14915=CARTESIAN_POINT ( 'NONE',  ( 0.4755220087074803481, 4.766607801171850497E-17, 0.000000000000000000 ) ) ;
#14919=CARTESIAN_POINT ( 'NONE',  ( 0.1637370714319410780, -0.07819377357278597951, 0.1401549625175002034 ) ) ;
#14923=CARTESIAN_POINT ( 'NONE',  ( 0.1583858528204730998, 0.1020630898162672995, 0.1041062675987153296 ) ) ;
#14926=CARTESIAN_POINT ( 'NONE',  ( 0.1631287816250558131, 0.08016185997947827824, -0.1388454444657191700 ) ) ;
#14933=AXIS2_PLACEMENT_3D ( 'NONE', #30644, #23436, #9290 ) ;
#14943=ORIENTED_EDGE ( 'NONE', *, *, #21420, .T. ) ;
#14951=EDGE_CURVE ( 'NONE', #9031, #39913, #38998, .T. ) ;
#14961=EDGE_CURVE ( 'NONE', #40610, #12359, #42801, .T. ) ;
#14966=AXIS2_PLACEMENT_3D ( 'NONE', #16021, #5199, #44967 ) ;
#15002=AXIS2_PLACEMENT_3D ( 'NONE', #3548, #21758, #21990 ) ;
#15004=CARTESIAN_POINT ( 'NONE',  ( 0.1631207519397639694, -0.08463291909044137751, 0.1344936127548389537 ) ) ;
#15016=CIRCLE ( 'NONE', #19566, 0.2114570894355444486 ) ;
#15021=CARTESIAN_POINT ( 'NONE',  ( 0.008625679036625592128, 0.1524122562642153123, -0.01160289892401995641 ) ) ;
#15030=ORIENTED_EDGE ( 'NONE', *, *, #2845, .T. ) ;
#15046=CARTESIAN_POINT ( 'NONE',  ( 0.1559665883013474363, 0.09131739707178464227, 0.1174241798378301144 ) ) ;
#15055=CARTESIAN_POINT ( 'NONE',  ( 0.1602931993194442739, 0.07955613945526338049, -0.1377952755905511861 ) ) ;
#15059=VERTEX_POINT ( 'NONE', #37200 ) ;
#15065=ADVANCED_FACE ( 'NONE', ( #1236 ), #26909, .T. ) ;
#15074=EDGE_CURVE ( 'NONE', #13158, #7079, #16084, .T. ) ;
#15093=ORIENTED_EDGE ( 'NONE', *, *, #43868, .T. ) ;
#15105=CARTESIAN_POINT ( 'NONE',  ( 0.5415383587465882886, 4.466152701071653354E-17, 0.000000000000000000 ) ) ;
#15125=DIRECTION ( 'NONE',  ( -1.000000000000000000, 0.000000000000000000, 0.000000000000000000 ) ) ;
#15152=CARTESIAN_POINT ( 'NONE',  ( 0.2821522309711287368, 4.616380251121755931E-17, 0.000000000000000000 ) ) ;
#15159=CARTESIAN_POINT ( 'NONE',  ( 0.1608764814808673338, -0.1607246848665348227, -0.002792769038232397350 ) ) ;
#15161=CARTESIAN_POINT ( 'NONE',  ( 0.5057057357416000487, 4.766607801171850497E-17, 0.000000000000000000 ) ) ;
#15170=ADVANCED_FACE ( 'NONE', ( #8430 ), #38847, .T. ) ;
#15182=DIRECTION ( 'NONE',  ( -1.000000000000000000, 0.000000000000000000, 0.000000000000000000 ) ) ;
#15185=CARTESIAN_POINT ( 'NONE',  ( 0.5358894627757212481, 1.205361022782824954E-17, -0.09842519685039370636 ) ) ;
#15194=DIRECTION ( 'NONE',  ( 0.000000000000000000, -1.000000000000000000, 0.000000000000000000 ) ) ;
#15218=DIRECTION ( 'NONE',  ( -1.000000000000000000, 0.000000000000000000, 0.000000000000000000 ) ) ;
#15235=CARTESIAN_POINT ( 'NONE',  ( 0.1605229034655323017, -0.09306627081912521859, 0.1197794644537587411 ) ) ;
#15266=DIRECTION ( 'NONE',  ( -1.000000000000000000, 0.000000000000000000, 0.000000000000000000 ) ) ;
#15271=ADVANCED_FACE ( 'NONE', ( #42192 ), #19085, .T. ) ;
#15273=CIRCLE ( 'NONE', #12982, 0.08090551181102362266 ) ;
#15277=CARTESIAN_POINT ( 'NONE',  ( 0.004734662961502830204, -0.1434636420619076758, 0.02711672434618991184 ) ) ;
#15292=DIRECTION ( 'NONE',  ( -1.000000000000000000, 0.000000000000000000, 0.000000000000000000 ) ) ;
#15318=ORIENTED_EDGE ( 'NONE', *, *, #28067, .F. ) ;
#15328=EDGE_LOOP ( 'NONE', ( #23045, #41791, #6973, #23452, #15735 ) ) ;
#15368=EDGE_LOOP ( 'NONE', ( #36075, #6492, #27475, #29725, #5385 ) ) ;
#15379=LINE ( 'NONE', #40736, #25743 ) ;
#15384=ADVANCED_FACE ( 'NONE', ( #7439 ), #3801, .T. ) ;
#15396=CARTESIAN_POINT ( 'NONE',  ( 0.1600714537641689805, 0.1485828198929401989, 0.02360507234453745537 ) ) ;
#15418=VECTOR ( 'NONE', #25103, 39.37007874015748143 ) ;
#15420=CONICAL_SURFACE ( 'NONE', #3142, 0.09842519685039370636, 0.9599310885968824758 ) ;
#15422=CARTESIAN_POINT ( 'NONE',  ( 0.1559665883013232335, -0.09131739707178367083, -0.1174241798378320850 ) ) ;
#15425=ORIENTED_EDGE ( 'NONE', *, *, #41756, .F. ) ;
#15473=CARTESIAN_POINT ( 'NONE',  ( 0.1592537043533252261, -0.09805585504228191140, 0.1110897172141831063 ) ) ;
#15485=CIRCLE ( 'NONE', #26179, 0.09842519685039370636 ) ;
#15488=CARTESIAN_POINT ( 'NONE',  ( 0.001106411046829904390, 0.1325885082367477263, -0.04596204078519285086 ) ) ;
#15513=CARTESIAN_POINT ( 'NONE',  ( 0.000000000000000000, 1.205361022782826802E-17, -0.09842519685039370636 ) ) ;
#15515=CARTESIAN_POINT ( 'NONE',  ( 0.1637370714319413278, 0.1604746447930040509, -0.002359686926948953087 ) ) ;
#15529=CARTESIAN_POINT ( 'NONE',  ( 0.1555687797274982465, -0.1458529223346498038, -0.02296587926509181116 ) ) ;
#15533=ORIENTED_EDGE ( 'NONE', *, *, #23850, .F. ) ;
#15541=DIRECTION ( 'NONE',  ( 0.000000000000000000, -1.000000000000000000, 0.000000000000000000 ) ) ;
#15546=EDGE_CURVE ( 'NONE', #11723, #42642, #22170, .T. ) ;
#15563=CARTESIAN_POINT ( 'NONE',  ( 0.1498753904841986506, 0.1193342091828952928, 0.06889763779527559306 ) ) ;
#15581=CARTESIAN_POINT ( 'NONE',  ( 0.1608809399420511876, -0.08280523680090119687, -0.1377952755905511861 ) ) ;
#15582=CARTESIAN_POINT ( 'NONE',  ( 0.4028871391076110364, 0.08090551181102362266, 0.000000000000000000 ) ) ;
#15614=ORIENTED_EDGE ( 'NONE', *, *, #18938, .T. ) ;
#15635=PLANE ( 'NONE',  #21697 ) ;
#15655=ORIENTED_EDGE ( 'NONE', *, *, #40139, .F. ) ;
#15661=( BOUNDED_SURFACE ( )  B_SPLINE_SURFACE ( 3, 2, ( 
 ( #4216, #394, #40865 ),
 ( #15046, #29696, #44237 ),
 ( #11442, #26059, #26309 ),
 ( #40629, #7827, #18845 ),
 ( #33747, #8061, #37290 ),
 ( #856, #15515, #23874 ) ),
 .UNSPECIFIED., .F., .F., .T. ) 
 B_SPLINE_SURFACE_WITH_KNOTS ( ( 4, 2, 4 ),
 ( 3, 3 ),
 ( 0.01651999345535504898, 0.01858032176739835006, 0.02064065007944164767 ),
 ( 0.000000000000000000, 1.000000000000000000 ),
 .UNSPECIFIED. ) 
 GEOMETRIC_REPRESENTATION_ITEM ( )  RATIONAL_B_SPLINE_SURFACE ( (
 ( 1.000000000000000000, 0.8047781103519390244, 1.000000000000000000),
 ( 1.000000000000000000, 0.8123785825606629762, 1.000000000000000000),
 ( 1.000000000000000000, 0.8190671539785250310, 1.000000000000000000),
 ( 1.000000000000000000, 0.8192352254837930170, 1.000000000000000000),
 ( 1.000000000000000000, 0.8126129677209299462, 1.000000000000000000),
 ( 1.000000000000000000, 0.8047712537969730073, 1.000000000000000000) ) ) 
 REPRESENTATION_ITEM ( '' )  SURFACE ( )  ) ;
#15666=AXIS2_PLACEMENT_3D ( 'NONE', #23026, #34304, #23514 ) ;
#15667=ORIENTED_EDGE ( 'NONE', *, *, #1913, .T. ) ;
#15671=EDGE_LOOP ( 'NONE', ( #35774, #9404, #30807, #36200, #17262, #41632 ) ) ;
#15716=DIRECTION ( 'NONE',  ( 0.000000000000000000, 0.000000000000000000, -1.000000000000000000 ) ) ;
#15718=CARTESIAN_POINT ( 'NONE',  ( 0.5660731898098425585, 4.766607801171850497E-17, 0.000000000000000000 ) ) ;
#15725=EDGE_CURVE ( 'NONE', #27223, #13283, #13026, .T. ) ;
#15727=ADVANCED_FACE ( 'NONE', ( #30005 ), #5377, .T. ) ;
#15733=ORIENTED_EDGE ( 'NONE', *, *, #42258, .F. ) ;
#15735=ORIENTED_EDGE ( 'NONE', *, *, #16611, .F. ) ;
#15759=CONICAL_SURFACE ( 'NONE', #44792, 0.08090551181102362266, 0.7853981633974511656 ) ;
#15776=ORIENTED_EDGE ( 'NONE', *, *, #39156, .T. ) ;
#15784=DIRECTION ( 'NONE',  ( 0.000000000000000000, -1.000000000000000000, 0.000000000000000000 ) ) ;
#15794=VERTEX_POINT ( 'NONE', #9104 ) ;
#15816=CARTESIAN_POINT ( 'NONE',  ( 0.1526812815691464542, -0.02763205629824401835, -0.1377952755905511861 ) ) ;
#15821=VERTEX_POINT ( 'NONE', #42606 ) ;
#15830=ORIENTED_EDGE ( 'NONE', *, *, #34649, .F. ) ;
#15831=ORIENTED_EDGE ( 'NONE', *, *, #10750, .T. ) ;
#15851=DIRECTION ( 'NONE',  ( 0.000000000000000000, 1.000000000000000000, 0.000000000000000000 ) ) ;
#15863=CARTESIAN_POINT ( 'NONE',  ( 0.008625679036592873508, 0.08625453335789746989, 0.1261914363108047332 ) ) ;
#15874=FACE_OUTER_BOUND ( 'NONE', #35512, .T. ) ;
#15882=CARTESIAN_POINT ( 'NONE',  ( 0.3425196850393700809, 4.616380251121755931E-17, 0.000000000000000000 ) ) ;
#15890=CARTESIAN_POINT ( 'NONE',  ( 0.000000000000000000, 0.000000000000000000, 0.000000000000000000 ) ) ;
#15907=CARTESIAN_POINT ( 'NONE',  ( 0.0003553830333942996095, 0.1260611533336402912, 0.05724849586090775128 ) ) ;
#15913=CARTESIAN_POINT ( 'NONE',  ( 0.008382045503145925391, -0.06595839018091839701, -0.1377952755905513804 ) ) ;
#15936=LINE ( 'NONE', #30563, #23791 ) ;
#15949=CARTESIAN_POINT ( 'NONE',  ( 0.1644020957507539848, 0.1623118080249112138, 1.367956046207553540E-19 ) ) ;
#15955=ORIENTED_EDGE ( 'NONE', *, *, #4758, .T. ) ;
#15957=CIRCLE ( 'NONE', #40385, 0.09842519685039370636 ) ;
#15963=ORIENTED_EDGE ( 'NONE', *, *, #2746, .T. ) ;
#15972=CARTESIAN_POINT ( 'NONE',  ( 0.004259712139235173438, -0.04573943165073560135, 0.1377945059011559392 ) ) ;
#15983=CARTESIAN_POINT ( 'NONE',  ( 0.4632545931758527691, 0.08090551181102362266, 0.000000000000000000 ) ) ;
#15990=EDGE_CURVE ( 'NONE', #18113, #5859, #16764, .T. ) ;
#16006=PLANE ( 'NONE',  #38231 ) ;
#16015=DIRECTION ( 'NONE',  ( -1.000000000000000000, 0.000000000000000000, 0.000000000000000000 ) ) ;
#16021=CARTESIAN_POINT ( 'NONE',  ( 0.4632545931758527691, 4.616380251121755931E-17, 0.000000000000000000 ) ) ;
#16026=CARTESIAN_POINT ( 'NONE',  ( 0.2944196465027555387, -0.09842519685039370636, 1.205361022782828805E-17 ) ) ;
#16031=CARTESIAN_POINT ( 'NONE',  ( 0.1634876958211989029, -0.08035719075736870443, 0.1391819764462846332 ) ) ;
#16032=DIRECTION ( 'NONE',  ( -1.000000000000000000, 0.000000000000000000, 0.000000000000000000 ) ) ;
#16084=CIRCLE ( 'NONE', #28315, 0.09842519685039370636 ) ;
#16105=LINE ( 'NONE', #45054, #13755 ) ;
#16108=VECTOR ( 'NONE', #23662, 39.37007874015748143 ) ;
#16114=AXIS2_PLACEMENT_3D ( 'NONE', #32374, #46952, #43353 ) ;
#16120=DIRECTION ( 'NONE',  ( 0.000000000000000000, -1.000000000000000000, 0.000000000000000000 ) ) ;
#16124=CARTESIAN_POINT ( 'NONE',  ( 0.4755220087074803481, 4.766607801171850497E-17, 0.000000000000000000 ) ) ;
#16133=CARTESIAN_POINT ( 'NONE',  ( 0.1608809465420318885, -0.1607368455565696963, 0.002813831971227527366 ) ) ;
#16146=EDGE_CURVE ( 'NONE', #28970, #12246, #23750, .T. ) ;
#16159=CARTESIAN_POINT ( 'NONE',  ( 0.2397010884053811242, -3.032960542342102697E-32, 0.09842519685039370636 ) ) ;
#16160=ORIENTED_EDGE ( 'NONE', *, *, #29035, .T. ) ;
#16165=CARTESIAN_POINT ( 'NONE',  ( 0.5538057742782149795, 4.616380251121755931E-17, 0.000000000000000000 ) ) ;
#16171=CARTESIAN_POINT ( 'NONE',  ( 0.2642359194686346169, 4.766607801171850497E-17, 0.000000000000000000 ) ) ;
#16212=CARTESIAN_POINT ( 'NONE',  ( 0.2007874015748031815, 0.000000000000000000, 0.000000000000000000 ) ) ;
#16234=CARTESIAN_POINT ( 'NONE',  ( 0.3547871005709968273, 4.766607801171850497E-17, 0.000000000000000000 ) ) ;
#16240=CARTESIAN_POINT ( 'NONE',  ( 0.6141732283464567121, 0.000000000000000000, 0.000000000000000000 ) ) ;
#16249=CARTESIAN_POINT ( 'NONE',  ( 0.3123359580052492146, 0.08090551181102362266, 9.908067607274841931E-18 ) ) ;
#16265=DIRECTION ( 'NONE',  ( 0.000000000000000000, -1.224646799147353207E-16, 1.000000000000000000 ) ) ;
#16273=CIRCLE ( 'NONE', #14720, 0.01968503937007875723 ) ;
#16285=CONICAL_SURFACE ( 'NONE', #36151, 0.09842519685039370636, 0.9599310885968824758 ) ;
#16294=EDGE_CURVE ( 'NONE', #12116, #4993, #39034, .T. ) ;
#16295=CARTESIAN_POINT ( 'NONE',  ( 0.1564636162838598521, 0.1358284121151826784, -0.04551197418441087217 ) ) ;
#16296=ORIENTED_EDGE ( 'NONE', *, *, #12646, .F. ) ;
#16297=VERTEX_POINT ( 'NONE', #25843 ) ;
#16319=AXIS2_PLACEMENT_3D ( 'NONE', #8238, #18329, #18788 ) ;
#16324=EDGE_CURVE ( 'NONE', #16297, #13158, #12663, .T. ) ;
#16362=ADVANCED_FACE ( 'NONE', ( #1595 ), #27288, .T. ) ;
#16372=DIRECTION ( 'NONE',  ( 0.000000000000000000, -1.000000000000000000, 0.000000000000000000 ) ) ;
#16399=CARTESIAN_POINT ( 'NONE',  ( 0.000000000000000000, 0.000000000000000000, 0.000000000000000000 ) ) ;
#16420=EDGE_CURVE ( 'NONE', #7386, #9117, #9976, .T. ) ;
#16422=CIRCLE ( 'NONE', #28678, 0.09842519685039370636 ) ;
#16423=EDGE_CURVE ( 'NONE', #21725, #30249, #44960, .T. ) ;
#16426=ORIENTED_EDGE ( 'NONE', *, *, #14951, .T. ) ;
#16438=AXIS2_PLACEMENT_3D ( 'NONE', #6140, #9767, #20767 ) ;
#16445=FACE_OUTER_BOUND ( 'NONE', #35101, .T. ) ;
#16447=DIRECTION ( 'NONE',  ( -1.000000000000000000, 0.000000000000000000, 0.000000000000000000 ) ) ;
#16450=DIRECTION ( 'NONE',  ( 0.000000000000000000, 1.000000000000000000, 0.000000000000000000 ) ) ;
#16496=CARTESIAN_POINT ( 'NONE',  ( 0.1629747150817544565, -0.08009238079686641087, 0.1387239969760788449 ) ) ;
#16505=ORIENTED_EDGE ( 'NONE', *, *, #44341, .T. ) ;
#16512=FACE_OUTER_BOUND ( 'NONE', #18994, .T. ) ;
#16516=ORIENTED_EDGE ( 'NONE', *, *, #26901, .T. ) ;
#16528=ORIENTED_EDGE ( 'NONE', *, *, #35815, .F. ) ;
#16545=CARTESIAN_POINT ( 'NONE',  ( 0.3302522695077432791, 4.466152701071653354E-17, 0.000000000000000000 ) ) ;
#16593=VERTEX_POINT ( 'NONE', #4906 ) ;
#16601=CARTESIAN_POINT ( 'NONE',  ( 0.002317115957707514655, 0.1361028492807104251, 0.03985382897102638516 ) ) ;
#16606=DIRECTION ( 'NONE',  ( 0.000000000000000000, 0.000000000000000000, 1.000000000000000000 ) ) ;
#16611=EDGE_CURVE ( 'NONE', #42642, #9764, #41785, .T. ) ;
#16612=DIRECTION ( 'NONE',  ( 0.000000000000000000, -1.000000000000000000, 0.000000000000000000 ) ) ;
#16613=AXIS2_PLACEMENT_3D ( 'NONE', #18982, #41469, #41231 ) ;
#16632=ORIENTED_EDGE ( 'NONE', *, *, #7523, .T. ) ;
#16663=ORIENTED_EDGE ( 'NONE', *, *, #16611, .T. ) ;
#16678=EDGE_CURVE ( 'NONE', #28106, #39448, #39846, .T. ) ;
#16699=DIRECTION ( 'NONE',  ( 0.000000000000000000, -1.000000000000000000, 0.000000000000000000 ) ) ;
#16708=CARTESIAN_POINT ( 'NONE',  ( 0.004457209083872700622, 0.04679503328990077676, -0.1377943176258828173 ) ) ;
#16755=CARTESIAN_POINT ( 'NONE',  ( 0.1645805237892203066, 0.08067386790044665801, -0.1414080254031222506 ) ) ;
#16759=EDGE_LOOP ( 'NONE', ( #22536, #4186 ) ) ;
#16764=LINE ( 'NONE', #38571, #42841 ) ;
#16813=CARTESIAN_POINT ( 'NONE',  ( 0.3849708276051176936, 4.766607801171850497E-17, 0.000000000000000000 ) ) ;
#16822=DIRECTION ( 'NONE',  ( 0.000000000000000000, -1.000000000000000000, 0.000000000000000000 ) ) ;
#16825=AXIS2_PLACEMENT_3D ( 'NONE', #45905, #42065, #16699 ) ;
#16843=VERTEX_POINT ( 'NONE', #45128 ) ;
#16853=FACE_OUTER_BOUND ( 'NONE', #7979, .T. ) ;
#16905=CIRCLE ( 'NONE', #43683, 0.09842519685039370636 ) ;
#16917=ORIENTED_EDGE ( 'NONE', *, *, #11475, .T. ) ;
#16941=VERTEX_POINT ( 'NONE', #1049 ) ;
#16946=AXIS2_PLACEMENT_3D ( 'NONE', #20301, #31588, #23914 ) ;
#16967=CARTESIAN_POINT ( 'NONE',  ( 0.4509871776442260227, -3.032960542342102697E-32, 0.09842519685039370636 ) ) ;
#16975=ORIENTED_EDGE ( 'NONE', *, *, #8633, .T. ) ;
#16976=VECTOR ( 'NONE', #24266, 39.37007874015748854 ) ;
#17039=DIRECTION ( 'NONE',  ( -1.000000000000000000, 0.000000000000000000, 0.000000000000000000 ) ) ;
#17061=CIRCLE ( 'NONE', #32419, 0.08090551181102362266 ) ;
#17063=CARTESIAN_POINT ( 'NONE',  ( 0.1620125769266285432, -0.1593973085597378270, -5.302411703423666122E-08 ) ) ;
#17064=ORIENTED_EDGE ( 'NONE', *, *, #25015, .T. ) ;
#17120=ORIENTED_EDGE ( 'NONE', *, *, #15990, .T. ) ;
#17122=CARTESIAN_POINT ( 'NONE',  ( 0.002794899975992053229, -0.1377744224360938075, -0.03695826049548953801 ) ) ;
#17127=EDGE_CURVE ( 'NONE', #37845, #22837, #35265, .T. ) ;
#17137=CARTESIAN_POINT ( 'NONE',  ( 0.5660731898098425585, 4.766607801171850497E-17, 0.000000000000000000 ) ) ;
#17150=CARTESIAN_POINT ( 'NONE',  ( 0.5415383587465882886, 4.466152701071653354E-17, 0.000000000000000000 ) ) ;
#17153=ORIENTED_EDGE ( 'NONE', *, *, #22284, .T. ) ;
#17173=EDGE_CURVE ( 'NONE', #9764, #23901, #14591, .T. ) ;
#17175=CARTESIAN_POINT ( 'NONE',  ( 0.008639645916121835995, 0.06621452963738141961, -0.1377924362075181319 ) ) ;
#17185=ORIENTED_EDGE ( 'NONE', *, *, #5153, .F. ) ;
#17189=FILL_AREA_STYLE ('',( #20543 ) ) ;
#17206=FACE_OUTER_BOUND ( 'NONE', #12713, .T. ) ;
#17213=CIRCLE ( 'NONE', #7263, 0.09842519685039370636 ) ;
#17215=CARTESIAN_POINT ( 'NONE',  ( 0.003062405574111899762, 0.1000190445539651529, -0.1023525292013673232 ) ) ;
#17230=DIRECTION ( 'NONE',  ( 0.000000000000000000, 0.000000000000000000, 1.000000000000000000 ) ) ;
#17236=CARTESIAN_POINT ( 'NONE',  ( 0.000000000000000000, 1.205361022782826802E-17, -0.09842519685039370636 ) ) ;
#17262=ORIENTED_EDGE ( 'NONE', *, *, #36755, .F. ) ;
#17289=ORIENTED_EDGE ( 'NONE', *, *, #3089, .T. ) ;
#17300=CARTESIAN_POINT ( 'NONE',  ( 0.1641609508005656415, -0.1617434695452283633, -1.990205904980697972E-06 ) ) ;
#17305=LINE ( 'NONE', #24975, #39460 ) ;
#17308=EDGE_CURVE ( 'NONE', #41232, #43350, #34507, .T. ) ;
#17316=CARTESIAN_POINT ( 'NONE',  ( 0.1636082376785381876, 0.1608670784834268785, 1.645031862152206036E-07 ) ) ;
#17352=ORIENTED_EDGE ( 'NONE', *, *, #20386, .F. ) ;
#17357=AXIS2_PLACEMENT_3D ( 'NONE', #27332, #22989, #1644 ) ;
#17386=AXIS2_PLACEMENT_3D ( 'NONE', #14028, #9254, #44182 ) ;
#17387=CARTESIAN_POINT ( 'NONE',  ( 0.1571284080983731402, -0.02678626661708362333, -0.1404155760989511115 ) ) ;
#17392=VERTEX_POINT ( 'NONE', #19444 ) ;
#17402=ORIENTED_EDGE ( 'NONE', *, *, #36692, .T. ) ;
#17405=B_SPLINE_CURVE_WITH_KNOTS ( 'NONE', 3,
 ( #7059, #29156, #36772, #39873, #21686 ),
 .UNSPECIFIED., .F., .F.,
 ( 4, 1, 4 ),
 ( 0.000000000000000000, 0.002020725942163689639, 0.004041451884327379278 ),
 .UNSPECIFIED. ) ;
#17417=LINE ( 'NONE', #40156, #3458 ) ;
#17426=CARTESIAN_POINT ( 'NONE',  ( 0.000000000000000000, 1.205361022782826802E-17, -0.09842519685039370636 ) ) ;
#17430=CYLINDRICAL_SURFACE ( 'NONE', #39668, 0.09842519685039370636 ) ;
#17441=CARTESIAN_POINT ( 'NONE',  ( 0.1618465483937462923, 0.06719994080174256090, -0.1405161193130588237 ) ) ;
#17486=CIRCLE ( 'NONE', #38911, 0.09842519685039370636 ) ;
#17489=EDGE_CURVE ( 'NONE', #15059, #1067, #838, .T. ) ;
#17499=CARTESIAN_POINT ( 'NONE',  ( 0.4151545546392377273, 0.09842519685039370636, 0.000000000000000000 ) ) ;
#17524=VERTEX_POINT ( 'NONE', #34547 ) ;
#17526=AXIS2_PLACEMENT_3D ( 'NONE', #21095, #35733, #2176 ) ;
#17554=CARTESIAN_POINT ( 'NONE',  ( 0.3302522695077432791, 4.466152701071653354E-17, 0.000000000000000000 ) ) ;
#17585=AXIS2_PLACEMENT_3D ( 'NONE', #34086, #26658, #11800 ) ;
#17643=CARTESIAN_POINT ( 'NONE',  ( 0.2698848154395015464, 0.09842519685039370636, 1.205361022782828805E-17 ) ) ;
#17651=ADVANCED_FACE ( 'NONE', ( #8887 ), #15420, .T. ) ;
#17657=CARTESIAN_POINT ( 'NONE',  ( 0.000000000000000000, 0.000000000000000000, -0.1377952755905511861 ) ) ;
#17683=AXIS2_PLACEMENT_3D ( 'NONE', #25649, #12150, #40224 ) ;
#17706=ORIENTED_EDGE ( 'NONE', *, *, #1541, .T. ) ;
#17746=ORIENTED_EDGE ( 'NONE', *, *, #70, .T. ) ;
#17764=ORIENTED_EDGE ( 'NONE', *, *, #10121, .T. ) ;
#17780=AXIS2_PLACEMENT_3D ( 'NONE', #38305, #23940, #27078 ) ;
#17787=FACE_OUTER_BOUND ( 'NONE', #22358, .T. ) ;
#17790=CARTESIAN_POINT ( 'NONE',  ( 0.1624141299556661477, 0.1597555635152225761, 1.164103944325189621E-06 ) ) ;
#17800=CARTESIAN_POINT ( 'NONE',  ( 0.4208034506101054895, 4.466152701071653354E-17, 0.000000000000000000 ) ) ;
#17816=UNCERTAINTY_MEASURE_WITH_UNIT (LENGTH_MEASURE( 1.000000000000000082E-05 ), #28286, 'distance_accuracy_value', 'NONE') ;
#17829=ORIENTED_EDGE ( 'NONE', *, *, #35815, .T. ) ;
#17854=DIRECTION ( 'NONE',  ( 1.000000000000000000, 0.000000000000000000, 0.000000000000000000 ) ) ;
#17867=ORIENTED_EDGE ( 'NONE', *, *, #8880, .F. ) ;
#17868=CARTESIAN_POINT ( 'NONE',  ( 0.1619971594100464152, -0.06735705997062264860, -0.1405166210180647801 ) ) ;
#17887=DIRECTION ( 'NONE',  ( -1.000000000000000000, 0.000000000000000000, 0.000000000000000000 ) ) ;
#17903=ORIENTED_EDGE ( 'NONE', *, *, #12189, .F. ) ;
#17914=CARTESIAN_POINT ( 'NONE',  ( 0.1606807218934673820, 0.07955615087644739292, 0.1377952558084805934 ) ) ;
#17915=CARTESIAN_POINT ( 'NONE',  ( 0.1564216623530368111, -8.910440797025414093E-13, -0.1403857474672218497 ) ) ;
#17933=DIRECTION ( 'NONE',  ( -1.000000000000000000, 0.000000000000000000, 0.000000000000000000 ) ) ;
#17938=ORIENTED_EDGE ( 'NONE', *, *, #40917, .F. ) ;
#17957=CARTESIAN_POINT ( 'NONE',  ( 0.1643970000112103258, -0.08114886790928133031, -0.1405539621936140182 ) ) ;
#17977=VERTEX_POINT ( 'NONE', #40219 ) ;
#18001=CARTESIAN_POINT ( 'NONE',  ( 0.4811709046783464450, 0.09842519685039370636, 1.205361022782828805E-17 ) ) ;
#18017=DIRECTION ( 'NONE',  ( 0.5735764363510447161, 0.8191520442889925757, 0.000000000000000000 ) ) ;
#18023=CARTESIAN_POINT ( 'NONE',  ( 0.000000000000000000, 0.000000000000000000, 0.000000000000000000 ) ) ;
#18028=ORIENTED_EDGE ( 'NONE', *, *, #5365, .F. ) ;
#18076=DIRECTION ( 'NONE',  ( 0.000000000000000000, 1.000000000000000000, 0.000000000000000000 ) ) ;
#18111=ORIENTED_EDGE ( 'NONE', *, *, #18516, .T. ) ;
#18113=VERTEX_POINT ( 'NONE', #19130 ) ;
#18127=DIRECTION ( 'NONE',  ( 1.000000000000000000, 0.000000000000000000, 0.000000000000000000 ) ) ;
#18134=( NAMED_UNIT ( * ) SI_UNIT ( $, .STERADIAN. ) SOLID_ANGLE_UNIT ( ) ) ;
#18143=CARTESIAN_POINT ( 'NONE',  ( 0.3547871005709968273, 0.09842519685039370636, 0.000000000000000000 ) ) ;
#18175=CARTESIAN_POINT ( 'NONE',  ( 0.1564216623530370054, 0.01359171937779157097, 0.1403857474671354466 ) ) ;
#18182=CIRCLE ( 'NONE', #45688, 0.09842519685039370636 ) ;
#18189=ORIENTED_EDGE ( 'NONE', *, *, #29340, .F. ) ;
#18190=EDGE_CURVE ( 'NONE', #19819, #9918, #28418, .T. ) ;
#18206=DIRECTION ( 'NONE',  ( -1.000000000000000000, 0.000000000000000000, 0.000000000000000000 ) ) ;
#18207=DIRECTION ( 'NONE',  ( -1.000000000000000000, 0.000000000000000000, 0.000000000000000000 ) ) ;
#18220=ORIENTED_EDGE ( 'NONE', *, *, #4160, .T. ) ;
#18221=VERTEX_POINT ( 'NONE', #30212 ) ;
#18224=ORIENTED_EDGE ( 'NONE', *, *, #6091, .F. ) ;
#18229=LINE ( 'NONE', #14408, #12380 ) ;
#18245=CIRCLE ( 'NONE', #25124, 0.09842519685039370636 ) ;
#18266=CARTESIAN_POINT ( 'NONE',  ( 0.4934383202099732468, -0.08090551181102362266, 1.098083891755157578E-17 ) ) ;
#18270=CARTESIAN_POINT ( 'NONE',  ( 0.1618536817989107979, 0.08807120157702044705, 0.1284887221114194289 ) ) ;
#18280=AXIS2_PLACEMENT_3D ( 'NONE', #31606, #28237, #13598 ) ;
#18285=CARTESIAN_POINT ( 'NONE',  ( 0.1594510458733990610, 0.09722652869638431783, -0.1125335630252820018 ) ) ;
#18329=DIRECTION ( 'NONE',  ( -1.000000000000000000, 0.000000000000000000, 0.000000000000000000 ) ) ;
#18339=CARTESIAN_POINT ( 'NONE',  ( 7.155189876034614158E-05, 0.006740216713035995962, 0.1377954718200116446 ) ) ;
#18352=ORIENTED_EDGE ( 'NONE', *, *, #2428, .T. ) ;
#18358=CARTESIAN_POINT ( 'NONE',  ( 0.000000000000000000, 0.1193342091828950846, -0.06889763779527559306 ) ) ;
#18365=FACE_OUTER_BOUND ( 'NONE', #43902, .T. ) ;
#18381=DIRECTION ( 'NONE',  ( -0.5735764363510518216, -0.8191520442889876907, 0.000000000000000000 ) ) ;
#18390=B_SPLINE_CURVE_WITH_KNOTS ( 'NONE', 3,
 ( #33111, #10823, #11059, #28814, #7668, #25900, #25437, #33346, #14639, #26140, #7207, #32871, #21830, #36456 ),
 .UNSPECIFIED., .F., .F.,
 ( 4, 2, 2, 2, 2, 2, 4 ),
 ( 0.000000000000000000, 0.1249999999999997780, 0.2499999999999995559, 0.3749999999999993339, 0.4374999999999992228, 0.4999999999999991118, 1.000000000000000000 ),
 .UNSPECIFIED. ) ;
#18396=DIRECTION ( 'NONE',  ( 1.000000000000000000, 0.000000000000000000, 0.000000000000000000 ) ) ;
#18428=CARTESIAN_POINT ( 'NONE',  ( 0.5057057357416000487, 4.766607801171850497E-17, 0.000000000000000000 ) ) ;
#18429=CARTESIAN_POINT ( 'NONE',  ( 0.1640396990260823695, -0.08075828909096639807, -0.1398798884322421388 ) ) ;
#18440=CARTESIAN_POINT ( 'NONE',  ( 0.3547871005709968273, -3.032960542342102697E-32, 0.09842519685039370636 ) ) ;
#18463=DIRECTION ( 'NONE',  ( 0.000000000000000000, 1.000000000000000000, 0.000000000000000000 ) ) ;
#18475=AXIS2_PLACEMENT_3D ( 'NONE', #42338, #28220, #5689 ) ;
#18489=DIRECTION ( 'NONE',  ( -1.000000000000000000, 0.000000000000000000, 0.000000000000000000 ) ) ;
#18497=CARTESIAN_POINT ( 'NONE',  ( 0.1559665883013663656, -0.1473510212940053188, 0.02037109575272184891 ) ) ;
#18500=CARTESIAN_POINT ( 'NONE',  ( 0.1579024634500834634, 0.1046578554684915313, 0.09958160468956725464 ) ) ;
#18512=CIRCLE ( 'NONE', #45280, 0.1377952755905511861 ) ;
#18516=EDGE_CURVE ( 'NONE', #39448, #36523, #3533, .T. ) ;
#18517=CARTESIAN_POINT ( 'NONE',  ( 0.1600714537641983737, 0.09473400225496043936, -0.1168739604210893984 ) ) ;
#18528=DIRECTION ( 'NONE',  ( 0.5735764363510447161, 0.8191520442889925757, 0.000000000000000000 ) ) ;
#18563=VERTEX_POINT ( 'NONE', #6872 ) ;
#18578=ORIENTED_EDGE ( 'NONE', *, *, #44717, .F. ) ;
#18589=EDGE_LOOP ( 'NONE', ( #43145, #20933, #1937, #45909 ) ) ;
#18613=ORIENTED_EDGE ( 'NONE', *, *, #46906, .T. ) ;
#18623=FACE_OUTER_BOUND ( 'NONE', #16759, .T. ) ;
#18650=EDGE_CURVE ( 'NONE', #6014, #35175, #34461, .T. ) ;
#18655=LINE ( 'NONE', #13949, #28388 ) ;
#18675=UNCERTAINTY_MEASURE_WITH_UNIT (LENGTH_MEASURE( 1.000000000000000082E-05 ), #33257, 'distance_accuracy_value', 'NONE') ;
#18677=ORIENTED_EDGE ( 'NONE', *, *, #40079, .T. ) ;
#18743=DIRECTION ( 'NONE',  ( 0.000000000000000000, -1.000000000000000000, 0.000000000000000000 ) ) ;
#18756=CARTESIAN_POINT ( 'NONE',  ( 0.3547871005709968273, 4.766607801171850497E-17, 0.000000000000000000 ) ) ;
#18771=VECTOR ( 'NONE', #28223, 39.37007874015748143 ) ;
#18788=DIRECTION ( 'NONE',  ( 0.000000000000000000, -1.000000000000000000, 0.000000000000000000 ) ) ;
#18791=CARTESIAN_POINT ( 'NONE',  ( 0.4453382816733590377, 4.766607801171850497E-17, 0.000000000000000000 ) ) ;
#18801=CONICAL_SURFACE ( 'NONE', #15002, 0.09842519685039370636, 0.9599310885968824758 ) ;
#18802=CARTESIAN_POINT ( 'NONE',  ( 0.1588779435336241663, -0.09971251034085006071, 0.1082054717951722450 ) ) ;
#18814=AXIS2_PLACEMENT_3D ( 'NONE', #35865, #18127, #43515 ) ;
#18818=DIRECTION ( 'NONE',  ( -1.000000000000000000, 0.000000000000000000, 0.000000000000000000 ) ) ;
#18825=CYLINDRICAL_SURFACE ( 'NONE', #9291, 0.09842519685039370636 ) ;
#18833=CARTESIAN_POINT ( 'NONE',  ( 0.3849708276051176936, -3.032960542342102697E-32, 0.09842519685039370636 ) ) ;
#18845=CARTESIAN_POINT ( 'NONE',  ( 0.1563805530828631662, 0.1352584698612726566, 0.04649480693109582508 ) ) ;
#18852=ADVANCED_FACE ( 'NONE', ( #9724 ), #27253, .T. ) ;
#18854=VERTEX_POINT ( 'NONE', #15983 ) ;
#18855=DIRECTION ( 'NONE',  ( 1.000000000000000000, 0.000000000000000000, 0.000000000000000000 ) ) ;
#18870=CARTESIAN_POINT ( 'NONE',  ( 0.3547871005709968273, 4.766607801171850497E-17, 0.000000000000000000 ) ) ;
#18935=ADVANCED_FACE ( 'NONE', ( #34418 ), #41805, .T. ) ;
#18938=EDGE_CURVE ( 'NONE', #20645, #2888, #86, .T. ) ;
#18941=VECTOR ( 'NONE', #2510, 39.37007874015748143 ) ;
#18959=CARTESIAN_POINT ( 'NONE',  ( 0.1577586585109200246, 0.1055041328676883661, 0.09810528961771382284 ) ) ;
#18982=CARTESIAN_POINT ( 'NONE',  ( 0.5966535433070866423, 0.000000000000000000, 0.000000000000000000 ) ) ;
#18983=EDGE_LOOP ( 'NONE', ( #28981, #22805, #29782, #3297, #34264 ) ) ;
#18994=EDGE_LOOP ( 'NONE', ( #6967, #2311, #46388, #16160, #33239, #43676 ) ) ;
#19034=CARTESIAN_POINT ( 'NONE',  ( 0.1644020957507539848, -0.1623118080249112138, 7.560884646099310910E-18 ) ) ;
#19079=VERTEX_POINT ( 'NONE', #3215 ) ;
#19085=CONICAL_SURFACE ( 'NONE', #19888, 0.09842519685039370636, 0.9599310885968824758 ) ;
#19116=CARTESIAN_POINT ( 'NONE',  ( 0.4151545546392377273, 4.766607801171850497E-17, 0.000000000000000000 ) ) ;
#19130=CARTESIAN_POINT ( 'NONE',  ( 0.2821522309711287368, 0.08090551181102362266, 0.000000000000000000 ) ) ;
#19133=DIRECTION ( 'NONE',  ( -1.000000000000000000, 0.000000000000000000, 0.000000000000000000 ) ) ;
#19187=DIRECTION ( 'NONE',  ( 0.000000000000000000, 1.000000000000000000, 0.000000000000000000 ) ) ;
#19208=DIRECTION ( 'NONE',  ( 0.000000000000000000, -1.000000000000000000, 0.000000000000000000 ) ) ;
#19237=CARTESIAN_POINT ( 'NONE',  ( 0.3246033735368759610, 4.766607801171850497E-17, 0.000000000000000000 ) ) ;
#19244=EDGE_CURVE ( 'NONE', #21725, #43350, #40569, .T. ) ;
#19245=CARTESIAN_POINT ( 'NONE',  ( 0.01230737760510134012, -0.07955613945526751607, -0.1377952755905511861 ) ) ;
#19249=DIRECTION ( 'NONE',  ( 0.000000000000000000, 0.000000000000000000, -1.000000000000000000 ) ) ;
#19269=CARTESIAN_POINT ( 'NONE',  ( 0.5358894627757212481, 0.09842519685039370636, 0.000000000000000000 ) ) ;
#19278=CARTESIAN_POINT ( 'NONE',  ( 0.1566053014577235558, -0.1284161769475049009, 0.05833949276692128316 ) ) ;
#19290=AXIS2_PLACEMENT_3D ( 'NONE', #7182, #29519, #44068 ) ;
#19293=FACE_OUTER_BOUND ( 'NONE', #11663, .T. ) ;
#19302=DIRECTION ( 'NONE',  ( 1.000000000000000000, 0.000000000000000000, 0.000000000000000000 ) ) ;
#19309=DIRECTION ( 'NONE',  ( -1.000000000000000000, 0.000000000000000000, 0.000000000000000000 ) ) ;
#19344=FACE_OUTER_BOUND ( 'NONE', #41945, .T. ) ;
#19361=LINE ( 'NONE', #12438, #35590 ) ;
#19394=ORIENTED_EDGE ( 'NONE', *, *, #1012, .T. ) ;
#19410=DIRECTION ( 'NONE',  ( 0.000000000000000000, -1.000000000000000000, 0.000000000000000000 ) ) ;
#19431=AXIS2_PLACEMENT_3D ( 'NONE', #36418, #7630, #7403 ) ;
#19438=DIRECTION ( 'NONE',  ( 0.000000000000000000, 0.5000000000000003331, -0.8660254037844384856 ) ) ;
#19444=CARTESIAN_POINT ( 'NONE',  ( 0.2698848154395015464, -0.09842519685039370636, 0.000000000000000000 ) ) ;
#19462=EDGE_LOOP ( 'NONE', ( #17764, #44282, #22899, #44203, #27991 ) ) ;
#19464=CARTESIAN_POINT ( 'NONE',  ( 0.1608764814808673338, -0.07794373349925551309, -0.1405880446287836594 ) ) ;
#19467=AXIS2_PLACEMENT_3D ( 'NONE', #24073, #5849, #23363 ) ;
#19476=CARTESIAN_POINT ( 'NONE',  ( 0.000000000000000000, 0.000000000000000000, 0.09842519685039370636 ) ) ;
#19507=EDGE_LOOP ( 'NONE', ( #8976, #38554, #42533, #28626, #9695, #15318 ) ) ;
#19509=ORIENTED_EDGE ( 'NONE', *, *, #16324, .T. ) ;
#19535=VERTEX_POINT ( 'NONE', #16159 ) ;
#19539=CARTESIAN_POINT ( 'NONE',  ( 0.000000000000000000, 1.478656101119254046E-17, 0.1377952755905511861 ) ) ;
#19552=DIRECTION ( 'NONE',  ( 0.000000000000000000, 0.000000000000000000, 1.000000000000000000 ) ) ;
#19561=FACE_OUTER_BOUND ( 'NONE', #6317, .T. ) ;
#19566=AXIS2_PLACEMENT_3D ( 'NONE', #38764, #10247, #43037 ) ;
#19573=EDGE_LOOP ( 'NONE', ( #13006, #1606, #22186, #20522, #26556 ) ) ;
#19585=ADVANCED_FACE ( 'NONE', ( #27674 ), #40588, .T. ) ;
#19594=CIRCLE ( 'NONE', #24228, 0.09842519685039370636 ) ;
#19603=CARTESIAN_POINT ( 'NONE',  ( 0.1631287631785732217, -0.08016276244899019077, 0.1388449842062895456 ) ) ;
#19636=VERTEX_POINT ( 'NONE', #31020 ) ;
#19671=CARTESIAN_POINT ( 'NONE',  ( 0.1577476715125368523, -0.03207557811198601810, 0.1404216743935849665 ) ) ;
#19694=ORIENTED_EDGE ( 'NONE', *, *, #21362, .F. ) ;
#19706=ORIENTED_EDGE ( 'NONE', *, *, #16146, .F. ) ;
#19711=CARTESIAN_POINT ( 'NONE',  ( 0.001132063567037208413, 0.1311094469945639218, 0.04850708733689491209 ) ) ;
#19722=CARTESIAN_POINT ( 'NONE',  ( 0.4028871391076110364, 4.616380251121755931E-17, 0.000000000000000000 ) ) ;
#19729=ORIENTED_EDGE ( 'NONE', *, *, #25831, .F. ) ;
#19741=VERTEX_POINT ( 'NONE', #4756 ) ;
#19745=ORIENTED_EDGE ( 'NONE', *, *, #4160, .F. ) ;
#19787=PLANE ( 'NONE',  #30065 ) ;
#19819=VERTEX_POINT ( 'NONE', #37594 ) ;
#19829=ORIENTED_EDGE ( 'NONE', *, *, #46477, .F. ) ;
#19837=CARTESIAN_POINT ( 'NONE',  ( 0.1637019648883152323, -0.08049522773984678359, 0.1394218127426261888 ) ) ;
#19847=ADVANCED_FACE ( 'NONE', ( #26116 ), #44727, .F. ) ;
#19856=CARTESIAN_POINT ( 'NONE',  ( 0.1602931993194442739, -0.07955613945526318620, 0.1377952755905511861 ) ) ;
#19859=ORIENTED_EDGE ( 'NONE', *, *, #26804, .T. ) ;
#19861=CARTESIAN_POINT ( 'NONE',  ( 0.1608764898047789493, 0.08278099671294095185, -0.1377952755905511861 ) ) ;
#19862=DIRECTION ( 'NONE',  ( 0.000000000000000000, -1.000000000000000000, 0.000000000000000000 ) ) ;
#19888=AXIS2_PLACEMENT_3D ( 'NONE', #16124, #38377, #12767 ) ;
#19907=AXIS2_PLACEMENT_3D ( 'NONE', #1563, #16447, #13324 ) ;
#19911=CARTESIAN_POINT ( 'NONE',  ( 0.2204724409448818867, 0.1591122789105269553, 0.000000000000000000 ) ) ;
#19930=ORIENTED_EDGE ( 'NONE', *, *, #14951, .F. ) ;
#19942=CARTESIAN_POINT ( 'NONE',  ( 0.4453382816733590377, 0.09842519685039370636, 0.000000000000000000 ) ) ;
#19964=DIRECTION ( 'NONE',  ( 0.000000000000000000, -1.000000000000000000, 0.000000000000000000 ) ) ;
#19972=CARTESIAN_POINT ( 'NONE',  ( 0.6141732283464567121, 0.000000000000000000, 0.000000000000000000 ) ) ;
#20000=CARTESIAN_POINT ( 'NONE',  ( 0.2642359194686346169, 4.766607801171850497E-17, 0.000000000000000000 ) ) ;
#20013=EDGE_CURVE ( 'NONE', #32919, #11416, #46953, .T. ) ;
#20031=ORIENTED_EDGE ( 'NONE', *, *, #36822, .T. ) ;
#20061=DIRECTION ( 'NONE',  ( -1.000000000000000000, 0.000000000000000000, 0.000000000000000000 ) ) ;
#20068=EDGE_CURVE ( 'NONE', #19535, #14831, #7133, .T. ) ;
#20069=TOROIDAL_SURFACE ( 'NONE', #44506, 0.2047244094488188948, 0.01968503937007873988 ) ;
#20074=CARTESIAN_POINT ( 'NONE',  ( 0.1606807218793907532, -0.07955611661335547369, 0.1377952755905512694 ) ) ;
#20103=CARTESIAN_POINT ( 'NONE',  ( 0.1555213372790611448, 0.1336203177416501464, -0.04415337192905793851 ) ) ;
#20134=LINE ( 'NONE', #27604, #40856 ) ;
#20140=CARTESIAN_POINT ( 'NONE',  ( 0.4509871776442260227, 4.466152701071653354E-17, 0.000000000000000000 ) ) ;
#20141=CARTESIAN_POINT ( 'NONE',  ( 0.1573498687646869010, -0.02697554138024618048, 0.1404067023994647889 ) ) ;
#20259=CARTESIAN_POINT ( 'NONE',  ( 0.5057057357416000487, 0.09842519685039370636, 0.000000000000000000 ) ) ;
#20295=DIRECTION ( 'NONE',  ( -1.000000000000000000, 0.000000000000000000, 0.000000000000000000 ) ) ;
#20299=DIRECTION ( 'NONE',  ( -1.000000000000000000, 0.000000000000000000, 0.000000000000000000 ) ) ;
#20301=CARTESIAN_POINT ( 'NONE',  ( 0.000000000000000000, 0.000000000000000000, 0.000000000000000000 ) ) ;
#20311=VECTOR ( 'NONE', #5509, 39.37007874015748854 ) ;
#20323=CARTESIAN_POINT ( 'NONE',  ( 0.2944196465027555387, 4.766607801171850497E-17, 0.000000000000000000 ) ) ;
#20337=CYLINDRICAL_SURFACE ( 'NONE', #25057, 0.09842519685039370636 ) ;
#20352=EDGE_CURVE ( 'NONE', #9934, #21151, #24350, .T. ) ;
#20373=FACE_OUTER_BOUND ( 'NONE', #25478, .T. ) ;
#20374=CARTESIAN_POINT ( 'NONE',  ( 0.004734662961524557616, 0.09521559318215297441, 0.1106847963720228034 ) ) ;
#20381=CARTESIAN_POINT ( 'NONE',  ( 0.6141732283464567121, 0.000000000000000000, 0.000000000000000000 ) ) ;
#20386=EDGE_CURVE ( 'NONE', #15821, #37845, #35293, .T. ) ;
#20397=EDGE_CURVE ( 'NONE', #8724, #21404, #16905, .T. ) ;
#20405=ORIENTED_EDGE ( 'NONE', *, *, #4702, .T. ) ;
#20419=DIRECTION ( 'NONE',  ( 0.5735764363510447161, 0.8191520442889925757, 0.000000000000000000 ) ) ;
#20467=EDGE_LOOP ( 'NONE', ( #5309, #44877, #31177, #17903, #2148 ) ) ;
#20494=DIRECTION ( 'NONE',  ( -1.000000000000000000, 0.000000000000000000, 0.000000000000000000 ) ) ;
#20498=DIRECTION ( 'NONE',  ( -1.000000000000000000, 0.000000000000000000, 0.000000000000000000 ) ) ;
#20508=CARTESIAN_POINT ( 'NONE',  ( 0.4330708661417322913, 0.08090551181102362266, 9.908067607274841931E-18 ) ) ;
#20514=DIRECTION ( 'NONE',  ( 0.000000000000000000, -1.000000000000000000, 0.000000000000000000 ) ) ;
#20522=ORIENTED_EDGE ( 'NONE', *, *, #7247, .F. ) ;
#20534=ORIENTED_EDGE ( 'NONE', *, *, #7370, .F. ) ;
#20543=FILL_AREA_STYLE_COLOUR ( '', #46276 ) ;
#20557=CARTESIAN_POINT ( 'NONE',  ( 0.4632545931758527691, 4.616380251121755931E-17, 0.000000000000000000 ) ) ;
#20564=CARTESIAN_POINT ( 'NONE',  ( 0.1583744855326529033, 0.03901141430315911013, -0.1404421906569247869 ) ) ;
#20569=CARTESIAN_POINT ( 'NONE',  ( 0.5358894627757212481, 4.766607801171850497E-17, 0.000000000000000000 ) ) ;
#20573=CARTESIAN_POINT ( 'NONE',  ( 0.1608764814808673338, 0.1607246848665348227, 0.002792769038232334466 ) ) ;
#20580=DIRECTION ( 'NONE',  ( -1.000000000000000000, 0.000000000000000000, 0.000000000000000000 ) ) ;
#20596=ORIENTED_EDGE ( 'NONE', *, *, #45925, .F. ) ;
#20643=SHAPE_REPRESENTATION ( 'ISO 4162 M5x10 Hex Flange Bolt', ( #20860 ), #30086 ) ;
#20645=VERTEX_POINT ( 'NONE', #7540 ) ;
#20658=DIMENSIONAL_EXPONENTS ( 1.000000000000000000, 0.000000000000000000, 0.000000000000000000, 0.000000000000000000, 0.000000000000000000, 0.000000000000000000, 0.000000000000000000 ) ;
#20664=CARTESIAN_POINT ( 'NONE',  ( 0.000000000000000000, 0.000000000000000000, 0.000000000000000000 ) ) ;
#20671=CARTESIAN_POINT ( 'NONE',  ( 0.5057057357416000487, 0.09842519685039370636, 0.000000000000000000 ) ) ;
#20673=VERTEX_POINT ( 'NONE', #19269 ) ;
#20697=DIRECTION ( 'NONE',  ( -1.000000000000000000, 0.000000000000000000, 0.000000000000000000 ) ) ;
#20705=ORIENTED_EDGE ( 'NONE', *, *, #39094, .T. ) ;
#20707=B_SPLINE_CURVE_WITH_KNOTS ( 'NONE', 3,
 ( #13563, #21452, #17868, #10937, #6601, #35845, #32511, #28198, #28688, #17387, #14287, #39896 ),
 .UNSPECIFIED., .F., .F.,
 ( 4, 2, 2, 2, 2, 4 ),
 ( 0.000000000000000000, 0.2500000000000009437, 0.3750000000000012212, 0.4375000000000013323, 0.5000000000000013323, 1.000000000000000000 ),
 .UNSPECIFIED. ) ;
#20727=CARTESIAN_POINT ( 'NONE',  ( 0.1634463026673921293, -0.08033096794652530570, -0.1391362646951039561 ) ) ;
#20737=CARTESIAN_POINT ( 'NONE',  ( 0.2642359194686346169, 4.766607801171850497E-17, 0.000000000000000000 ) ) ;
#20742=FACE_OUTER_BOUND ( 'NONE', #10692, .T. ) ;
#20754=ORIENTED_EDGE ( 'NONE', *, *, #37158, .F. ) ;
#20759=ORIENTED_EDGE ( 'NONE', *, *, #36313, .T. ) ;
#20767=DIRECTION ( 'NONE',  ( 0.000000000000000000, -1.000000000000000000, 0.000000000000000000 ) ) ;
#20774=CARTESIAN_POINT ( 'NONE',  ( 0.000000000000000000, 0.000000000000000000, 0.09842519685039370636 ) ) ;
#20793=LINE ( 'NONE', #27324, #3909 ) ;
#20798=CARTESIAN_POINT ( 'NONE',  ( 7.107660667884922897E-05, 0.1159713038039417443, -0.07472206960542350507 ) ) ;
#20806=CARTESIAN_POINT ( 'NONE',  ( 0.1563805530828639712, 0.1078949188770173262, -0.09388986751133071573 ) ) ;
#20825=AXIS2_PLACEMENT_3D ( 'NONE', #24740, #28121, #10857 ) ;
#20827=CIRCLE ( 'NONE', #19290, 0.09842519685039370636 ) ;
#20846=CARTESIAN_POINT ( 'NONE',  ( 0.1644020957507539848, -0.08115590401245571794, -0.1405661490837558925 ) ) ;
#20853=AXIS2_PLACEMENT_3D ( 'NONE', #8188, #41222, #16120 ) ;
#20860=AXIS2_PLACEMENT_3D ( 'NONE', #25692, #32652, #10835 ) ;
#20867=VERTEX_POINT ( 'NONE', #46153 ) ;
#20868=PRODUCT_DEFINITION_SHAPE ( 'NONE', 'NONE',  #1359 ) ;
#20879=ORIENTED_EDGE ( 'NONE', *, *, #12750, .T. ) ;
#20889=CONICAL_SURFACE ( 'NONE', #20825, 0.08090551181102362266, 0.9599310885968742602 ) ;
#20890=LINE ( 'NONE', #12555, #45538 ) ;
#20906=CARTESIAN_POINT ( 'NONE',  ( 0.1631287632119293174, 0.1603246647599305685, 4.966163489190320679E-07 ) ) ;
#20918=VERTEX_POINT ( 'NONE', #28200 ) ;
#20930=CARTESIAN_POINT ( 'NONE',  ( 0.5717220857807087109, 4.466152701071653354E-17, 0.000000000000000000 ) ) ;
#20933=ORIENTED_EDGE ( 'NONE', *, *, #24423, .T. ) ;
#20937=CARTESIAN_POINT ( 'NONE',  ( 0.5057057357416000487, 4.766607801171850497E-17, 0.000000000000000000 ) ) ;
#20953=CARTESIAN_POINT ( 'NONE',  ( 0.1554368334888477088, 0.02742154311898540794, 0.1377952755905511584 ) ) ;
#20986=AXIS2_PLACEMENT_3D ( 'NONE', #19237, #41021, #15194 ) ;
#20987=DIRECTION ( 'NONE',  ( 1.000000000000000000, 0.000000000000000000, 0.000000000000000000 ) ) ;
#20993=ORIENTED_EDGE ( 'NONE', *, *, #22350, .F. ) ;
#21000=ADVANCED_FACE ( 'NONE', ( #47349 ), #2388, .T. ) ;
#21006=ORIENTED_EDGE ( 'NONE', *, *, #35133, .F. ) ;
#21017=DIRECTION ( 'NONE',  ( 0.000000000000000000, 0.000000000000000000, -1.000000000000000000 ) ) ;
#21024=CARTESIAN_POINT ( 'NONE',  ( 0.1619802298545178210, 0.07975292738397864178, 0.1381419564372848019 ) ) ;
#21078=CARTESIAN_POINT ( 'NONE',  ( 0.1587072800412991924, -0.1427694538647072964, -0.03362159989229708545 ) ) ;
#21080=AXIS2_PLACEMENT_3D ( 'NONE', #23885, #5665, #20514 ) ;
#21095=CARTESIAN_POINT ( 'NONE',  ( 0.2944196465027555387, 4.766607801171850497E-17, 0.000000000000000000 ) ) ;
#21116=ORIENTED_EDGE ( 'NONE', *, *, #13012, .F. ) ;
#21124=CARTESIAN_POINT ( 'NONE',  ( 0.1639941273274911349, -0.1614384449312174230, -8.749531877264769744E-07 ) ) ;
#21139=EDGE_LOOP ( 'NONE', ( #10220, #21540, #31457 ) ) ;
#21148=DIRECTION ( 'NONE',  ( 0.000000000000000000, -1.000000000000000000, 0.000000000000000000 ) ) ;
#21151=VERTEX_POINT ( 'NONE', #46498 ) ;
#21169=ORIENTED_EDGE ( 'NONE', *, *, #22552, .T. ) ;
#21176=CARTESIAN_POINT ( 'NONE',  ( 0.001132063566998833728, -0.1311094469944007745, -0.04850708733712583154 ) ) ;
#21236=EDGE_LOOP ( 'NONE', ( #17867, #37267, #6285, #4585, #34863 ) ) ;
#21238=LINE ( 'NONE', #3016, #40877 ) ;
#21245=CIRCLE ( 'NONE', #27419, 0.09842519685039370636 ) ;
#21266=CARTESIAN_POINT ( 'NONE',  ( 0.1602931993194442739, 0.07955613945526338049, 0.1377952755905511861 ) ) ;
#21269=VERTEX_POINT ( 'NONE', #39070 ) ;
#21277=VECTOR ( 'NONE', #37117, 39.37007874015748854 ) ;
#21278=ORIENTED_EDGE ( 'NONE', *, *, #20068, .F. ) ;
#21316=ORIENTED_EDGE ( 'NONE', *, *, #24215, .F. ) ;
#21326=ORIENTED_EDGE ( 'NONE', *, *, #41625, .T. ) ;
#21330=CARTESIAN_POINT ( 'NONE',  ( 0.1602931993194442739, -0.07955613945526357478, -0.1377952755905511861 ) ) ;
#21341=ORIENTED_EDGE ( 'NONE', *, *, #26096, .T. ) ;
#21362=EDGE_CURVE ( 'NONE', #32919, #6075, #18229, .T. ) ;
#21372=CIRCLE ( 'NONE', #24461, 0.09842519685039370636 ) ;
#21380=CARTESIAN_POINT ( 'NONE',  ( 0.1606807218938896276, 0.1591122674893432898, -1.978207022268160401E-08 ) ) ;
#21382=CARTESIAN_POINT ( 'NONE',  ( 0.1596650774283295271, -0.1494101348903348336, 0.02216197906078582955 ) ) ;
#21399=DIRECTION ( 'NONE',  ( 0.000000000000000000, -1.000000000000000000, 0.000000000000000000 ) ) ;
#21404=VERTEX_POINT ( 'NONE', #11521 ) ;
#21408=ORIENTED_EDGE ( 'NONE', *, *, #5694, .F. ) ;
#21415=ORIENTED_EDGE ( 'NONE', *, *, #6804, .F. ) ;
#21417=CARTESIAN_POINT ( 'NONE',  ( 0.4509871776442260227, 4.466152701071653354E-17, 0.000000000000000000 ) ) ;
#21420=EDGE_CURVE ( 'NONE', #31223, #16843, #18390, .T. ) ;
#21442=ORIENTED_EDGE ( 'NONE', *, *, #36491, .T. ) ;
#21452=CARTESIAN_POINT ( 'NONE',  ( 0.1631243713103771309, -0.07417819129880506845, -0.1405411351623387928 ) ) ;
#21485=ORIENTED_EDGE ( 'NONE', *, *, #4540, .F. ) ;
#21497=FACE_OUTER_BOUND ( 'NONE', #26849, .T. ) ;
#21503=CARTESIAN_POINT ( 'NONE',  ( 0.1626913500577309712, 0.07997639175683110557, 0.1385232029213226412 ) ) ;
#21504=CARTESIAN_POINT ( 'NONE',  ( 0.1565984635743036257, 0.01350052470346802501, -0.1403812994534590630 ) ) ;
#21532=CARTESIAN_POINT ( 'NONE',  ( 0.4509871776442260227, -0.09842519685039370636, 0.000000000000000000 ) ) ;
#21534=EDGE_CURVE ( 'NONE', #40174, #17524, #32069, .T. ) ;
#21536=EDGE_CURVE ( 'NONE', #9918, #32777, #7807, .T. ) ;
#21540=ORIENTED_EDGE ( 'NONE', *, *, #21660, .T. ) ;
#21557=CARTESIAN_POINT ( 'NONE',  ( 0.1644020957507539848, -0.08115590401245571794, -0.1405661490837558925 ) ) ;
#21560=CARTESIAN_POINT ( 'NONE',  ( 0.1618536817989234267, -0.08807120157698605789, -0.1284887221114794087 ) ) ;
#21599=AXIS2_PLACEMENT_3D ( 'NONE', #20381, #12275, #27143 ) ;
#21601=ORIENTED_EDGE ( 'NONE', *, *, #41303, .F. ) ;
#21604=LINE ( 'NONE', #6737, #23098 ) ;
#21608=CARTESIAN_POINT ( 'NONE',  ( 0.2007874015748031815, 0.000000000000000000, 0.2047244094488188948 ) ) ;
#21609=CARTESIAN_POINT ( 'NONE',  ( 0.1643970176812789008, -0.1622977831747160482, 1.011058549611711511E-12 ) ) ;
#21628=CARTESIAN_POINT ( 'NONE',  ( 0.1637325577037128943, -0.1604625459914955088, -0.002338731188024976374 ) ) ;
#21638=CIRCLE ( 'NONE', #38500, 0.09842519685039370636 ) ;
#21653=ORIENTED_EDGE ( 'NONE', *, *, #92, .T. ) ;
#21660=EDGE_CURVE ( 'NONE', #34218, #32653, #2425, .T. ) ;
#21665=ORIENTED_EDGE ( 'NONE', *, *, #6091, .T. ) ;
#21670=CIRCLE ( 'NONE', #229, 0.09842519685039370636 ) ;
#21684=FACE_OUTER_BOUND ( 'NONE', #9437, .T. ) ;
#21686=CARTESIAN_POINT ( 'NONE',  ( 0.1602931993194442739, -0.07955613945526357478, -0.1377952755905511861 ) ) ;
#21692=DIRECTION ( 'NONE',  ( -1.000000000000000000, 0.000000000000000000, 0.000000000000000000 ) ) ;
#21697=AXIS2_PLACEMENT_3D ( 'NONE', #19911, #42171, #19438 ) ;
#21725=VERTEX_POINT ( 'NONE', #44940 ) ;
#21740=AXIS2_PLACEMENT_3D ( 'NONE', #29330, #11539, #11078 ) ;
#21756=DIRECTION ( 'NONE',  ( -1.000000000000000000, 0.000000000000000000, 0.000000000000000000 ) ) ;
#21758=DIRECTION ( 'NONE',  ( 1.000000000000000000, 0.000000000000000000, 0.000000000000000000 ) ) ;
#21761=ADVANCED_FACE ( 'NONE', ( #26540 ), #42974, .T. ) ;
#21764=ORIENTED_EDGE ( 'NONE', *, *, #5153, .T. ) ;
#21791=ADVANCED_FACE ( 'NONE', ( #19561 ), #15661, .F. ) ;
#21830=CARTESIAN_POINT ( 'NONE',  ( 0.008396861977785833459, -0.08632935120555602915, 0.1260637287086050495 ) ) ;
#21841=VERTEX_POINT ( 'NONE', #28428 ) ;
#21844=ORIENTED_EDGE ( 'NONE', *, *, #2746, .F. ) ;
#21859=FACE_OUTER_BOUND ( 'NONE', #12249, .T. ) ;
#21867=CIRCLE ( 'NONE', #37153, 0.01968503937007875723 ) ;
#21877=CARTESIAN_POINT ( 'NONE',  ( 0.2698848154395015464, 1.205361022782824954E-17, -0.09842519685039370636 ) ) ;
#21906=CARTESIAN_POINT ( 'NONE',  ( 0.002094777259443145277, -0.1352690037933263756, -0.04129845016576910027 ) ) ;
#21921=DIRECTION ( 'NONE',  ( 0.5735764363510447161, 0.8191520442889925757, 0.000000000000000000 ) ) ;
#21922=CARTESIAN_POINT ( 'NONE',  ( 0.1608764731649685309, -0.08278090606525061179, 0.1377952755905511861 ) ) ;
#21962=CARTESIAN_POINT ( 'NONE',  ( 0.4453382816733590377, 4.766607801171850497E-17, 0.000000000000000000 ) ) ;
#21967=ADVANCED_FACE ( 'NONE', ( #2517 ), #32011, .F. ) ;
#21978=DIRECTION ( 'NONE',  ( 0.000000000000000000, 0.000000000000000000, -1.000000000000000000 ) ) ;
#21987=CARTESIAN_POINT ( 'NONE',  ( 0.1631287632117340569, 0.08016190229754059648, 0.1388454808432816601 ) ) ;
#21990=DIRECTION ( 'NONE',  ( 0.000000000000000000, 1.000000000000000000, 0.000000000000000000 ) ) ;
#22001=CARTESIAN_POINT ( 'NONE',  ( 0.1600813888245113392, 0.05392405859269203128, 0.1404791960285011465 ) ) ;
#22007=DIRECTION ( 'NONE',  ( -1.000000000000000000, 0.000000000000000000, 0.000000000000000000 ) ) ;
#22019=DIRECTION ( 'NONE',  ( -1.000000000000000000, 0.000000000000000000, 0.000000000000000000 ) ) ;
#22031=DIRECTION ( 'NONE',  ( 0.5735764363510447161, -0.8191520442889925757, 1.003171929053525486E-16 ) ) ;
#22040=DIRECTION ( 'NONE',  ( 0.000000000000000000, -1.000000000000000000, 0.000000000000000000 ) ) ;
#22042=AXIS2_PLACEMENT_3D ( 'NONE', #46798, #35095, #31743 ) ;
#22090=CARTESIAN_POINT ( 'NONE',  ( 0.1586955767088436831, -0.09170575825941058856, 0.1167515185291693181 ) ) ;
#22092=CARTESIAN_POINT ( 'NONE',  ( 0.1592537043533210628, 0.1452344447278379747, 0.02937400284934486849 ) ) ;
#22096=AXIS2_PLACEMENT_3D ( 'NONE', #6103, #24802, #32003 ) ;
#22104=DIRECTION ( 'NONE',  ( -1.000000000000000000, 0.000000000000000000, 0.000000000000000000 ) ) ;
#22112=VECTOR ( 'NONE', #3791, 39.37007874015748854 ) ;
#22124=ADVANCED_FACE ( 'NONE', ( #26483 ), #39917, .T. ) ;
#22131=CIRCLE ( 'NONE', #25185, 0.09842519685039370636 ) ;
#22170=CIRCLE ( 'NONE', #7627, 0.09842519685039370636 ) ;
#22186=ORIENTED_EDGE ( 'NONE', *, *, #29670, .F. ) ;
#22189=AXIS2_PLACEMENT_3D ( 'NONE', #39245, #6419, #35901 ) ;
#22223=ADVANCED_FACE ( 'NONE', ( #16853 ), #3973, .T. ) ;
#22234=EDGE_CURVE ( 'NONE', #21841, #44803, #26950, .T. ) ;
#22239=EDGE_LOOP ( 'NONE', ( #43258, #7452, #33006, #26870, #6170, #47116 ) ) ;
#22284=EDGE_CURVE ( 'NONE', #27712, #32411, #18512, .T. ) ;
#22295=ORIENTED_EDGE ( 'NONE', *, *, #1614, .T. ) ;
#22297=VECTOR ( 'NONE', #46771, 39.37007874015748854 ) ;
#22305=ORIENTED_EDGE ( 'NONE', *, *, #44446, .T. ) ;
#22315=CARTESIAN_POINT ( 'NONE',  ( 0.2642359194686346169, 1.205361022782824954E-17, -0.09842519685039370636 ) ) ;
#22318=DIRECTION ( 'NONE',  ( -1.000000000000000000, 0.000000000000000000, 0.000000000000000000 ) ) ;
#22338=CARTESIAN_POINT ( 'NONE',  ( 0.4755220087074803481, -3.032960542342102697E-32, 0.09842519685039370636 ) ) ;
#22345=DIRECTION ( 'NONE',  ( -1.000000000000000000, 0.000000000000000000, 0.000000000000000000 ) ) ;
#22350=EDGE_CURVE ( 'NONE', #1825, #18854, #9389, .T. ) ;
#22358=EDGE_LOOP ( 'NONE', ( #5793, #2491, #767, #30804, #37213 ) ) ;
#22361=DIRECTION ( 'NONE',  ( -1.000000000000000000, 0.000000000000000000, 0.000000000000000000 ) ) ;
#22381=DIRECTION ( 'NONE',  ( 0.000000000000000000, -1.000000000000000000, 0.000000000000000000 ) ) ;
#22441=LINE ( 'NONE', #44467, #26676 ) ;
#22466=CARTESIAN_POINT ( 'NONE',  ( 0.5113546317124669782, 4.466152701071653354E-17, 0.000000000000000000 ) ) ;
#22470=LINE ( 'NONE', #40196, #22112 ) ;
#22475=AXIS2_PLACEMENT_3D ( 'NONE', #9061, #41376, #41857 ) ;
#22491=CARTESIAN_POINT ( 'NONE',  ( 0.4453382816733590377, -0.09842519685039370636, 1.205361022782828805E-17 ) ) ;
#22497=CARTESIAN_POINT ( 'NONE',  ( 0.2642359194686346169, 0.09842519685039370636, 0.000000000000000000 ) ) ;
#22504=CARTESIAN_POINT ( 'NONE',  ( 0.1637325661183565428, 0.08225671873206810703, -0.1377952755905511306 ) ) ;
#22514=ORIENTED_EDGE ( 'NONE', *, *, #2373, .F. ) ;
#22536=ORIENTED_EDGE ( 'NONE', *, *, #4010, .F. ) ;
#22537=CIRCLE ( 'NONE', #16438, 0.09842519685039370636 ) ;
#22540=AXIS2_PLACEMENT_3D ( 'NONE', #16212, #11429, #7814 ) ;
#22545=EDGE_LOOP ( 'NONE', ( #3969, #5037, #21442, #45586, #45700 ) ) ;
#22550=EDGE_CURVE ( 'NONE', #8098, #829, #41460, .T. ) ;
#22552=EDGE_CURVE ( 'NONE', #29529, #42873, #9911, .T. ) ;
#22556=DIRECTION ( 'NONE',  ( 0.000000000000000000, 0.000000000000000000, 1.000000000000000000 ) ) ;
#22559=DIRECTION ( 'NONE',  ( -1.000000000000000000, 0.000000000000000000, 0.000000000000000000 ) ) ;
#22567=CARTESIAN_POINT ( 'NONE',  ( 0.1588779435336218349, 0.1435649425735163465, 0.03225083113271716428 ) ) ;
#22579=CARTESIAN_POINT ( 'NONE',  ( 0.1599045142068303837, 0.1486426375328276928, -0.02349808476882435729 ) ) ;
#22588=ORIENTED_EDGE ( 'NONE', *, *, #36491, .F. ) ;
#22625=EDGE_CURVE ( 'NONE', #19741, #34889, #43396, .T. ) ;
#22662=CARTESIAN_POINT ( 'NONE',  ( 0.3246033735368759610, 4.766607801171850497E-17, 0.000000000000000000 ) ) ;
#22767=ORIENTED_EDGE ( 'NONE', *, *, #37009, .T. ) ;
#22780=VERTEX_POINT ( 'NONE', #21877 ) ;
#22805=ORIENTED_EDGE ( 'NONE', *, *, #35133, .T. ) ;
#22811=CARTESIAN_POINT ( 'NONE',  ( 0.1582120475477782062, 0.1402876732178915120, -0.03788922412827557679 ) ) ;
#22825=EDGE_CURVE ( 'NONE', #44147, #13283, #32917, .T. ) ;
#22826=CARTESIAN_POINT ( 'NONE',  ( 0.5660731898098425585, -0.09842519685039370636, 1.205361022782828805E-17 ) ) ;
#22829=CARTESIAN_POINT ( 'NONE',  ( 0.1588150004738562715, -0.09138854459949809217, -0.1173009487050077904 ) ) ;
#22837=VERTEX_POINT ( 'NONE', #34795 ) ;
#22842=B_SPLINE_CURVE_WITH_KNOTS ( 'NONE', 3,
 ( #14727, #25031, #29400, #25535, #7519 ),
 .UNSPECIFIED., .F., .F.,
 ( 4, 1, 4 ),
 ( 0.000000000000000000, 0.002020725942163694843, 0.004041451884327384482 ),
 .UNSPECIFIED. ) ;
#22843=CARTESIAN_POINT ( 'NONE',  ( 0.01035225325197390578, -0.08294251416999544324, -0.1319299025311632956 ) ) ;
#22858=CIRCLE ( 'NONE', #13685, 0.08090551181102362266 ) ;
#22861=CARTESIAN_POINT ( 'NONE',  ( 0.000000000000000000, 0.000000000000000000, 0.09842519685039370636 ) ) ;
#22864=CARTESIAN_POINT ( 'NONE',  ( 0.2397010884053811242, 4.466152701071653354E-17, 0.000000000000000000 ) ) ;
#22893=ADVANCED_FACE ( 'NONE', ( #15874 ), #9382, .F. ) ;
#22897=CARTESIAN_POINT ( 'NONE',  ( 0.3425196850393700809, -0.08090551181102362266, 0.000000000000000000 ) ) ;
#22899=ORIENTED_EDGE ( 'NONE', *, *, #45207, .F. ) ;
#22902=CARTESIAN_POINT ( 'NONE',  ( 0.004714672091284868166, -0.04816527795631998093, 0.1377938255964467340 ) ) ;
#22903=CONICAL_SURFACE ( 'NONE', #30595, 0.09842519685039370636, 0.9599310885968824758 ) ;
#22936=EDGE_LOOP ( 'NONE', ( #29475, #44565, #32044, #37156, #14543, #20534 ) ) ;
#22975=VERTEX_POINT ( 'NONE', #13495 ) ;
#22989=DIRECTION ( 'NONE',  ( 1.000000000000000000, 0.000000000000000000, 0.000000000000000000 ) ) ;
#22998=EDGE_CURVE ( 'NONE', #30008, #11246, #34877, .T. ) ;
#23026=CARTESIAN_POINT ( 'NONE',  ( 0.000000000000000000, 0.000000000000000000, 0.000000000000000000 ) ) ;
#23045=ORIENTED_EDGE ( 'NONE', *, *, #9595, .T. ) ;
#23061=ORIENTED_EDGE ( 'NONE', *, *, #36589, .F. ) ;
#23076=VERTEX_POINT ( 'NONE', #20671 ) ;
#23098=VECTOR ( 'NONE', #24966, 39.37007874015748143 ) ;
#23134=VECTOR ( 'NONE', #46611, 39.37007874015748143 ) ;
#23142=ORIENTED_EDGE ( 'NONE', *, *, #1193, .F. ) ;
#23146=DIRECTION ( 'NONE',  ( -1.000000000000000000, 0.000000000000000000, 0.000000000000000000 ) ) ;
#23166=DIRECTION ( 'NONE',  ( 0.000000000000000000, 0.000000000000000000, -1.000000000000000000 ) ) ;
#23181=DIRECTION ( 'NONE',  ( 1.000000000000000000, 0.000000000000000000, 0.000000000000000000 ) ) ;
#23183=ORIENTED_EDGE ( 'NONE', *, *, #28056, .T. ) ;
#23192=DIRECTION ( 'NONE',  ( 0.000000000000000000, 0.000000000000000000, 1.000000000000000000 ) ) ;
#23214=DIRECTION ( 'NONE',  ( 0.000000000000000000, -1.000000000000000000, 0.000000000000000000 ) ) ;
#23227=EDGE_CURVE ( 'NONE', #26427, #12403, #2454, .T. ) ;
#23278=EDGE_CURVE ( 'NONE', #35809, #827, #25479, .T. ) ;
#23279=CARTESIAN_POINT ( 'NONE',  ( 0.1598936088129108701, -0.05389714384564588123, 0.1404773021332396676 ) ) ;
#23291=ORIENTED_EDGE ( 'NONE', *, *, #20397, .T. ) ;
#23308=CIRCLE ( 'NONE', #39359, 0.09842519685039370636 ) ;
#23363=DIRECTION ( 'NONE',  ( 0.000000000000000000, -1.000000000000000000, 0.000000000000000000 ) ) ;
#23368=DIRECTION ( 'NONE',  ( 0.000000000000000000, -1.000000000000000000, 0.000000000000000000 ) ) ;
#23371=ORIENTED_EDGE ( 'NONE', *, *, #43215, .F. ) ;
#23379=VERTEX_POINT ( 'NONE', #13390 ) ;
#23389=ORIENTED_EDGE ( 'NONE', *, *, #36822, .F. ) ;
#23392=ADVANCED_FACE ( 'NONE', ( #16512 ), #27560, .T. ) ;
#23396=FACE_OUTER_BOUND ( 'NONE', #18589, .T. ) ;
#23405=DIRECTION ( 'NONE',  ( 1.000000000000000000, 0.000000000000000000, 0.000000000000000000 ) ) ;
#23415=VECTOR ( 'NONE', #25578, 39.37007874015748143 ) ;
#23424=DIRECTION ( 'NONE',  ( -1.000000000000000000, 0.000000000000000000, 0.000000000000000000 ) ) ;
#23436=DIRECTION ( 'NONE',  ( -1.000000000000000000, 0.000000000000000000, 0.000000000000000000 ) ) ;
#23447=ADVANCED_FACE ( 'NONE', ( #17206 ), #11724, .T. ) ;
#23450=DIRECTION ( 'NONE',  ( 0.000000000000000000, -1.000000000000000000, 0.000000000000000000 ) ) ;
#23452=ORIENTED_EDGE ( 'NONE', *, *, #17173, .F. ) ;
#23460=FACE_OUTER_BOUND ( 'NONE', #42415, .T. ) ;
#23465=FACE_OUTER_BOUND ( 'NONE', #37187, .T. ) ;
#23485=CARTESIAN_POINT ( 'NONE',  ( 0.1558458267876858538, 0.09164332750980257181, -0.1168596517594497897 ) ) ;
#23487=ORIENTED_EDGE ( 'NONE', *, *, #729, .T. ) ;
#23514=DIRECTION ( 'NONE',  ( 0.000000000000000000, 0.000000000000000000, 1.000000000000000000 ) ) ;
#23521=CARTESIAN_POINT ( 'NONE',  ( 0.003583035186813061154, 0.09844385435687157127, 0.1050988454125816457 ) ) ;
#23544=ORIENTED_EDGE ( 'NONE', *, *, #38476, .T. ) ;
#23558=CIRCLE ( 'NONE', #2861, 0.09842519685039370636 ) ;
#23599=EDGE_CURVE ( 'NONE', #4842, #19535, #38490, .T. ) ;
#23632=FACE_OUTER_BOUND ( 'NONE', #43518, .T. ) ;
#23654=EDGE_CURVE ( 'NONE', #34498, #41232, #36948, .T. ) ;
#23662=DIRECTION ( 'NONE',  ( -0.5735764363510518216, 0.8191520442889876907, 1.003171929053519693E-16 ) ) ;
#23664=DIRECTION ( 'NONE',  ( 0.000000000000000000, -1.000000000000000000, 0.000000000000000000 ) ) ;
#23669=EDGE_LOOP ( 'NONE', ( #10653, #8064, #14422, #32018, #40461 ) ) ;
#23678=AXIS2_PLACEMENT_3D ( 'NONE', #34315, #1446, #30961 ) ;
#23710=FACE_OUTER_BOUND ( 'NONE', #47353, .T. ) ;
#23750=CIRCLE ( 'NONE', #6120, 0.09842519685039370636 ) ;
#23785=CARTESIAN_POINT ( 'NONE',  ( 0.001477421097737172118, 0.1327706367220780892, 0.04562747989112364566 ) ) ;
#23787=CARTESIAN_POINT ( 'NONE',  ( 0.5358894627757212481, -0.09842519685039370636, 1.205361022782828805E-17 ) ) ;
#23791=VECTOR ( 'NONE', #18381, 39.37007874015748143 ) ;
#23830=DIRECTION ( 'NONE',  ( 0.000000000000000000, -1.000000000000000000, 0.000000000000000000 ) ) ;
#23848=VERTEX_POINT ( 'NONE', #7473 ) ;
#23850=EDGE_CURVE ( 'NONE', #11246, #11416, #41685, .T. ) ;
#23874=CARTESIAN_POINT ( 'NONE',  ( 0.1645805237892204731, 0.1627998762483226503, -0.0008383936782242519276 ) ) ;
#23885=CARTESIAN_POINT ( 'NONE',  ( 0.2698848154395015464, 4.466152701071653354E-17, 0.000000000000000000 ) ) ;
#23889=AXIS2_PLACEMENT_3D ( 'NONE', #25932, #6995, #40513 ) ;
#23901=VERTEX_POINT ( 'NONE', #44129 ) ;
#23914=DIRECTION ( 'NONE',  ( 0.000000000000000000, 0.000000000000000000, 1.000000000000000000 ) ) ;
#23935=DIRECTION ( 'NONE',  ( 0.000000000000000000, 0.000000000000000000, -1.000000000000000000 ) ) ;
#23937=DIRECTION ( 'NONE',  ( -1.000000000000000000, 0.000000000000000000, 0.000000000000000000 ) ) ;
#23938=EDGE_CURVE ( 'NONE', #27624, #23076, #46891, .T. ) ;
#23940=DIRECTION ( 'NONE',  ( -1.000000000000000000, 0.000000000000000000, 0.000000000000000000 ) ) ;
#23956=VERTEX_POINT ( 'NONE', #26660 ) ;
#23960=ORIENTED_EDGE ( 'NONE', *, *, #23654, .T. ) ;
#23963=DIRECTION ( 'NONE',  ( -1.000000000000000000, 0.000000000000000000, 0.000000000000000000 ) ) ;
#23966=AXIS2_PLACEMENT_3D ( 'NONE', #31744, #31274, #21399 ) ;
#23995=CARTESIAN_POINT ( 'NONE',  ( 0.1582007246420326085, -0.03721045995875271739, 0.1404371117717379547 ) ) ;
#24044=EDGE_CURVE ( 'NONE', #18563, #12246, #27142, .T. ) ;
#24056=CARTESIAN_POINT ( 'NONE',  ( 0.2519685039370078705, 4.616380251121755931E-17, 0.000000000000000000 ) ) ;
#24066=EDGE_LOOP ( 'NONE', ( #21408, #28828, #42254, #40700, #27533 ) ) ;
#24073=CARTESIAN_POINT ( 'NONE',  ( 0.4934383202099732468, 4.616380251121755931E-17, 0.000000000000000000 ) ) ;
#24093=ORIENTED_EDGE ( 'NONE', *, *, #15546, .T. ) ;
#24100=AXIS2_PLACEMENT_3D ( 'NONE', #41086, #19309, #26295 ) ;
#24103=ADVANCED_FACE ( 'NONE', ( #27383 ), #15635, .F. ) ;
#24152=LINE ( 'NONE', #31814, #44747 ) ;
#24158=ORIENTED_EDGE ( 'NONE', *, *, #24044, .T. ) ;
#24174=FACE_OUTER_BOUND ( 'NONE', #8149, .T. ) ;
#24184=DIRECTION ( 'NONE',  ( -1.000000000000000000, 0.000000000000000000, 0.000000000000000000 ) ) ;
#24215=EDGE_CURVE ( 'NONE', #36523, #34498, #46933, .T. ) ;
#24217=ADVANCED_FACE ( 'NONE', ( #40233 ), #12515, .T. ) ;
#24228=AXIS2_PLACEMENT_3D ( 'NONE', #33935, #11169, #15716 ) ;
#24244=EDGE_CURVE ( 'NONE', #1067, #42873, #27834, .T. ) ;
#24245=CARTESIAN_POINT ( 'NONE',  ( 0.4811709046783464450, 4.466152701071653354E-17, 0.000000000000000000 ) ) ;
#24253=EDGE_CURVE ( 'NONE', #11416, #28921, #10242, .T. ) ;
#24266=DIRECTION ( 'NONE',  ( 0.5735764363510447161, -0.8191520442889925757, 1.003171929053525486E-16 ) ) ;
#24271=CARTESIAN_POINT ( 'NONE',  ( 0.1602931993194444682, -0.1591122789105269553, 0.000000000000000000 ) ) ;
#24286=CARTESIAN_POINT ( 'NONE',  ( 0.1643927470070918051, 0.1622860936273138877, 1.482178915982735805E-13 ) ) ;
#24314=EDGE_LOOP ( 'NONE', ( #21415, #9981, #9986, #8388, #39177 ) ) ;
#24337=CARTESIAN_POINT ( 'NONE',  ( 0.000000000000000000, 0.000000000000000000, 0.000000000000000000 ) ) ;
#24350=LINE ( 'NONE', #20508, #29950 ) ;
#24367=EDGE_CURVE ( 'NONE', #23901, #14042, #21670, .T. ) ;
#24369=CONICAL_SURFACE ( 'NONE', #8278, 0.1377952755905511861, 1.047197551196598297 ) ;
#24396=DIRECTION ( 'NONE',  ( -1.000000000000000000, 0.000000000000000000, 0.000000000000000000 ) ) ;
#24406=CARTESIAN_POINT ( 'NONE',  ( 0.0003553830333942854065, 0.1126092284109782571, -0.08054791328661504990 ) ) ;
#24414=CARTESIAN_POINT ( 'NONE',  ( 0.1596650774283297214, 0.1494101348903360271, -0.02216197906078976390 ) ) ;
#24423=EDGE_CURVE ( 'NONE', #35869, #32338, #14034, .T. ) ;
#24441=LENGTH_MEASURE_WITH_UNIT ( LENGTH_MEASURE( 0.02539999999999999897 ), #42624 ) ;
#24443=DIRECTION ( 'NONE',  ( 0.000000000000000000, 1.000000000000000000, 0.000000000000000000 ) ) ;
#24451=CARTESIAN_POINT ( 'NONE',  ( 0.4151545546392377273, 4.766607801171850497E-17, 0.000000000000000000 ) ) ;
#24460=ADVANCED_FACE ( 'NONE', ( #19344 ), #36985, .T. ) ;
#24461=AXIS2_PLACEMENT_3D ( 'NONE', #43364, #11753, #7653 ) ;
#24476=AXIS2_PLACEMENT_3D ( 'NONE', #38912, #20697, #5619 ) ;
#24488=ORIENTED_EDGE ( 'NONE', *, *, #12026, .F. ) ;
#24514=EDGE_CURVE ( 'NONE', #4886, #20673, #29388, .T. ) ;
#24523=ORIENTED_EDGE ( 'NONE', *, *, #6270, .F. ) ;
#24532=CARTESIAN_POINT ( 'NONE',  ( 0.2519685039370078705, 4.616380251121755931E-17, 0.000000000000000000 ) ) ;
#24554=AXIS2_PLACEMENT_3D ( 'NONE', #20557, #9317, #27077 ) ;
#24568=CARTESIAN_POINT ( 'NONE',  ( 0.1636096867514420516, -0.08042879899057427118, -0.1393067463704355524 ) ) ;
#24600=CARTESIAN_POINT ( 'NONE',  ( 0.006399490001471973451, 0.05645636337047107295, -0.1377922246562235109 ) ) ;
#24612=FACE_OUTER_BOUND ( 'NONE', #22936, .T. ) ;
#24637=ORIENTED_EDGE ( 'NONE', *, *, #46658, .F. ) ;
#24642=CARTESIAN_POINT ( 'NONE',  ( 0.1573498687646868455, 0.02697554138032596735, -0.1404067023994485797 ) ) ;
#24687=DIRECTION ( 'NONE',  ( 0.000000000000000000, 1.000000000000000000, 0.000000000000000000 ) ) ;
#24688=CARTESIAN_POINT ( 'NONE',  ( 0.1592537043533306107, -0.1452344447278721418, -0.02937400284930944891 ) ) ;
#24699=DIRECTION ( 'NONE',  ( 0.000000000000000000, -1.000000000000000000, 0.000000000000000000 ) ) ;
#24710=ORIENTED_EDGE ( 'NONE', *, *, #25397, .T. ) ;
#24724=EDGE_CURVE ( 'NONE', #46256, #32405, #5983, .T. ) ;
#24729=DIRECTION ( 'NONE',  ( 0.000000000000000000, 0.000000000000000000, -1.000000000000000000 ) ) ;
#24740=CARTESIAN_POINT ( 'NONE',  ( 0.5839895013123354017, 4.616380251121755931E-17, 0.000000000000000000 ) ) ;
#24768=FACE_OUTER_BOUND ( 'NONE', #29676, .T. ) ;
#24784=ORIENTED_EDGE ( 'NONE', *, *, #31995, .F. ) ;
#24785=CARTESIAN_POINT ( 'NONE',  ( 0.001477421097679590357, -0.1327706367218486061, -0.04562747989148444039 ) ) ;
#24800=CARTESIAN_POINT ( 'NONE',  ( 0.1527643571647078757, -0.02877566944792483983, 0.1377952755905511861 ) ) ;
#24802=DIRECTION ( 'NONE',  ( -1.000000000000000000, 0.000000000000000000, 0.000000000000000000 ) ) ;
#24819=ORIENTED_EDGE ( 'NONE', *, *, #40395, .T. ) ;
#24837=VECTOR ( 'NONE', #45629, 39.37007874015748143 ) ;
#24838=CARTESIAN_POINT ( 'NONE',  ( 0.004759645784635634091, 0.04840028875945810022, -0.1377938811595105506 ) ) ;
#24890=VERTEX_POINT ( 'NONE', #6685 ) ;
#24908=EDGE_CURVE ( 'NONE', #829, #43186, #32605, .T. ) ;
#24929=CARTESIAN_POINT ( 'NONE',  ( 0.1619907858920943411, -0.1553500912767243614, -0.01195870310697006757 ) ) ;
#24932=AXIS2_PLACEMENT_3D ( 'NONE', #11218, #43544, #47396 ) ;
#24960=ADVANCED_FACE ( 'NONE', ( #43578 ), #14067, .T. ) ;
#24966=DIRECTION ( 'NONE',  ( -1.000000000000000000, 0.000000000000000000, 0.000000000000000000 ) ) ;
#24969=DIRECTION ( 'NONE',  ( 0.000000000000000000, 0.000000000000000000, -1.000000000000000000 ) ) ;
#24970=CARTESIAN_POINT ( 'NONE',  ( 0.1636096891710253631, -0.1608575822371333675, 1.015068312943880306E-08 ) ) ;
#24975=CARTESIAN_POINT ( 'NONE',  ( 0.3547871005709968273, 0.09842519685039370636, 0.000000000000000000 ) ) ;
#24985=CARTESIAN_POINT ( 'NONE',  ( 0.1636882031745872657, 0.1609730488751321964, 5.008074394060701725E-08 ) ) ;
#24986=EDGE_LOOP ( 'NONE', ( #13527, #11590, #31045, #5538, #25195, #29748 ) ) ;
#25015=EDGE_CURVE ( 'NONE', #31651, #35175, #29508, .T. ) ;
#25025=AXIS2_PLACEMENT_3D ( 'NONE', #11984, #27088, #30683 ) ;
#25031=CARTESIAN_POINT ( 'NONE',  ( 0.1555687797274982465, -0.1458529223346496095, 0.02296587926509184932 ) ) ;
#25045=ORIENTED_EDGE ( 'NONE', *, *, #41432, .F. ) ;
#25057=AXIS2_PLACEMENT_3D ( 'NONE', #31390, #32078, #45959 ) ;
#25077=CARTESIAN_POINT ( 'NONE',  ( 0.6141732283464567121, 0.000000000000000000, 0.000000000000000000 ) ) ;
#25082=CARTESIAN_POINT ( 'NONE',  ( 0.000000000000000000, 0.000000000000000000, 0.000000000000000000 ) ) ;
#25103=DIRECTION ( 'NONE',  ( -0.5735764363510518216, -0.8191520442889876907, 0.000000000000000000 ) ) ;
#25106=ORIENTED_EDGE ( 'NONE', *, *, #10694, .T. ) ;
#25124=AXIS2_PLACEMENT_3D ( 'NONE', #45973, #20580, #13412 ) ;
#25142=VECTOR ( 'NONE', #43235, 39.37007874015748143 ) ;
#25153=ORIENTED_EDGE ( 'NONE', *, *, #15546, .F. ) ;
#25159=EDGE_CURVE ( 'NONE', #21151, #16941, #34755, .T. ) ;
#25167=VERTEX_POINT ( 'NONE', #40909 ) ;
#25185=AXIS2_PLACEMENT_3D ( 'NONE', #17554, #32192, #42471 ) ;
#25195=ORIENTED_EDGE ( 'NONE', *, *, #36108, .F. ) ;
#25199=CIRCLE ( 'NONE', #31341, 0.08090551181102362266 ) ;
#25224=DIRECTION ( 'NONE',  ( -1.000000000000000000, 0.000000000000000000, 0.000000000000000000 ) ) ;
#25225=DIRECTION ( 'NONE',  ( 0.000000000000000000, -1.000000000000000000, 0.000000000000000000 ) ) ;
#25238=ORIENTED_EDGE ( 'NONE', *, *, #10564, .T. ) ;
#25261=ORIENTED_EDGE ( 'NONE', *, *, #46847, .F. ) ;
#25269=CIRCLE ( 'NONE', #1547, 0.08090551181102362266 ) ;
#25272=EDGE_CURVE ( 'NONE', #16941, #26427, #26101, .T. ) ;
#25283=CARTESIAN_POINT ( 'NONE',  ( 0.1595445804228954878, 0.05486576152185763944, 0.1404716313526493954 ) ) ;
#25317=ORIENTED_EDGE ( 'NONE', *, *, #41756, .T. ) ;
#25321=CARTESIAN_POINT ( 'NONE',  ( 0.01230737760510397689, 0.07955613945526338049, 0.1377952755905511861 ) ) ;
#25324=ORIENTED_EDGE ( 'NONE', *, *, #33414, .F. ) ;
#25338=ADVANCED_FACE ( 'NONE', ( #44749 ), #27307, .F. ) ;
#25339=AXIS2_PLACEMENT_3D ( 'NONE', #37341, #33319, #4492 ) ;
#25359=DIRECTION ( 'NONE',  ( 0.000000000000000000, 0.000000000000000000, -1.000000000000000000 ) ) ;
#25362=CARTESIAN_POINT ( 'NONE',  ( 0.1636082376784445125, 0.08043339677773757301, 0.1393150588506956167 ) ) ;
#25363=CARTESIAN_POINT ( 'NONE',  ( 0.1578913225048159952, 0.03378178545796894222, -0.1404269458896922063 ) ) ;
#25368=CYLINDRICAL_SURFACE ( 'NONE', #22189, 0.09842519685039370636 ) ;
#25372=DIRECTION ( 'NONE',  ( 0.000000000000000000, 1.000000000000000000, 0.000000000000000000 ) ) ;
#25380=VECTOR ( 'NONE', #39227, 39.37007874015748143 ) ;
#25382=EDGE_CURVE ( 'NONE', #9638, #46176, #14859, .T. ) ;
#25397=EDGE_CURVE ( 'NONE', #44147, #21725, #40849, .T. ) ;
#25407=AXIS2_PLACEMENT_3D ( 'NONE', #44885, #25773, #339 ) ;
#25437=CARTESIAN_POINT ( 'NONE',  ( 0.001477421097695146273, -0.1058998750575174536, 0.09216900433216509980 ) ) ;
#25468=CIRCLE ( 'NONE', #20853, 0.08090551181102362266 ) ;
#25478=EDGE_LOOP ( 'NONE', ( #20993, #43020, #11755, #5105, #22588 ) ) ;
#25479=CIRCLE ( 'NONE', #1736, 0.09842519685039370636 ) ;
#25516=CARTESIAN_POINT ( 'NONE',  ( 0.5358894627757212481, 0.09842519685039370636, 0.000000000000000000 ) ) ;
#25518=ORIENTED_EDGE ( 'NONE', *, *, #11475, .F. ) ;
#25528=CARTESIAN_POINT ( 'NONE',  ( 0.2204724409448818867, -0.07955613945526318620, 0.1377952755905511861 ) ) ;
#25535=CARTESIAN_POINT ( 'NONE',  ( 0.1555687797274980522, -0.09281549603114055969, 0.1148293963254594513 ) ) ;
#25540=CARTESIAN_POINT ( 'NONE',  ( 0.2204724409448818867, -0.1591122789105269553, 0.000000000000000000 ) ) ;
#25551=CARTESIAN_POINT ( 'NONE',  ( 0.003086919931961261236, 0.03878710687431414367, 0.1377952978224512848 ) ) ;
#25578=DIRECTION ( 'NONE',  ( -1.000000000000000000, 0.000000000000000000, 0.000000000000000000 ) ) ;
#25597=ORIENTED_EDGE ( 'NONE', *, *, #5235, .F. ) ;
#25602=CARTESIAN_POINT ( 'NONE',  ( 0.1624141299553157614, 0.07987677361383865859, 0.1383529584519434252 ) ) ;
#25620=CLOSED_SHELL ( 'NONE', ( #4357, #23447, #22893, #36329, #46196, #45395, #22223, #45736, #11065, #21000, #10302, #15170, #189, #14615, #18852, #44607, #15271, #23392, #28832, #13476, #32400, #5114, #24960, #11368, #33300, #45485, #45270, #33583, #14350, #42028, #24460, #4977, #36235, #39693, #30029, #30143, #19585, #3468, #29914, #21791, #19847, #40249, #9814, #28936, #3338, #24103, #25338, #28157, #1670, #21967, #3247, #27243, #40023, #24217, #10052, #21761, #11347, #41354, #6915, #45642, #1564, #12136, #36044, #36639, #22124, #31252, #4594, #15727, #1674, #40020, #13750, #27586, #3783, #38826, #31078, #45572, #8547, #15384, #37165, #42361, #10854, #18935, #39787, #31417, #12312, #37097, #31681, #10297, #17651, #47235, #32664, #26212, #42173, #16362, #38298, #25879, #15065, #32304, #34946, #44838, #13532 ) ) ;
#25635=( NAMED_UNIT ( * ) SI_UNIT ( $, .STERADIAN. ) SOLID_ANGLE_UNIT ( ) ) ;
#25649=CARTESIAN_POINT ( 'NONE',  ( 0.5358894627757212481, 4.766607801171850497E-17, 0.000000000000000000 ) ) ;
#25653=CARTESIAN_POINT ( 'NONE',  ( 0.2821522309711287368, 4.616380251121755931E-17, 0.000000000000000000 ) ) ;
#25658=CARTESIAN_POINT ( 'NONE',  ( 0.3849708276051176936, 4.766607801171850497E-17, 0.000000000000000000 ) ) ;
#25661=CARTESIAN_POINT ( 'NONE',  ( 0.3425196850393700809, 0.08090551181102362266, 0.000000000000000000 ) ) ;
#25692=CARTESIAN_POINT ( 'NONE',  ( 0.000000000000000000, 0.000000000000000000, 0.000000000000000000 ) ) ;
#25697=FACE_OUTER_BOUND ( 'NONE', #13525, .T. ) ;
#25716=CARTESIAN_POINT ( 'NONE',  ( 0.1554371429169691954, -0.1056204263327882586, 0.09265060645564116015 ) ) ;
#25731=CARTESIAN_POINT ( 'NONE',  ( 0.1564139474900879123, 0.1149079234230807184, -0.08174552760864516043 ) ) ;
#25742=ORIENTED_EDGE ( 'NONE', *, *, #13747, .T. ) ;
#25743=VECTOR ( 'NONE', #964, 39.37007874015748143 ) ;
#25769=DIRECTION ( 'NONE',  ( -1.000000000000000000, 0.000000000000000000, 0.000000000000000000 ) ) ;
#25773=DIRECTION ( 'NONE',  ( 1.000000000000000000, 0.000000000000000000, 0.000000000000000000 ) ) ;
#25774=DIRECTION ( 'NONE',  ( 0.5735764363510447161, -0.8191520442889925757, 1.003171929053525486E-16 ) ) ;
#25788=ORIENTED_EDGE ( 'NONE', *, *, #42449, .T. ) ;
#25807=CARTESIAN_POINT ( 'NONE',  ( 0.003436456682582578626, -0.04094436872149315176, 0.1377952874252535709 ) ) ;
#25831=EDGE_CURVE ( 'NONE', #19535, #39641, #43948, .T. ) ;
#25836=CARTESIAN_POINT ( 'NONE',  ( 0.1498753904841986506, -0.1193342091828952928, -0.06889763779527559306 ) ) ;
#25843=CARTESIAN_POINT ( 'NONE',  ( 0.3123359580052492146, 0.08090551181102362266, 0.000000000000000000 ) ) ;
#25844=CARTESIAN_POINT ( 'NONE',  ( 0.1588891437629025849, 0.04395497937033298469, 0.1404564352527446769 ) ) ;
#25860=CARTESIAN_POINT ( 'NONE',  ( 0.5113546317124669782, 0.09842519685039370636, 1.205361022782828805E-17 ) ) ;
#25868=DIRECTION ( 'NONE',  ( 0.000000000000000000, 0.000000000000000000, 1.000000000000000000 ) ) ;
#25879=ADVANCED_FACE ( 'NONE', ( #16445 ), #34819, .T. ) ;
#25897=CARTESIAN_POINT ( 'NONE',  ( 0.5966535433070866423, 1.205361022782828805E-17, -0.09842519685039370636 ) ) ;
#25900=CARTESIAN_POINT ( 'NONE',  ( 0.001132063567009175716, -0.1075630933946832152, 0.08929056810482036144 ) ) ;
#25904=ORIENTED_EDGE ( 'NONE', *, *, #23938, .F. ) ;
#25932=CARTESIAN_POINT ( 'NONE',  ( 0.3727034120734909473, 4.616380251121755931E-17, 0.000000000000000000 ) ) ;
#25937=FACE_OUTER_BOUND ( 'NONE', #46914, .T. ) ;
#25942=CARTESIAN_POINT ( 'NONE',  ( 0.1610681406158918083, 0.07955616528309404634, -0.1377952308554367400 ) ) ;
#25945=ORIENTED_EDGE ( 'NONE', *, *, #18938, .F. ) ;
#25994=DIRECTION ( 'NONE',  ( 0.000000000000000000, -1.000000000000000000, 0.000000000000000000 ) ) ;
#25998=DIRECTION ( 'NONE',  ( 0.000000000000000000, -1.000000000000000000, 0.000000000000000000 ) ) ;
#25999=CARTESIAN_POINT ( 'NONE',  ( 0.5717220857807087109, 1.205361022782824954E-17, -0.09842519685039370636 ) ) ;
#26001=ORIENTED_EDGE ( 'NONE', *, *, #35178, .F. ) ;
#26012=CARTESIAN_POINT ( 'NONE',  ( 0.1579024634500803825, -0.1385691271449887019, 0.04084555919664353829 ) ) ;
#26029=DIRECTION ( 'NONE',  ( 0.000000000000000000, -1.000000000000000000, 0.000000000000000000 ) ) ;
#26037=CARTESIAN_POINT ( 'NONE',  ( 0.000000000000000000, 0.000000000000000000, 0.09842519685039370636 ) ) ;
#26043=EDGE_LOOP ( 'NONE', ( #13518, #4271, #18111, #2609, #4671, #31359 ) ) ;
#26059=CARTESIAN_POINT ( 'NONE',  ( 0.1555213372790610893, 0.1050481006241530957, 0.09364190366146164790 ) ) ;
#26076=CONICAL_SURFACE ( 'NONE', #7687, 0.08090551181102362266, 0.9599310885968742602 ) ;
#26087=AXIS2_PLACEMENT_3D ( 'NONE', #42719, #28645, #6076 ) ;
#26096=EDGE_CURVE ( 'NONE', #23956, #8667, #22842, .T. ) ;
#26101=LINE ( 'NONE', #27064, #37773 ) ;
#26116=FACE_OUTER_BOUND ( 'NONE', #37685, .T. ) ;
#26132=VERTEX_POINT ( 'NONE', #6807 ) ;
#26140=CARTESIAN_POINT ( 'NONE',  ( 0.002794899976001078128, -0.1008940036867598672, 0.1008370195737266495 ) ) ;
#26144=ORIENTED_EDGE ( 'NONE', *, *, #29340, .T. ) ;
#26179=AXIS2_PLACEMENT_3D ( 'NONE', #24451, #13440, #6699 ) ;
#26187=CARTESIAN_POINT ( 'NONE',  ( 0.1636096891713402501, 0.08042878232803850336, -0.1393067576844427280 ) ) ;
#26190=EDGE_LOOP ( 'NONE', ( #33713, #35860, #29167, #23061, #1312, #13644 ) ) ;
#26212=ADVANCED_FACE ( 'NONE', ( #3211 ), #3427, .T. ) ;
#26220=AXIS2_PLACEMENT_3D ( 'NONE', #44119, #30032, #11795 ) ;
#26222=CARTESIAN_POINT ( 'NONE',  ( 0.008625679036690871507, -0.08625453335776224473, -0.1261914363111028836 ) ) ;
#26225=VECTOR ( 'NONE', #11098, 39.37007874015748143 ) ;
#26249=EDGE_LOOP ( 'NONE', ( #36414, #26144, #35729, #10633, #7330 ) ) ;
#26256=CARTESIAN_POINT ( 'NONE',  ( 0.4453382816733590377, 4.766607801171850497E-17, 0.000000000000000000 ) ) ;
#26260=CARTESIAN_POINT ( 'NONE',  ( 0.1594510458733827685, -0.09722652869640824314, 0.1125335630252017605 ) ) ;
#26266=AXIS2_PLACEMENT_3D ( 'NONE', #7486, #36966, #18743 ) ;
#26282=AXIS2_PLACEMENT_3D ( 'NONE', #44451, #9419, #16606 ) ;
#26286=ORIENTED_EDGE ( 'NONE', *, *, #24724, .T. ) ;
#26288=FACE_OUTER_BOUND ( 'NONE', #24066, .T. ) ;
#26295=DIRECTION ( 'NONE',  ( 0.000000000000000000, -1.000000000000000000, 0.000000000000000000 ) ) ;
#26305=DIRECTION ( 'NONE',  ( -0.5735764363510518216, 0.8191520442889876907, 1.003171929053519693E-16 ) ) ;
#26309=CARTESIAN_POINT ( 'NONE',  ( 0.1564636162838604350, 0.1073287318776763866, 0.09487486835524192030 ) ) ;
#26318=CARTESIAN_POINT ( 'NONE',  ( 0.1602931993194444682, 0.1591122789105269553, 0.000000000000000000 ) ) ;
#26323=ORIENTED_EDGE ( 'NONE', *, *, #34982, .F. ) ;
#26347=( NAMED_UNIT ( * ) PLANE_ANGLE_UNIT ( ) SI_UNIT ( $, .RADIAN. ) ) ;
#26364=CARTESIAN_POINT ( 'NONE',  ( 0.1563808587774279391, -0.02736954274996897599, -0.1403846824214370070 ) ) ;
#26392=CARTESIAN_POINT ( 'NONE',  ( 0.4151545546392377273, -0.09842519685039370636, 1.205361022782828805E-17 ) ) ;
#26427=VERTEX_POINT ( 'NONE', #26708 ) ;
#26428=CIRCLE ( 'NONE', #44748, 0.08090551181102362266 ) ;
#26483=FACE_OUTER_BOUND ( 'NONE', #33883, .T. ) ;
#26514=ORIENTED_EDGE ( 'NONE', *, *, #42513, .T. ) ;
#26516=ORIENTED_EDGE ( 'NONE', *, *, #25159, .T. ) ;
#26520=CARTESIAN_POINT ( 'NONE',  ( 0.3906197235759846786, -3.032960542342102697E-32, 0.09842519685039370636 ) ) ;
#26540=FACE_OUTER_BOUND ( 'NONE', #7375, .T. ) ;
#26556=ORIENTED_EDGE ( 'NONE', *, *, #37009, .F. ) ;
#26585=DIRECTION ( 'NONE',  ( 0.5735764363510447161, -0.8191520442889925757, 1.003171929053525486E-16 ) ) ;
#26591=DIRECTION ( 'NONE',  ( -1.000000000000000000, 0.000000000000000000, 0.000000000000000000 ) ) ;
#26601=VERTEX_POINT ( 'NONE', #6219 ) ;
#26603=DIRECTION ( 'NONE',  ( 0.000000000000000000, -1.000000000000000000, 0.000000000000000000 ) ) ;
#26644=FACE_OUTER_BOUND ( 'NONE', #22239, .T. ) ;
#26658=DIRECTION ( 'NONE',  ( -1.000000000000000000, 0.000000000000000000, 0.000000000000000000 ) ) ;
#26660=CARTESIAN_POINT ( 'NONE',  ( 0.1602931993194444682, -0.1591122789105269553, 0.000000000000000000 ) ) ;
#26671=CARTESIAN_POINT ( 'NONE',  ( 0.1618536817989107701, 0.1553100982367987826, -0.01202753685181061002 ) ) ;
#26676=VECTOR ( 'NONE', #26305, 39.37007874015748143 ) ;
#26678=ORIENTED_EDGE ( 'NONE', *, *, #41245, .T. ) ;
#26708=CARTESIAN_POINT ( 'NONE',  ( 0.4151545546392377273, 1.205361022782824954E-17, -0.09842519685039370636 ) ) ;
#26716=DIRECTION ( 'NONE',  ( 1.000000000000000000, 0.000000000000000000, 0.000000000000000000 ) ) ;
#26726=ORIENTED_EDGE ( 'NONE', *, *, #16678, .F. ) ;
#26743=EDGE_CURVE ( 'NONE', #27963, #20645, #43828, .T. ) ;
#26786=AXIS2_PLACEMENT_3D ( 'NONE', #15890, #15182, #44148 ) ;
#26804=EDGE_CURVE ( 'NONE', #29608, #26427, #35817, .T. ) ;
#26817=CARTESIAN_POINT ( 'NONE',  ( 0.1617601974678946619, -0.07970883846569555564, 0.1380527197741285850 ) ) ;
#26849=EDGE_LOOP ( 'NONE', ( #15963, #44082, #47102 ) ) ;
#26870=ORIENTED_EDGE ( 'NONE', *, *, #13885, .F. ) ;
#26878=DIRECTION ( 'NONE',  ( -1.000000000000000000, 0.000000000000000000, 0.000000000000000000 ) ) ;
#26882=DIRECTION ( 'NONE',  ( 1.000000000000000000, 0.000000000000000000, 0.000000000000000000 ) ) ;
#26885=DIRECTION ( 'NONE',  ( -1.000000000000000000, 0.000000000000000000, 0.000000000000000000 ) ) ;
#26886=CARTESIAN_POINT ( 'NONE',  ( -6.669550765781891660E-19, 0.1126122229446088890, 0.08054045948776612784 ) ) ;
#26901=EDGE_CURVE ( 'NONE', #19079, #22837, #11491, .T. ) ;
#26909=CYLINDRICAL_SURFACE ( 'NONE', #26786, 0.09842519685039370636 ) ;
#26933=CARTESIAN_POINT ( 'NONE',  ( 0.003857550520879598089, -0.09763768210237290524, -0.1064941629723520911 ) ) ;
#26944=DIRECTION ( 'NONE',  ( -1.000000000000000000, 0.000000000000000000, 0.000000000000000000 ) ) ;
#26950=CIRCLE ( 'NONE', #12421, 0.08090551181102362266 ) ;
#26978=EDGE_CURVE ( 'NONE', #7386, #26132, #31376, .T. ) ;
#26987=AXIS2_PLACEMENT_3D ( 'NONE', #39804, #46768, #44118 ) ;
#26999=AXIS2_PLACEMENT_3D ( 'NONE', #46079, #2002, #13281 ) ;
#27017=CARTESIAN_POINT ( 'NONE',  ( 0.5057057357416000487, -3.032960542342102697E-32, 0.09842519685039370636 ) ) ;
#27044=CARTESIAN_POINT ( 'NONE',  ( 0.4755220087074803481, -0.09842519685039370636, 1.205361022782828805E-17 ) ) ;
#27054=ORIENTED_EDGE ( 'NONE', *, *, #36697, .F. ) ;
#27064=CARTESIAN_POINT ( 'NONE',  ( 0.000000000000000000, 1.205361022782826802E-17, -0.09842519685039370636 ) ) ;
#27077=DIRECTION ( 'NONE',  ( 0.000000000000000000, -1.000000000000000000, 0.000000000000000000 ) ) ;
#27078=DIRECTION ( 'NONE',  ( 0.000000000000000000, -1.000000000000000000, 0.000000000000000000 ) ) ;
#27081=FACE_OUTER_BOUND ( 'NONE', #45358, .T. ) ;
#27088=DIRECTION ( 'NONE',  ( -1.000000000000000000, 0.000000000000000000, 0.000000000000000000 ) ) ;
#27093=CARTESIAN_POINT ( 'NONE',  ( 0.1637370714319410780, 0.07819377357278597951, -0.1401549625175002034 ) ) ;
#27115=CIRCLE ( 'NONE', #21740, 0.09842519685039370636 ) ;
#27142=LINE ( 'NONE', #31196, #13231 ) ;
#27143=DIRECTION ( 'NONE',  ( 0.000000000000000000, 0.000000000000000000, 1.000000000000000000 ) ) ;
#27178=DIRECTION ( 'NONE',  ( -0.5735764363510518216, -0.8191520442889876907, 0.000000000000000000 ) ) ;
#27188=DIRECTION ( 'NONE',  ( 0.000000000000000000, -1.000000000000000000, 0.000000000000000000 ) ) ;
#27223=VERTEX_POINT ( 'NONE', #46190 ) ;
#27225=ORIENTED_EDGE ( 'NONE', *, *, #35720, .T. ) ;
#27233=DIRECTION ( 'NONE',  ( 1.000000000000000000, 0.000000000000000000, 0.000000000000000000 ) ) ;
#27238=ORIENTED_EDGE ( 'NONE', *, *, #30395, .F. ) ;
#27243=ADVANCED_FACE ( 'NONE', ( #21497 ), #24369, .T. ) ;
#27253=CYLINDRICAL_SURFACE ( 'NONE', #13789, 0.09842519685039370636 ) ;
#27270=DIRECTION ( 'NONE',  ( 0.000000000000000000, -1.000000000000000000, 0.000000000000000000 ) ) ;
#27288=CYLINDRICAL_SURFACE ( 'NONE', #33742, 0.09842519685039370636 ) ;
#27307=PLANE ( 'NONE',  #22475 ) ;
#27322=DIRECTION ( 'NONE',  ( 0.000000000000000000, 0.000000000000000000, 1.000000000000000000 ) ) ;
#27324=CARTESIAN_POINT ( 'NONE',  ( 0.3246033735368759610, -0.09842519685039370636, 1.205361022782828805E-17 ) ) ;
#27327=ORIENTED_EDGE ( 'NONE', *, *, #8633, .F. ) ;
#27332=CARTESIAN_POINT ( 'NONE',  ( 0.000000000000000000, 0.000000000000000000, 0.000000000000000000 ) ) ;
#27333=B_SPLINE_CURVE_WITH_KNOTS ( 'NONE', 3,
 ( #17915, #10266, #21504, #2810, #24642, #42811, #25363, #39945, #20564, #35673, #17441, #32569 ),
 .UNSPECIFIED., .F., .F.,
 ( 4, 2, 2, 2, 2, 4 ),
 ( 0.000000000000000000, 0.2499999999999998335, 0.3749999999999997780, 0.4374999999999997224, 0.4999999999999996669, 1.000000000000000000 ),
 .UNSPECIFIED. ) ;
#27338=DIRECTION ( 'NONE',  ( 0.5735764363510447161, -0.8191520442889925757, 1.003171929053525486E-16 ) ) ;
#27343=ORIENTED_EDGE ( 'NONE', *, *, #1012, .F. ) ;
#27383=FACE_OUTER_BOUND ( 'NONE', #28400, .T. ) ;
#27394=DIRECTION ( 'NONE',  ( -1.000000000000000000, 0.000000000000000000, 0.000000000000000000 ) ) ;
#27419=AXIS2_PLACEMENT_3D ( 'NONE', #39066, #27394, #13675 ) ;
#27421=EDGE_CURVE ( 'NONE', #18854, #33098, #22441, .T. ) ;
#27451=ORIENTED_EDGE ( 'NONE', *, *, #26901, .F. ) ;
#27469=ORIENTED_EDGE ( 'NONE', *, *, #12247, .T. ) ;
#27475=ORIENTED_EDGE ( 'NONE', *, *, #12527, .T. ) ;
#27486=EDGE_CURVE ( 'NONE', #11723, #14042, #3537, .T. ) ;
#27496=CARTESIAN_POINT ( 'NONE',  ( 0.1638066838320702268, -0.08057055941993987447, -0.1395522756397764574 ) ) ;
#27506=DIRECTION ( 'NONE',  ( -1.000000000000000000, 0.000000000000000000, 0.000000000000000000 ) ) ;
#27512=DIRECTION ( 'NONE',  ( 0.3420201433256624401, 1.150791560227853721E-16, 0.9396926207859106484 ) ) ;
#27513=AXIS2_PLACEMENT_3D ( 'NONE', #5593, #33677, #12336 ) ;
#27515=DIRECTION ( 'NONE',  ( -0.000000000000000000, 0.8660254037844384856, 0.5000000000000003331 ) ) ;
#27533=ORIENTED_EDGE ( 'NONE', *, *, #39094, .F. ) ;
#27541=CIRCLE ( 'NONE', #45095, 0.08090551181102362266 ) ;
#27542=CARTESIAN_POINT ( 'NONE',  ( 0.1633669211492204676, -0.08028893826450952953, 0.1390634969805222276 ) ) ;
#27553=FACE_OUTER_BOUND ( 'NONE', #8627, .T. ) ;
#27554=CYLINDRICAL_SURFACE ( 'NONE', #2501, 0.09842519685039370636 ) ;
#27555=AXIS2_PLACEMENT_3D ( 'NONE', #31279, #35340, #2482 ) ;
#27560=CYLINDRICAL_SURFACE ( 'NONE', #10947, 0.09842519685039370636 ) ;
#27572=LINE ( 'NONE', #34495, #13016 ) ;
#27586=ADVANCED_FACE ( 'NONE', ( #29692 ), #35856, .T. ) ;
#27600=VERTEX_POINT ( 'NONE', #31311 ) ;
#27604=CARTESIAN_POINT ( 'NONE',  ( 0.2519685039370078705, -0.08090551181102362266, 0.000000000000000000 ) ) ;
#27611=CARTESIAN_POINT ( 'NONE',  ( 0.004280036809617362818, 0.09642780928091415626, 0.1085877958707450186 ) ) ;
#27623=EDGE_LOOP ( 'NONE', ( #34280, #21169, #44109, #32156, #8118 ) ) ;
#27624=VERTEX_POINT ( 'NONE', #27017 ) ;
#27626=CARTESIAN_POINT ( 'NONE',  ( 0.3302522695077432791, 4.466152701071653354E-17, 0.000000000000000000 ) ) ;
#27663=CARTESIAN_POINT ( 'NONE',  ( 0.2821522309711287368, -0.08090551181102362266, 1.098083891755157578E-17 ) ) ;
#27666=DIRECTION ( 'NONE',  ( -1.000000000000000000, 0.000000000000000000, 0.000000000000000000 ) ) ;
#27674=FACE_OUTER_BOUND ( 'NONE', #18983, .T. ) ;
#27675=EDGE_LOOP ( 'NONE', ( #15655, #23291, #7196, #26514, #24784, #37505 ) ) ;
#27682=VECTOR ( 'NONE', #12690, 39.37007874015748143 ) ;
#27697=DIRECTION ( 'NONE',  ( -1.000000000000000000, 0.000000000000000000, 0.000000000000000000 ) ) ;
#27712=VERTEX_POINT ( 'NONE', #4932 ) ;
#27719=AXIS2_PLACEMENT_3D ( 'NONE', #28108, #42668, #16822 ) ;
#27748=CARTESIAN_POINT ( 'NONE',  ( 0.005686768416161533217, -0.1458881524272479802, 0.02291217744961116659 ) ) ;
#27753=CARTESIAN_POINT ( 'NONE',  ( 0.1822895153388602307, 2.589602477342551251E-17, 0.2114570894355444486 ) ) ;
#27769=CARTESIAN_POINT ( 'NONE',  ( -1.003767390250174765E-17, 0.006751761263662639685, -0.1377952755905511861 ) ) ;
#27774=DIRECTION ( 'NONE',  ( 0.000000000000000000, 0.000000000000000000, 1.000000000000000000 ) ) ;
#27792=ORIENTED_EDGE ( 'NONE', *, *, #24514, .T. ) ;
#27815=CARTESIAN_POINT ( 'NONE',  ( 0.1527640389977631963, 0.1337207259432474371, -0.04397945982240433066 ) ) ;
#27834=CIRCLE ( 'NONE', #45394, 0.09842519685039370636 ) ;
#27885=CARTESIAN_POINT ( 'NONE',  ( 0.1644020957507539848, -0.08115590401245571794, -0.1405661490837558925 ) ) ;
#27894=EDGE_CURVE ( 'NONE', #27975, #5683, #29780, .T. ) ;
#27902=FACE_OUTER_BOUND ( 'NONE', #5566, .T. ) ;
#27917=EDGE_LOOP ( 'NONE', ( #35350, #12064, #34170, #41133, #17352, #44804 ) ) ;
#27926=ORIENTED_EDGE ( 'NONE', *, *, #7094, .F. ) ;
#27963=VERTEX_POINT ( 'NONE', #35828 ) ;
#27975=VERTEX_POINT ( 'NONE', #42299 ) ;
#27986=CARTESIAN_POINT ( 'NONE',  ( 0.01230737760510395781, 0.07955613945526338049, -0.1377952755905511861 ) ) ;
#27991=ORIENTED_EDGE ( 'NONE', *, *, #38229, .F. ) ;
#27992=LINE ( 'NONE', #38975, #40147 ) ;
#27997=AXIS2_PLACEMENT_3D ( 'NONE', #16234, #9022, #34921 ) ;
#28009=AXIS2_PLACEMENT_3D ( 'NONE', #41072, #18818, #26029 ) ;
#28010=CYLINDRICAL_SURFACE ( 'NONE', #3171, 0.09842519685039370636 ) ;
#28019=DIRECTION ( 'NONE',  ( -1.000000000000000000, 0.000000000000000000, 0.000000000000000000 ) ) ;
#28025=CARTESIAN_POINT ( 'NONE',  ( 0.000000000000000000, 0.1193342091828950846, -0.06889763779527559306 ) ) ;
#28034=CARTESIAN_POINT ( 'NONE',  ( 0.1637325577037128943, 0.1604625459914952312, 0.002338731188024917394 ) ) ;
#28035=ORIENTED_EDGE ( 'NONE', *, *, #14309, .F. ) ;
#28042=CONICAL_SURFACE ( 'NONE', #27997, 0.09842519685039370636, 0.9599310885968824758 ) ;
#28048=CARTESIAN_POINT ( 'NONE',  ( 0.2944196465027555387, 0.09842519685039370636, 0.000000000000000000 ) ) ;
#28056=EDGE_CURVE ( 'NONE', #12116, #27624, #2282, .T. ) ;
#28059=ORIENTED_EDGE ( 'NONE', *, *, #43925, .F. ) ;
#28067=EDGE_CURVE ( 'NONE', #27600, #15794, #45031, .T. ) ;
#28071=CARTESIAN_POINT ( 'NONE',  ( 0.1588779435336272472, -0.1435649425735359141, -0.03225083113269787416 ) ) ;
#28100=EDGE_CURVE ( 'NONE', #16297, #9744, #14734, .T. ) ;
#28106=VERTEX_POINT ( 'NONE', #40572 ) ;
#28108=CARTESIAN_POINT ( 'NONE',  ( 0.4755220087074803481, 4.766607801171850497E-17, 0.000000000000000000 ) ) ;
#28121=DIRECTION ( 'NONE',  ( -1.000000000000000000, 0.000000000000000000, 0.000000000000000000 ) ) ;
#28126=CARTESIAN_POINT ( 'NONE',  ( 0.1629747151065570054, 0.1601846959074193222, 3.793325934747440125E-08 ) ) ;
#28156=CONICAL_SURFACE ( 'NONE', #40359, 0.09842519685039370636, 0.9599310885968824758 ) ;
#28157=ADVANCED_FACE ( 'NONE', ( #29864 ), #33209, .F. ) ;
#28198=CARTESIAN_POINT ( 'NONE',  ( 0.1588891437628947301, -0.04395497937029503588, -0.1404564352527339355 ) ) ;
#28200=CARTESIAN_POINT ( 'NONE',  ( 0.1644020957507539848, -0.1623118080249112138, 7.560884646099310910E-18 ) ) ;
#28212=CARTESIAN_POINT ( 'NONE',  ( 0.4453382816733590377, 4.766607801171850497E-17, 0.000000000000000000 ) ) ;
#28217=FACE_OUTER_BOUND ( 'NONE', #9856, .T. ) ;
#28220=DIRECTION ( 'NONE',  ( -1.000000000000000000, 0.000000000000000000, 0.000000000000000000 ) ) ;
#28223=DIRECTION ( 'NONE',  ( -1.000000000000000000, 0.000000000000000000, 0.000000000000000000 ) ) ;
#28237=DIRECTION ( 'NONE',  ( 1.000000000000000000, 0.000000000000000000, 0.000000000000000000 ) ) ;
#28251=DIRECTION ( 'NONE',  ( 0.000000000000000000, 1.000000000000000000, 0.000000000000000000 ) ) ;
#28262=ORIENTED_EDGE ( 'NONE', *, *, #35015, .F. ) ;
#28266=EDGE_CURVE ( 'NONE', #34889, #4911, #17405, .T. ) ;
#28286=( CONVERSION_BASED_UNIT ( 'INCH', #24441 ) LENGTH_UNIT ( ) NAMED_UNIT ( #35696 ) ) ;
#28303=CIRCLE ( 'NONE', #33656, 0.09842519685039370636 ) ;
#28315=AXIS2_PLACEMENT_3D ( 'NONE', #8668, #22345, #37678 ) ;
#28325=EDGE_LOOP ( 'NONE', ( #41750, #44186, #20879, #41519, #40487, #31368 ) ) ;
#28326=DIRECTION ( 'NONE',  ( 1.000000000000000000, 0.000000000000000000, 0.000000000000000000 ) ) ;
#28388=VECTOR ( 'NONE', #2904, 39.37007874015748143 ) ;
#28400=EDGE_LOOP ( 'NONE', ( #19694, #18613, #16505, #11062, #27054 ) ) ;
#28418=CIRCLE ( 'NONE', #25339, 0.09842519685039370636 ) ;
#28419=CARTESIAN_POINT ( 'NONE',  ( 0.1602931993194442739, -0.07955613945526357478, -0.1377952755905511861 ) ) ;
#28428=CARTESIAN_POINT ( 'NONE',  ( 0.6141732283464567121, 1.098083891755155421E-17, -0.08090551181102362266 ) ) ;
#28443=ORIENTED_EDGE ( 'NONE', *, *, #35185, .T. ) ;
#28454=CARTESIAN_POINT ( 'NONE',  ( 0.5839895013123354017, -0.08090551181102362266, 0.000000000000000000 ) ) ;
#28458=CARTESIAN_POINT ( 'NONE',  ( 0.3246033735368759610, 0.09842519685039370636, 0.000000000000000000 ) ) ;
#28462=AXIS2_PLACEMENT_3D ( 'NONE', #45405, #23146, #11899 ) ;
#28471=CARTESIAN_POINT ( 'NONE',  ( 0.3123359580052492146, -0.08090551181102362266, 0.000000000000000000 ) ) ;
#28549=EDGE_CURVE ( 'NONE', #27712, #31223, #37412, .T. ) ;
#28604=EDGE_CURVE ( 'NONE', #30249, #27223, #45818, .T. ) ;
#28626=ORIENTED_EDGE ( 'NONE', *, *, #42258, .T. ) ;
#28632=VECTOR ( 'NONE', #22031, 39.37007874015748854 ) ;
#28645=DIRECTION ( 'NONE',  ( -1.000000000000000000, 0.000000000000000000, 0.000000000000000000 ) ) ;
#28646=LINE ( 'NONE', #25516, #33639 ) ;
#28652=EDGE_CURVE ( 'NONE', #42873, #29582, #22131, .T. ) ;
#28653=CARTESIAN_POINT ( 'NONE',  ( 0.008396861977716250230, -0.1523390671600990398, -0.01173154688214765075 ) ) ;
#28666=CARTESIAN_POINT ( 'NONE',  ( 0.1563802477479413477, 0.02735756446292999730, 0.1403846664728047311 ) ) ;
#28678=AXIS2_PLACEMENT_3D ( 'NONE', #9362, #26878, #12737 ) ;
#28688=CARTESIAN_POINT ( 'NONE',  ( 0.1587185860253795822, -0.04237460976005667790, -0.1404529029258574369 ) ) ;
#28707=VECTOR ( 'NONE', #30300, 39.37007874015748854 ) ;
#28718=CARTESIAN_POINT ( 'NONE',  ( 0.001099666138475116151, -0.02328811444560369148, -0.1377843663819193765 ) ) ;
#28742=CARTESIAN_POINT ( 'NONE',  ( 0.0005737749932732162661, 0.1108949133173907642, -0.08352002191776017326 ) ) ;
#28805=ORIENTED_EDGE ( 'NONE', *, *, #42705, .T. ) ;
#28814=CARTESIAN_POINT ( 'NONE',  ( 0.0003553830333942847560, -0.1126092284109665720, 0.08054791328663142569 ) ) ;
#28828=ORIENTED_EDGE ( 'NONE', *, *, #11546, .T. ) ;
#28832=ADVANCED_FACE ( 'NONE', ( #25937 ), #29059, .T. ) ;
#28872=LINE ( 'NONE', #43430, #38124 ) ;
#28916=ORIENTED_EDGE ( 'NONE', *, *, #41907, .F. ) ;
#28921=VERTEX_POINT ( 'NONE', #11092 ) ;
#28936=ADVANCED_FACE ( 'NONE', ( #4106 ), #12560, .F. ) ;
#28955=FACE_OUTER_BOUND ( 'NONE', #24986, .T. ) ;
#28970=VERTEX_POINT ( 'NONE', #4324 ) ;
#28981=ORIENTED_EDGE ( 'NONE', *, *, #43046, .F. ) ;
#28999=VECTOR ( 'NONE', #31172, 39.37007874015748854 ) ;
#29010=CARTESIAN_POINT ( 'NONE',  ( 0.2204724409448818867, 0.1591122789105269553, 0.000000000000000000 ) ) ;
#29035=EDGE_CURVE ( 'NONE', #3818, #30831, #16105, .T. ) ;
#29059=CONICAL_SURFACE ( 'NONE', #40483, 0.08090551181102362266, 0.9599310885968742602 ) ;
#29067=DIRECTION ( 'NONE',  ( 0.000000000000000000, -1.000000000000000000, 0.000000000000000000 ) ) ;
#29078=CARTESIAN_POINT ( 'NONE',  ( 0.1630380177254369123, -0.1602364199967901970, 6.745834889254991641E-08 ) ) ;
#29094=CARTESIAN_POINT ( 'NONE',  ( 0.4330708661417322913, 4.616380251121755931E-17, 0.000000000000000000 ) ) ;
#29097=ORIENTED_EDGE ( 'NONE', *, *, #39795, .F. ) ;
#29102=AXIS2_PLACEMENT_3D ( 'NONE', #1955, #2185, #41943 ) ;
#29107=EDGE_CURVE ( 'NONE', #13283, #21269, #35919, .T. ) ;
#29147=CARTESIAN_POINT ( 'NONE',  ( 0.5538057742782149795, 0.08090551181102362266, 0.000000000000000000 ) ) ;
#29156=CARTESIAN_POINT ( 'NONE',  ( 0.1555687797274980522, 0.05303742630350882087, -0.1377952755905511861 ) ) ;
#29167=ORIENTED_EDGE ( 'NONE', *, *, #40139, .T. ) ;
#29176=DIRECTION ( 'NONE',  ( 0.000000000000000000, -1.000000000000000000, 0.000000000000000000 ) ) ;
#29205=EDGE_LOOP ( 'NONE', ( #5679, #1793, #37304, #27792, #28035 ) ) ;
#29214=AXIS2_PLACEMENT_3D ( 'NONE', #27626, #38136, #12279 ) ;
#29238=EDGE_CURVE ( 'NONE', #38091, #40174, #41248, .T. ) ;
#29250=AXIS2_PLACEMENT_3D ( 'NONE', #10219, #10461, #7329 ) ;
#29272=CARTESIAN_POINT ( 'NONE',  ( 0.000000000000000000, 0.000000000000000000, 0.09842519685039370636 ) ) ;
#29276=CIRCLE ( 'NONE', #8552, 0.08090551181102362266 ) ;
#29277=AXIS2_PLACEMENT_3D ( 'NONE', #36066, #3223, #17854 ) ;
#29308=CIRCLE ( 'NONE', #26987, 0.09842519685039370636 ) ;
#29322=AXIS2_PLACEMENT_3D ( 'NONE', #40046, #22559, #40282 ) ;
#29330=CARTESIAN_POINT ( 'NONE',  ( 0.4755220087074803481, 4.766607801171850497E-17, 0.000000000000000000 ) ) ;
#29340=EDGE_CURVE ( 'NONE', #23379, #40935, #27541, .T. ) ;
#29353=CARTESIAN_POINT ( 'NONE',  ( 0.1564636162838602407, -0.1358284121151820956, 0.04551197418441456366 ) ) ;
#29360=ORIENTED_EDGE ( 'NONE', *, *, #6873, .F. ) ;
#29369=CARTESIAN_POINT ( 'NONE',  ( 0.1587072800413000528, 0.1005018865549645452, -0.1068311739851162540 ) ) ;
#29388=CIRCLE ( 'NONE', #38524, 0.09842519685039370636 ) ;
#29400=CARTESIAN_POINT ( 'NONE',  ( 0.1498753904841984286, -0.1193342091828950846, 0.06889763779527559306 ) ) ;
#29404=AXIS2_PLACEMENT_3D ( 'NONE', #39521, #18206, #14384 ) ;
#29427=DIRECTION ( 'NONE',  ( 0.000000000000000000, -1.000000000000000000, 0.000000000000000000 ) ) ;
#29446=CARTESIAN_POINT ( 'NONE',  ( 0.3849708276051176936, 4.766607801171850497E-17, 0.000000000000000000 ) ) ;
#29461=DIRECTION ( 'NONE',  ( 1.000000000000000000, 0.000000000000000000, 0.000000000000000000 ) ) ;
#29462=DIRECTION ( 'NONE',  ( 0.000000000000000000, -1.000000000000000000, 0.000000000000000000 ) ) ;
#29468=CARTESIAN_POINT ( 'NONE',  ( 0.1629747151064184774, 0.08009231510251769992, 0.1387240349198020917 ) ) ;
#29473=EDGE_CURVE ( 'NONE', #5973, #18563, #15273, .T. ) ;
#29475=ORIENTED_EDGE ( 'NONE', *, *, #4758, .F. ) ;
#29508=LINE ( 'NONE', #29272, #39288 ) ;
#29514=CARTESIAN_POINT ( 'NONE',  ( 0.000000000000000000, 0.000000000000000000, 0.000000000000000000 ) ) ;
#29519=DIRECTION ( 'NONE',  ( -1.000000000000000000, 0.000000000000000000, 0.000000000000000000 ) ) ;
#29520=ORIENTED_EDGE ( 'NONE', *, *, #28067, .T. ) ;
#29529=VERTEX_POINT ( 'NONE', #25661 ) ;
#29564=CYLINDRICAL_SURFACE ( 'NONE', #1020, 0.09842519685039370636 ) ;
#29582=VERTEX_POINT ( 'NONE', #47213 ) ;
#29599=DIRECTION ( 'NONE',  ( 0.000000000000000000, -1.000000000000000000, 0.000000000000000000 ) ) ;
#29608=VERTEX_POINT ( 'NONE', #17499 ) ;
#29624=CARTESIAN_POINT ( 'NONE',  ( 0.005686768416281180565, -0.09278660394087787089, -0.1148867573887376176 ) ) ;
#29655=CARTESIAN_POINT ( 'NONE',  ( 0.1582120475477730714, -0.1402876732178527375, 0.03788922412836724651 ) ) ;
#29664=ORIENTED_EDGE ( 'NONE', *, *, #5136, .F. ) ;
#29670=EDGE_CURVE ( 'NONE', #3818, #33098, #21372, .T. ) ;
#29676=EDGE_LOOP ( 'NONE', ( #7944, #20405, #28443, #5107, #8194, #21316 ) ) ;
#29679=CARTESIAN_POINT ( 'NONE',  ( -6.002595689203704805E-19, -0.01343938916650502628, 0.1377952755905511861 ) ) ;
#29692=FACE_OUTER_BOUND ( 'NONE', #47095, .T. ) ;
#29693=CIRCLE ( 'NONE', #17386, 0.09842519685039370636 ) ;
#29696=CARTESIAN_POINT ( 'NONE',  ( 0.1588150004738740628, 0.09138854459950905562, 0.1173009487050022392 ) ) ;
#29720=DIRECTION ( 'NONE',  ( 0.000000000000000000, -1.000000000000000000, 0.000000000000000000 ) ) ;
#29725=ORIENTED_EDGE ( 'NONE', *, *, #27894, .T. ) ;
#29747=CARTESIAN_POINT ( 'NONE',  ( 0.1588147753335400203, 0.05589013274906071138, -0.1377952755905511861 ) ) ;
#29748=ORIENTED_EDGE ( 'NONE', *, *, #12905, .F. ) ;
#29780=CIRCLE ( 'NONE', #624, 0.09842519685039370636 ) ;
#29782=ORIENTED_EDGE ( 'NONE', *, *, #4574, .T. ) ;
#29788=DIRECTION ( 'NONE',  ( -1.000000000000000000, 0.000000000000000000, 0.000000000000000000 ) ) ;
#29800=EDGE_CURVE ( 'NONE', #22780, #17392, #28303, .T. ) ;
#29803=CARTESIAN_POINT ( 'NONE',  ( 0.1563805530828635826, -0.1078949188770171180, 0.09388986751132855080 ) ) ;
#29805=CARTESIAN_POINT ( 'NONE',  ( 0.1573602050224763571, 0.1080344010929730203, 0.09369282772931890324 ) ) ;
#29814=DIRECTION ( 'NONE',  ( -1.000000000000000000, 0.000000000000000000, 0.000000000000000000 ) ) ;
#29824=AXIS2_PLACEMENT_3D ( 'NONE', #28212, #20987, #36811 ) ;
#29859=VECTOR ( 'NONE', #14814, 39.37007874015748143 ) ;
#29863=LINE ( 'NONE', #22861, #47288 ) ;
#29864=FACE_OUTER_BOUND ( 'NONE', #8481, .T. ) ;
#29885=VECTOR ( 'NONE', #27512, 39.37007874015748143 ) ;
#29901=CARTESIAN_POINT ( 'NONE',  ( 0.000000000000000000, 0.000000000000000000, 0.000000000000000000 ) ) ;
#29914=ADVANCED_FACE ( 'NONE', ( #23710 ), #38286, .F. ) ;
#29916=EDGE_CURVE ( 'NONE', #19636, #15821, #27572, .T. ) ;
#29943=CARTESIAN_POINT ( 'NONE',  ( 0.1564216623530370331, 8.908831420875236139E-13, 0.1403857474672218497 ) ) ;
#29950=VECTOR ( 'NONE', #2288, 39.37007874015748143 ) ;
#29966=DIRECTION ( 'NONE',  ( -1.000000000000000000, 0.000000000000000000, 0.000000000000000000 ) ) ;
#29971=CARTESIAN_POINT ( 'NONE',  ( 0.000000000000000000, 0.1193342091828950846, 0.06889763779527559306 ) ) ;
#29977=CARTESIAN_POINT ( 'NONE',  ( 0.4151545546392377273, 4.766607801171850497E-17, 0.000000000000000000 ) ) ;
#29978=CONICAL_SURFACE ( 'NONE', #42122, 0.09842519685039370636, 0.9599310885968824758 ) ;
#30001=CARTESIAN_POINT ( 'NONE',  ( 0.4208034506101054895, 4.466152701071653354E-17, 0.000000000000000000 ) ) ;
#30005=FACE_OUTER_BOUND ( 'NONE', #13662, .T. ) ;
#30008=VERTEX_POINT ( 'NONE', #2125 ) ;
#30016=AXIS2_PLACEMENT_3D ( 'NONE', #783, #26944, #1031 ) ;
#30028=CARTESIAN_POINT ( 'NONE',  ( 0.3906197235759846786, 1.205361022782824954E-17, -0.09842519685039370636 ) ) ;
#30029=ADVANCED_FACE ( 'NONE', ( #2817 ), #41295, .T. ) ;
#30032=DIRECTION ( 'NONE',  ( -1.000000000000000000, 0.000000000000000000, 0.000000000000000000 ) ) ;
#30036=DIRECTION ( 'NONE',  ( 0.000000000000000000, -1.000000000000000000, 0.000000000000000000 ) ) ;
#30065=AXIS2_PLACEMENT_3D ( 'NONE', #44933, #8290, #1329 ) ;
#30084=CARTESIAN_POINT ( 'NONE',  ( 0.004280036809667321987, -0.09642780928087142656, -0.1085877958708996449 ) ) ;
#30086=( GEOMETRIC_REPRESENTATION_CONTEXT ( 3 ) GLOBAL_UNCERTAINTY_ASSIGNED_CONTEXT ( ( #17816 ) ) GLOBAL_UNIT_ASSIGNED_CONTEXT ( ( #28286, #26347, #25635 ) ) REPRESENTATION_CONTEXT ( 'NONE', 'WORKASPACE' ) ) ;
#30118=CIRCLE ( 'NONE', #9413, 0.09842519685039370636 ) ;
#30131=CARTESIAN_POINT ( 'NONE',  ( -9.744954730003541136E-18, 0.1260561954212529312, -0.05725481610266102556 ) ) ;
#30143=ADVANCED_FACE ( 'NONE', ( #32574 ), #25368, .T. ) ;
#30196=ORIENTED_EDGE ( 'NONE', *, *, #1308, .F. ) ;
#30201=FACE_OUTER_BOUND ( 'NONE', #31820, .T. ) ;
#30202=CARTESIAN_POINT ( 'NONE',  ( 0.2007874015748031815, 2.507150927388283472E-17, -0.2047244094488188948 ) ) ;
#30209=CARTESIAN_POINT ( 'NONE',  ( 0.5538057742782149795, 4.616380251121755931E-17, 0.000000000000000000 ) ) ;
#30212=CARTESIAN_POINT ( 'NONE',  ( 0.01230737760510134012, -0.07955613945526751607, -0.1377952755905511861 ) ) ;
#30249=VERTEX_POINT ( 'NONE', #40411 ) ;
#30255=CIRCLE ( 'NONE', #24100, 0.08090551181102362266 ) ;
#30300=DIRECTION ( 'NONE',  ( 0.5735764363510447161, -0.8191520442889925757, 1.003171929053525486E-16 ) ) ;
#30307=ORIENTED_EDGE ( 'NONE', *, *, #20386, .T. ) ;
#30352=FACE_OUTER_BOUND ( 'NONE', #14631, .T. ) ;
#30353=DIRECTION ( 'NONE',  ( -1.000000000000000000, 0.000000000000000000, 0.000000000000000000 ) ) ;
#30361=AXIS2_PLACEMENT_3D ( 'NONE', #13263, #35994, #16612 ) ;
#30367=CARTESIAN_POINT ( 'NONE',  ( 0.004280036809634069940, 0.1422536944055189378, -0.02921503453314187176 ) ) ;
#30368=DIRECTION ( 'NONE',  ( 0.000000000000000000, 1.000000000000000000, 0.000000000000000000 ) ) ;
#30371=ORIENTED_EDGE ( 'NONE', *, *, #42449, .F. ) ;
#30375=CARTESIAN_POINT ( 'NONE',  ( 0.2642359194686346169, 4.766607801171850497E-17, 0.000000000000000000 ) ) ;
#30384=DIRECTION ( 'NONE',  ( 0.000000000000000000, -1.000000000000000000, 0.000000000000000000 ) ) ;
#30395=EDGE_CURVE ( 'NONE', #30008, #34889, #10463, .T. ) ;
#30444=CARTESIAN_POINT ( 'NONE',  ( 0.1559663611957041174, 0.05603239795798645867, -0.1377952755905511861 ) ) ;
#30457=ORIENTED_EDGE ( 'NONE', *, *, #10564, .F. ) ;
#30492=EDGE_CURVE ( 'NONE', #42394, #26601, #37499, .T. ) ;
#30497=DIRECTION ( 'NONE',  ( 0.000000000000000000, -1.000000000000000000, 0.000000000000000000 ) ) ;
#30561=DIRECTION ( 'NONE',  ( 0.000000000000000000, 0.000000000000000000, 1.000000000000000000 ) ) ;
#30563=CARTESIAN_POINT ( 'NONE',  ( 0.2821522309711287368, -0.08090551181102362266, 0.000000000000000000 ) ) ;
#30575=DIRECTION ( 'NONE',  ( 0.000000000000000000, -1.000000000000000000, 0.000000000000000000 ) ) ;
#30584=EDGE_CURVE ( 'NONE', #28921, #9031, #34683, .T. ) ;
#30593=ORIENTED_EDGE ( 'NONE', *, *, #7370, .T. ) ;
#30595=AXIS2_PLACEMENT_3D ( 'NONE', #18756, #46810, #33182 ) ;
#30600=CARTESIAN_POINT ( 'NONE',  ( 0.5236220472440944462, 0.08090551181102362266, 9.908067607274841931E-18 ) ) ;
#30633=CIRCLE ( 'NONE', #4545, 0.08090551181102362266 ) ;
#30644=CARTESIAN_POINT ( 'NONE',  ( 0.5113546317124669782, 4.466152701071653354E-17, 0.000000000000000000 ) ) ;
#30657=CARTESIAN_POINT ( 'NONE',  ( 0.2944196465027555387, 4.766607801171850497E-17, 0.000000000000000000 ) ) ;
#30678=ORIENTED_EDGE ( 'NONE', *, *, #25831, .T. ) ;
#30683=DIRECTION ( 'NONE',  ( 0.000000000000000000, -1.000000000000000000, 0.000000000000000000 ) ) ;
#30719=AXIS2_PLACEMENT_3D ( 'NONE', #20737, #35378, #2522 ) ;
#30725=CARTESIAN_POINT ( 'NONE',  ( 0.1565984635743035980, -0.01350052470311071708, 0.1403812994535005576 ) ) ;
#30763=EDGE_CURVE ( 'NONE', #42760, #5875, #20707, .T. ) ;
#30764=CARTESIAN_POINT ( 'NONE',  ( 0.1645805237892204731, -0.1627998762483228723, 0.0008383936782243070051 ) ) ;
#30771=DIRECTION ( 'NONE',  ( -1.000000000000000000, 0.000000000000000000, 0.000000000000000000 ) ) ;
#30775=CARTESIAN_POINT ( 'NONE',  ( 0.5358894627757212481, -0.09842519685039370636, 1.205361022782828805E-17 ) ) ;
#30804=ORIENTED_EDGE ( 'NONE', *, *, #15725, .F. ) ;
#30805=DIRECTION ( 'NONE',  ( -1.000000000000000000, 0.000000000000000000, 0.000000000000000000 ) ) ;
#30807=ORIENTED_EDGE ( 'NONE', *, *, #22550, .T. ) ;
#30816=ORIENTED_EDGE ( 'NONE', *, *, #1614, .F. ) ;
#30831=VERTEX_POINT ( 'NONE', #32272 ) ;
#30862=CARTESIAN_POINT ( 'NONE',  ( 0.5538057742782149795, 0.08090551181102362266, 9.908067607274841931E-18 ) ) ;
#30881=DIRECTION ( 'NONE',  ( -0.5735764363510518216, 0.8191520442889876907, 1.003171929053519693E-16 ) ) ;
#30895=AXIS2_PLACEMENT_3D ( 'NONE', #1361, #8558, #23192 ) ;
#30923=CARTESIAN_POINT ( 'NONE',  ( 0.1526809758745832635, 0.1055212057016139821, -0.09282246162998031291 ) ) ;
#30924=ORIENTED_EDGE ( 'NONE', *, *, #8384, .T. ) ;
#30929=AXIS2_PLACEMENT_3D ( 'NONE', #38821, #2383, #24443 ) ;
#30961=DIRECTION ( 'NONE',  ( 0.000000000000000000, -1.000000000000000000, 0.000000000000000000 ) ) ;
#30981=AXIS2_PLACEMENT_3D ( 'NONE', #21417, #32713, #9942 ) ;
#31012=CIRCLE ( 'NONE', #3423, 0.09842519685039370636 ) ;
#31018=AXIS2_PLACEMENT_3D ( 'NONE', #7102, #17887, #10236 ) ;
#31020=CARTESIAN_POINT ( 'NONE',  ( 0.2519685039370078705, -0.08090551181102362266, 1.098083891755157578E-17 ) ) ;
#31045=ORIENTED_EDGE ( 'NONE', *, *, #14961, .T. ) ;
#31078=ADVANCED_FACE ( 'NONE', ( #12531 ), #34496, .T. ) ;
#31112=VERTEX_POINT ( 'NONE', #43162 ) ;
#31116=FACE_OUTER_BOUND ( 'NONE', #9867, .T. ) ;
#31138=LINE ( 'NONE', #725, #10952 ) ;
#31145=DIRECTION ( 'NONE',  ( 0.000000000000000000, -1.000000000000000000, 0.000000000000000000 ) ) ;
#31149=LINE ( 'NONE', #2579, #37168 ) ;
#31172=DIRECTION ( 'NONE',  ( 0.5735764363510447161, 0.8191520442889925757, 0.000000000000000000 ) ) ;
#31177=ORIENTED_EDGE ( 'NONE', *, *, #41313, .F. ) ;
#31190=EDGE_CURVE ( 'NONE', #38091, #28106, #18655, .T. ) ;
#31196=CARTESIAN_POINT ( 'NONE',  ( 0.5236220472440944462, -0.08090551181102362266, 0.000000000000000000 ) ) ;
#31198=AXIS2_PLACEMENT_3D ( 'NONE', #15718, #30353, #30575 ) ;
#31223=VERTEX_POINT ( 'NONE', #31941 ) ;
#31243=DIRECTION ( 'NONE',  ( -1.000000000000000000, 0.000000000000000000, 0.000000000000000000 ) ) ;
#31252=ADVANCED_FACE ( 'NONE', ( #35763 ), #26076, .T. ) ;
#31274=DIRECTION ( 'NONE',  ( -1.000000000000000000, 0.000000000000000000, 0.000000000000000000 ) ) ;
#31279=CARTESIAN_POINT ( 'NONE',  ( 0.1822895153388602307, 0.000000000000000000, 0.000000000000000000 ) ) ;
#31311=CARTESIAN_POINT ( 'NONE',  ( 0.2944196465027555387, 1.205361022782824954E-17, -0.09842519685039370636 ) ) ;
#31333=ORIENTED_EDGE ( 'NONE', *, *, #24908, .F. ) ;
#31337=CARTESIAN_POINT ( 'NONE',  ( 0.002317772416624286781, 0.03366109551137453498, -0.1377956189922244779 ) ) ;
#31341=AXIS2_PLACEMENT_3D ( 'NONE', #45778, #17039, #24699 ) ;
#31359=ORIENTED_EDGE ( 'NONE', *, *, #46612, .F. ) ;
#31368=ORIENTED_EDGE ( 'NONE', *, *, #25015, .F. ) ;
#31375=AXIS2_PLACEMENT_3D ( 'NONE', #43317, #32087, #25372 ) ;
#31376=LINE ( 'NONE', #34253, #43460 ) ;
#31390=CARTESIAN_POINT ( 'NONE',  ( 0.000000000000000000, 0.000000000000000000, 0.000000000000000000 ) ) ;
#31395=ORIENTED_EDGE ( 'NONE', *, *, #26978, .T. ) ;
#31408=CARTESIAN_POINT ( 'NONE',  ( 0.5057057357416000487, -0.09842519685039370636, 1.205361022782828805E-17 ) ) ;
#31417=ADVANCED_FACE ( 'NONE', ( #27902 ), #43634, .T. ) ;
#31429=EDGE_LOOP ( 'NONE', ( #11839, #41213, #15955, #35481, #35890, #23371 ) ) ;
#31451=DIRECTION ( 'NONE',  ( -1.000000000000000000, 0.000000000000000000, 0.000000000000000000 ) ) ;
#31457=ORIENTED_EDGE ( 'NONE', *, *, #43557, .T. ) ;
#31464=LINE ( 'NONE', #23787, #16976 ) ;
#31478=CARTESIAN_POINT ( 'NONE',  ( 0.4509871776442260227, 0.09842519685039370636, 1.205361022782828805E-17 ) ) ;
#31481=CARTESIAN_POINT ( 'NONE',  ( 0.1617601974887943606, 0.1594115816221988724, 3.519129779734452560E-06 ) ) ;
#31494=FACE_OUTER_BOUND ( 'NONE', #6174, .T. ) ;
#31496=CIRCLE ( 'NONE', #30016, 0.08090551181102362266 ) ;
#31588=DIRECTION ( 'NONE',  ( -1.000000000000000000, 0.000000000000000000, 0.000000000000000000 ) ) ;
#31600=LINE ( 'NONE', #11140, #45387 ) ;
#31606=CARTESIAN_POINT ( 'NONE',  ( 0.4453382816733590377, 4.766607801171850497E-17, 0.000000000000000000 ) ) ;
#31614=ORIENTED_EDGE ( 'NONE', *, *, #9595, .F. ) ;
#31631=ORIENTED_EDGE ( 'NONE', *, *, #424, .T. ) ;
#31648=AXIS2_PLACEMENT_3D ( 'NONE', #25658, #47210, #22040 ) ;
#31651=VERTEX_POINT ( 'NONE', #45709 ) ;
#31681=ADVANCED_FACE ( 'NONE', ( #46191 ), #13090, .T. ) ;
#31697=ORIENTED_EDGE ( 'NONE', *, *, #17308, .T. ) ;
#31705=CONICAL_SURFACE ( 'NONE', #19431, 0.09842519685039370636, 0.9599310885968824758 ) ;
#31718=CARTESIAN_POINT ( 'NONE',  ( 0.1644020957507539848, 0.1623118080249112138, 1.367956046207553540E-19 ) ) ;
#31743=DIRECTION ( 'NONE',  ( 0.000000000000000000, 0.000000000000000000, 1.000000000000000000 ) ) ;
#31744=CARTESIAN_POINT ( 'NONE',  ( 0.3000685424736224127, 4.466152701071653354E-17, 0.000000000000000000 ) ) ;
#31761=CARTESIAN_POINT ( 'NONE',  ( 0.3547871005709968273, 4.766607801171850497E-17, 0.000000000000000000 ) ) ;
#31766=AXIS2_PLACEMENT_3D ( 'NONE', #31925, #28326, #5800 ) ;
#31781=CARTESIAN_POINT ( 'NONE',  ( 0.1631287777903855374, -0.08016275093080070524, -0.1388449280286157550 ) ) ;
#31814=CARTESIAN_POINT ( 'NONE',  ( 0.000000000000000000, 1.205361022782826802E-17, -0.09842519685039370636 ) ) ;
#31820=EDGE_LOOP ( 'NONE', ( #13345, #11391, #32537, #36299, #26726 ) ) ;
#31823=LINE ( 'NONE', #28471, #37882 ) ;
#31841=EDGE_LOOP ( 'NONE', ( #6144, #32025, #16426, #15830, #39308, #4601, #45400 ) ) ;
#31844=CARTESIAN_POINT ( 'NONE',  ( 0.6141732283464567121, 0.000000000000000000, 0.000000000000000000 ) ) ;
#31850=CARTESIAN_POINT ( 'NONE',  ( 0.005401850751909476230, 0.09279043093865825542, -0.1148724510413045297 ) ) ;
#31852=DIRECTION ( 'NONE',  ( -0.5735764363510518216, -0.8191520442889876907, 0.000000000000000000 ) ) ;
#31888=CARTESIAN_POINT ( 'NONE',  ( 0.000000000000000000, 0.000000000000000000, 0.09842519685039370636 ) ) ;
#31925=CARTESIAN_POINT ( 'NONE',  ( 0.000000000000000000, 0.000000000000000000, 0.000000000000000000 ) ) ;
#31941=CARTESIAN_POINT ( 'NONE',  ( 0.000000000000000000, -0.1193342091828949042, 0.06889763779527559306 ) ) ;
#31981=AXIS2_PLACEMENT_3D ( 'NONE', #40353, #11168, #44196 ) ;
#31995=EDGE_CURVE ( 'NONE', #46176, #4886, #36052, .T. ) ;
#32003=DIRECTION ( 'NONE',  ( 0.000000000000000000, -1.000000000000000000, 0.000000000000000000 ) ) ;
#32011=PLANE ( 'NONE',  #29277 ) ;
#32018=ORIENTED_EDGE ( 'NONE', *, *, #24367, .T. ) ;
#32025=ORIENTED_EDGE ( 'NONE', *, *, #30584, .T. ) ;
#32043=DIRECTION ( 'NONE',  ( -1.000000000000000000, 0.000000000000000000, 0.000000000000000000 ) ) ;
#32044=ORIENTED_EDGE ( 'NONE', *, *, #29107, .T. ) ;
#32066=CARTESIAN_POINT ( 'NONE',  ( 0.000000000000000000, 0.000000000000000000, 0.000000000000000000 ) ) ;
#32069=LINE ( 'NONE', #7130, #15418 ) ;
#32078=DIRECTION ( 'NONE',  ( -1.000000000000000000, 0.000000000000000000, 0.000000000000000000 ) ) ;
#32083=CARTESIAN_POINT ( 'NONE',  ( 0.2944196465027555387, 4.766607801171850497E-17, 0.000000000000000000 ) ) ;
#32086=VECTOR ( 'NONE', #45424, 39.37007874015748143 ) ;
#32087=DIRECTION ( 'NONE',  ( 1.000000000000000000, 0.000000000000000000, 0.000000000000000000 ) ) ;
#32108=VECTOR ( 'NONE', #37510, 39.37007874015748143 ) ;
#32156=ORIENTED_EDGE ( 'NONE', *, *, #17489, .F. ) ;
#32182=FACE_OUTER_BOUND ( 'NONE', #43793, .T. ) ;
#32188=CARTESIAN_POINT ( 'NONE',  ( 0.1633669211802766530, 0.1605769902838746210, 5.116904466765171429E-07 ) ) ;
#32192=DIRECTION ( 'NONE',  ( -1.000000000000000000, 0.000000000000000000, 0.000000000000000000 ) ) ;
#32236=CARTESIAN_POINT ( 'NONE',  ( 0.005401850751748405420, -0.1458776762657084669, -0.02292264490068926519 ) ) ;
#32251=CARTESIAN_POINT ( 'NONE',  ( 0.1608809531673208726, 0.08280530883162598443, 0.1377952755905511861 ) ) ;
#32272=CARTESIAN_POINT ( 'NONE',  ( 0.4453382816733590377, -3.032960542342102697E-32, 0.09842519685039370636 ) ) ;
#32299=DIRECTION ( 'NONE',  ( 0.000000000000000000, -1.000000000000000000, 0.000000000000000000 ) ) ;
#32304=ADVANCED_FACE ( 'NONE', ( #31494 ), #29978, .T. ) ;
#32307=CARTESIAN_POINT ( 'NONE',  ( 0.1602931993194444682, 0.1591122789105269553, 0.000000000000000000 ) ) ;
#32338=VERTEX_POINT ( 'NONE', #2698 ) ;
#32347=CARTESIAN_POINT ( 'NONE',  ( 0.1564216623530368111, -8.910440797025414093E-13, -0.1403857474672218497 ) ) ;
#32374=CARTESIAN_POINT ( 'NONE',  ( 0.3000685424736224127, 4.466152701071653354E-17, 0.000000000000000000 ) ) ;
#32377=CARTESIAN_POINT ( 'NONE',  ( 0.1579024634500865720, -0.1046578554684589463, -0.09958160468961345380 ) ) ;
#32400=ADVANCED_FACE ( 'NONE', ( #33317 ), #33077, .T. ) ;
#32402=CARTESIAN_POINT ( 'NONE',  ( 0.3727034120734909473, 4.616380251121755931E-17, 0.000000000000000000 ) ) ;
#32405=VERTEX_POINT ( 'NONE', #22491 ) ;
#32411=VERTEX_POINT ( 'NONE', #29971 ) ;
#32414=ORIENTED_EDGE ( 'NONE', *, *, #29670, .T. ) ;
#32419=AXIS2_PLACEMENT_3D ( 'NONE', #30209, #26591, #43461 ) ;
#32427=CARTESIAN_POINT ( 'NONE',  ( 0.2519685039370078705, 4.616380251121755931E-17, 0.000000000000000000 ) ) ;
#32436=DIRECTION ( 'NONE',  ( 0.000000000000000000, -1.000000000000000000, 0.000000000000000000 ) ) ;
#32437=CARTESIAN_POINT ( 'NONE',  ( 0.1626913500575924709, 0.1599528086217352763, 1.449618227866108752E-08 ) ) ;
#32439=ORIENTED_EDGE ( 'NONE', *, *, #43868, .F. ) ;
#32448=CARTESIAN_POINT ( 'NONE',  ( 0.3425196850393700809, 0.08090551181102362266, 9.908067607274841931E-18 ) ) ;
#32452=ORIENTED_EDGE ( 'NONE', *, *, #22234, .T. ) ;
#32490=EDGE_CURVE ( 'NONE', #22780, #3723, #5703, .T. ) ;
#32492=CARTESIAN_POINT ( 'NONE',  ( 0.1558461344925403669, 0.05538344815314961284, 0.1377952755905511861 ) ) ;
#32500=VECTOR ( 'NONE', #10305, 39.37007874015748143 ) ;
#32506=CYLINDRICAL_SURFACE ( 'NONE', #31981, 0.09842519685039370636 ) ;
#32511=CARTESIAN_POINT ( 'NONE',  ( 0.1592646090380026025, -0.04727201993818823389, -0.1404638620642042202 ) ) ;
#32531=AXIS2_PLACEMENT_3D ( 'NONE', #41802, #9243, #4926 ) ;
#32537=ORIENTED_EDGE ( 'NONE', *, *, #21534, .T. ) ;
#32566=CARTESIAN_POINT ( 'NONE',  ( 0.1643927470033121618, 0.08114304680833644978, 0.1405438797532735651 ) ) ;
#32567=AXIS2_PLACEMENT_3D ( 'NONE', #38515, #20061, #12180 ) ;
#32568=CONICAL_SURFACE ( 'NONE', #10350, 0.08090551181102362266, 0.9599310885968742602 ) ;
#32569=CARTESIAN_POINT ( 'NONE',  ( 0.1644020957507537628, 0.08115590401245532937, -0.1405661490837558925 ) ) ;
#32574=FACE_OUTER_BOUND ( 'NONE', #27917, .T. ) ;
#32605=LINE ( 'NONE', #31888, #7159 ) ;
#32639=DIRECTION ( 'NONE',  ( -1.000000000000000000, 0.000000000000000000, 0.000000000000000000 ) ) ;
#32640=DIRECTION ( 'NONE',  ( -1.000000000000000000, 0.000000000000000000, 0.000000000000000000 ) ) ;
#32648=DIRECTION ( 'NONE',  ( -1.000000000000000000, 0.000000000000000000, 0.000000000000000000 ) ) ;
#32652=DIRECTION ( 'NONE',  ( 0.000000000000000000, 0.000000000000000000, 1.000000000000000000 ) ) ;
#32653=VERTEX_POINT ( 'NONE', #38535 ) ;
#32664=ADVANCED_FACE ( 'NONE', ( #23460 ), #28010, .T. ) ;
#32674=DIRECTION ( 'NONE',  ( 0.000000000000000000, -1.000000000000000000, 0.000000000000000000 ) ) ;
#32675=CARTESIAN_POINT ( 'NONE',  ( 0.1588150004739004306, -0.1472798737662755764, 0.02049432688553643953 ) ) ;
#32684=ORIENTED_EDGE ( 'NONE', *, *, #7511, .T. ) ;
#32694=PRODUCT_DEFINITION_CONTEXT ( 'detailed design', #44058, 'design' ) ;
#32713=DIRECTION ( 'NONE',  ( -1.000000000000000000, 0.000000000000000000, 0.000000000000000000 ) ) ;
#32715=CONICAL_SURFACE ( 'NONE', #17357, 0.1377952755905511861, 1.047197551196598297 ) ;
#32722=CARTESIAN_POINT ( 'NONE',  ( 0.2204724409448818867, 2.548376702365417207E-17, -0.2047244094488188948 ) ) ;
#32752=LINE ( 'NONE', #7787, #35933 ) ;
#32777=VERTEX_POINT ( 'NONE', #18143 ) ;
#32779=LENGTH_MEASURE_WITH_UNIT ( LENGTH_MEASURE( 0.02539999999999999897 ), #40618 ) ;
#32798=CARTESIAN_POINT ( 'NONE',  ( 0.000000000000000000, -0.1193342091828949042, 0.06889763779527559306 ) ) ;
#32871=CARTESIAN_POINT ( 'NONE',  ( 0.005401850751818003393, -0.09279043093872742232, 0.1148724510410191468 ) ) ;
#32877=CARTESIAN_POINT ( 'NONE',  ( 0.5660731898098425585, 1.205361022782824954E-17, -0.09842519685039370636 ) ) ;
#32884=AXIS2_PLACEMENT_3D ( 'NONE', #22662, #27233, #30368 ) ;
#32888=DIRECTION ( 'NONE',  ( 0.000000000000000000, -1.000000000000000000, 0.000000000000000000 ) ) ;
#32890=DIRECTION ( 'NONE',  ( 0.000000000000000000, -1.000000000000000000, 0.000000000000000000 ) ) ;
#32917=LINE ( 'NONE', #43900, #26225 ) ;
#32919=VERTEX_POINT ( 'NONE', #4377 ) ;
#32927=CARTESIAN_POINT ( 'NONE',  ( 0.1592537043533390206, 0.09805585504226257965, -0.1110897172142509826 ) ) ;
#32961=CARTESIAN_POINT ( 'NONE',  ( 0.3849708276051176936, 0.09842519685039370636, 0.000000000000000000 ) ) ;
#32962=CARTESIAN_POINT ( 'NONE',  ( 0.1526806705396661357, 0.02761996292092228425, 0.1377952755905511861 ) ) ;
#32989=EDGE_CURVE ( 'NONE', #45437, #27963, #31496, .T. ) ;
#33006=ORIENTED_EDGE ( 'NONE', *, *, #32490, .T. ) ;
#33034=CARTESIAN_POINT ( 'NONE',  ( 0.001106411046829922822, -0.1325885082366765888, 0.04596204078548394439 ) ) ;
#33038=DIRECTION ( 'NONE',  ( 0.000000000000000000, 1.000000000000000000, 0.000000000000000000 ) ) ;
#33054=CARTESIAN_POINT ( 'NONE',  ( 0.1605321103696441820, 0.05726506528285952441, 0.1404876550525328283 ) ) ;
#33075=AXIS2_PLACEMENT_3D ( 'NONE', #16165, #12339, #5349 ) ;
#33077=CYLINDRICAL_SURFACE ( 'NONE', #10833, 0.09842519685039370636 ) ;
#33098=VERTEX_POINT ( 'NONE', #31478 ) ;
#33111=CARTESIAN_POINT ( 'NONE',  ( 0.000000000000000000, -0.1193342091828949042, 0.06889763779527559306 ) ) ;
#33122=CARTESIAN_POINT ( 'NONE',  ( 0.3246033735368759610, 4.766607801171850497E-17, 0.000000000000000000 ) ) ;
#33154=CARTESIAN_POINT ( 'NONE',  ( 0.1608809465420316664, -0.07793157280922068109, 0.1406091075617787456 ) ) ;
#33157=CARTESIAN_POINT ( 'NONE',  ( 0.1599045142068304115, 0.09467125711649578002, 0.1169792578045390219 ) ) ;
#33163=CIRCLE ( 'NONE', #26282, 0.2047244094488188948 ) ;
#33169=CARTESIAN_POINT ( 'NONE',  ( 0.1566053014577397373, 0.1284161769476721560, -0.05833949276666106076 ) ) ;
#33181=ORIENTED_EDGE ( 'NONE', *, *, #23599, .F. ) ;
#33182=DIRECTION ( 'NONE',  ( 0.000000000000000000, 1.000000000000000000, 0.000000000000000000 ) ) ;
#33190=AXIS2_PLACEMENT_3D ( 'NONE', #37559, #16015, #8319 ) ;
#33209=PLANE ( 'NONE',  #44248 ) ;
#33211=DIRECTION ( 'NONE',  ( -1.000000000000000000, 0.000000000000000000, 0.000000000000000000 ) ) ;
#33239=ORIENTED_EDGE ( 'NONE', *, *, #70, .F. ) ;
#33254=EDGE_CURVE ( 'NONE', #21841, #11723, #6755, .T. ) ;
#33257=( CONVERSION_BASED_UNIT ( 'INCH', #32779 ) LENGTH_UNIT ( ) NAMED_UNIT ( #20658 ) ) ;
#33264=CARTESIAN_POINT ( 'NONE',  ( 0.4755220087074803481, 4.766607801171850497E-17, 0.000000000000000000 ) ) ;
#33282=VECTOR ( 'NONE', #22361, 39.37007874015748143 ) ;
#33287=AXIS2_PLACEMENT_3D ( 'NONE', #7757, #33434, #18076 ) ;
#33300=ADVANCED_FACE ( 'NONE', ( #17787 ), #868, .T. ) ;
#33309=VECTOR ( 'NONE', #43566, 39.37007874015748143 ) ;
#33317=FACE_OUTER_BOUND ( 'NONE', #15671, .T. ) ;
#33319=DIRECTION ( 'NONE',  ( -1.000000000000000000, 0.000000000000000000, 0.000000000000000000 ) ) ;
#33327=ORIENTED_EDGE ( 'NONE', *, *, #33254, .T. ) ;
#33334=DIRECTION ( 'NONE',  ( -1.000000000000000000, 0.000000000000000000, 0.000000000000000000 ) ) ;
#33346=CARTESIAN_POINT ( 'NONE',  ( 0.002094777259458696639, -0.1034000088770426068, 0.09649716854689870116 ) ) ;
#33353=LINE ( 'NONE', #33826, #12658 ) ;
#33362=EDGE_CURVE ( 'NONE', #31223, #34218, #46028, .T. ) ;
#33364=EDGE_LOOP ( 'NONE', ( #20759, #7199, #665, #38624, #2344 ) ) ;
#33375=CARTESIAN_POINT ( 'NONE',  ( 0.3727034120734909473, 4.616380251121755931E-17, 0.000000000000000000 ) ) ;
#33377=CARTESIAN_POINT ( 'NONE',  ( 0.2397010884053811242, 0.09842519685039370636, 1.205361022782828805E-17 ) ) ;
#33388=CARTESIAN_POINT ( 'NONE',  ( 0.1644020957507539848, 0.1623118080249112138, 1.367956046207553540E-19 ) ) ;
#33391=CARTESIAN_POINT ( 'NONE',  ( 0.1638905441110397043, 0.08063435062917849450, -0.1396622675802317859 ) ) ;
#33400=CARTESIAN_POINT ( 'NONE',  ( 0.1573602050224861826, 0.1351575695125303012, -0.04671412196441625253 ) ) ;
#33414=EDGE_CURVE ( 'NONE', #23956, #7655, #11553, .T. ) ;
#33426=CARTESIAN_POINT ( 'NONE',  ( 0.4330708661417322913, -0.08090551181102362266, 1.098083891755157578E-17 ) ) ;
#33434=DIRECTION ( 'NONE',  ( 1.000000000000000000, 0.000000000000000000, 0.000000000000000000 ) ) ;
#33463=ORIENTED_EDGE ( 'NONE', *, *, #28266, .F. ) ;
#33497=CARTESIAN_POINT ( 'NONE',  ( 0.000000000000000000, 0.000000000000000000, 0.000000000000000000 ) ) ;
#33512=DIRECTION ( 'NONE',  ( 0.000000000000000000, 1.000000000000000000, 0.000000000000000000 ) ) ;
#33542=SHAPE_REPRESENTATION_RELATIONSHIP ( 'NONE' , 'NONE' ,  #20643, #47308 ) ;
#33549=ORIENTED_EDGE ( 'NONE', *, *, #92, .F. ) ;
#33556=CARTESIAN_POINT ( 'NONE',  ( 0.1554374527100134684, -0.02743359356286620768, -0.1377952755905450799 ) ) ;
#33583=ADVANCED_FACE ( 'NONE', ( #27081 ), #11654, .T. ) ;
#33589=CARTESIAN_POINT ( 'NONE',  ( 0.5717220857807087109, -3.032960542342102697E-32, 0.09842519685039370636 ) ) ;
#33603=DIRECTION ( 'NONE',  ( 0.000000000000000000, 0.000000000000000000, 1.000000000000000000 ) ) ;
#33611=DIRECTION ( 'NONE',  ( -1.000000000000000000, 0.000000000000000000, 0.000000000000000000 ) ) ;
#33622=CARTESIAN_POINT ( 'NONE',  ( 0.1634463062185840532, 0.08033005673471317609, -0.1391367933297039394 ) ) ;
#33639=VECTOR ( 'NONE', #18528, 39.37007874015748854 ) ;
#33647=FACE_OUTER_BOUND ( 'NONE', #34068, .T. ) ;
#33656=AXIS2_PLACEMENT_3D ( 'NONE', #37856, #33334, #34272 ) ;
#33657=CARTESIAN_POINT ( 'NONE',  ( 0.000000000000000000, -0.1193342091828950846, -0.06889763779527559306 ) ) ;
#33677=DIRECTION ( 'NONE',  ( -1.000000000000000000, 0.000000000000000000, 0.000000000000000000 ) ) ;
#33684=DIRECTION ( 'NONE',  ( 0.000000000000000000, -1.000000000000000000, 0.000000000000000000 ) ) ;
#33713=ORIENTED_EDGE ( 'NONE', *, *, #13482, .T. ) ;
#33723=ORIENTED_EDGE ( 'NONE', *, *, #2802, .F. ) ;
#33734=DIRECTION ( 'NONE',  ( -1.000000000000000000, 0.000000000000000000, 0.000000000000000000 ) ) ;
#33742=AXIS2_PLACEMENT_3D ( 'NONE', #34229, #37805, #35165 ) ;
#33747=CARTESIAN_POINT ( 'NONE',  ( 0.1558458267876559056, 0.1470250908559905534, 0.02093562383109653577 ) ) ;
#33760=CARTESIAN_POINT ( 'NONE',  ( 0.1555687797274980522, -0.09281549603114075397, -0.1148293963254592570 ) ) ;
#33768=CARTESIAN_POINT ( 'NONE',  ( 0.5113546317124669782, 4.466152701071653354E-17, 0.000000000000000000 ) ) ;
#33782=DIRECTION ( 'NONE',  ( 1.000000000000000000, 0.000000000000000000, 0.000000000000000000 ) ) ;
#33786=CARTESIAN_POINT ( 'NONE',  ( 0.1602931993194442739, 0.07955613945526338049, 0.1377952755905511861 ) ) ;
#33804=ORIENTED_EDGE ( 'NONE', *, *, #40395, .F. ) ;
#33826=CARTESIAN_POINT ( 'NONE',  ( 0.000000000000000000, 1.205361022782826802E-17, -0.09842519685039370636 ) ) ;
#33873=CARTESIAN_POINT ( 'NONE',  ( 0.1579024634500894864, 0.1385691271450621709, -0.04084555919648127226 ) ) ;
#33883=EDGE_LOOP ( 'NONE', ( #12808, #46540, #30307, #10943, #27451 ) ) ;
#33897=CONICAL_SURFACE ( 'NONE', #13995, 0.08090551181102362266, 0.9599310885968742602 ) ;
#33898=CARTESIAN_POINT ( 'NONE',  ( -8.737111503174280059E-18, -0.1126122229443935058, -0.08054045948813907951 ) ) ;
#33914=DIRECTION ( 'NONE',  ( -1.000000000000000000, 0.000000000000000000, 0.000000000000000000 ) ) ;
#33923=ORIENTED_EDGE ( 'NONE', *, *, #16294, .F. ) ;
#33935=CARTESIAN_POINT ( 'NONE',  ( 0.2204724409448818867, 0.000000000000000000, 0.000000000000000000 ) ) ;
#33938=AXIS2_PLACEMENT_3D ( 'NONE', #47039, #43670, #36024 ) ;
#33947=DIRECTION ( 'NONE',  ( -1.000000000000000000, 0.000000000000000000, 0.000000000000000000 ) ) ;
#33955=CARTESIAN_POINT ( 'NONE',  ( 0.001099666138426426583, -0.02645731785581961759, 0.1377950862353125028 ) ) ;
#33956=DIRECTION ( 'NONE',  ( 1.000000000000000000, 0.000000000000000000, 0.000000000000000000 ) ) ;
#33997=CARTESIAN_POINT ( 'NONE',  ( 0.5962569168439626477, 4.766607801171850497E-17, 0.000000000000000000 ) ) ;
#34003=EDGE_CURVE ( 'NONE', #29529, #649, #10095, .T. ) ;
#34018=CARTESIAN_POINT ( 'NONE',  ( 0.5358894627757212481, 4.766607801171850497E-17, 0.000000000000000000 ) ) ;
#34034=CARTESIAN_POINT ( 'NONE',  ( 0.1527637205565704759, 0.02877039512963421378, -0.1377952755905511861 ) ) ;
#34064=CARTESIAN_POINT ( 'NONE',  ( 0.2519685039370078705, 0.08090551181102362266, 9.908067607274841931E-18 ) ) ;
#34065=ORIENTED_EDGE ( 'NONE', *, *, #16420, .F. ) ;
#34068=EDGE_LOOP ( 'NONE', ( #4409, #13308, #22514, #23389 ) ) ;
#34070=ORIENTED_EDGE ( 'NONE', *, *, #2635, .F. ) ;
#34086=CARTESIAN_POINT ( 'NONE',  ( 0.3604359965418638123, 4.466152701071653354E-17, 0.000000000000000000 ) ) ;
#34098=CIRCLE ( 'NONE', #32567, 0.09842519685039370636 ) ;
#34117=CARTESIAN_POINT ( 'NONE',  ( 0.1564636162838570765, -0.1073287318776653676, -0.09487486835524251705 ) ) ;
#34128=DIRECTION ( 'NONE',  ( -1.000000000000000000, 0.000000000000000000, 0.000000000000000000 ) ) ;
#34170=ORIENTED_EDGE ( 'NONE', *, *, #12189, .T. ) ;
#34177=EDGE_CURVE ( 'NONE', #21269, #30249, #20827, .T. ) ;
#34215=CARTESIAN_POINT ( 'NONE',  ( 0.006378642920406700847, -0.1475107277140030593, 0.02009854774583735501 ) ) ;
#34218=VERTEX_POINT ( 'NONE', #45472 ) ;
#34224=EDGE_CURVE ( 'NONE', #2888, #40610, #1695, .T. ) ;
#34229=CARTESIAN_POINT ( 'NONE',  ( 0.000000000000000000, 0.000000000000000000, 0.000000000000000000 ) ) ;
#34232=DIRECTION ( 'NONE',  ( -1.000000000000000000, 0.000000000000000000, 0.000000000000000000 ) ) ;
#34244=CIRCLE ( 'NONE', #38025, 0.08090551181102362266 ) ;
#34253=CARTESIAN_POINT ( 'NONE',  ( 0.000000000000000000, 1.205361022782826802E-17, -0.09842519685039370636 ) ) ;
#34264=ORIENTED_EDGE ( 'NONE', *, *, #623, .F. ) ;
#34272=DIRECTION ( 'NONE',  ( 0.000000000000000000, -1.000000000000000000, 0.000000000000000000 ) ) ;
#34280=ORIENTED_EDGE ( 'NONE', *, *, #8325, .T. ) ;
#34304=DIRECTION ( 'NONE',  ( -1.000000000000000000, 0.000000000000000000, 0.000000000000000000 ) ) ;
#34312=CARTESIAN_POINT ( 'NONE',  ( 0.1578913225048159952, -0.03378178545795391258, 0.1404269458896959810 ) ) ;
#34313=DIRECTION ( 'NONE',  ( -1.000000000000000000, 0.000000000000000000, 0.000000000000000000 ) ) ;
#34315=CARTESIAN_POINT ( 'NONE',  ( 0.4028871391076110364, 4.616380251121755931E-17, 0.000000000000000000 ) ) ;
#34340=ORIENTED_EDGE ( 'NONE', *, *, #30395, .T. ) ;
#34353=DIRECTION ( 'NONE',  ( 0.000000000000000000, 1.000000000000000000, 0.000000000000000000 ) ) ;
#34392=ORIENTED_EDGE ( 'NONE', *, *, #33362, .F. ) ;
#34418=FACE_OUTER_BOUND ( 'NONE', #39055, .T. ) ;
#34448=CARTESIAN_POINT ( 'NONE',  ( 0.3727034120734909473, 0.08090551181102362266, 9.908067607274841931E-18 ) ) ;
#34459=DIRECTION ( 'NONE',  ( 0.000000000000000000, 1.000000000000000000, 0.000000000000000000 ) ) ;
#34461=CIRCLE ( 'NONE', #37603, 0.09842519685039370636 ) ;
#34483=CARTESIAN_POINT ( 'NONE',  ( 0.1602931993194442739, 0.07955613945526338049, 0.1377952755905511861 ) ) ;
#34495=CARTESIAN_POINT ( 'NONE',  ( 0.2642359194686346169, -0.09842519685039370636, 1.205361022782828805E-17 ) ) ;
#34496=CONICAL_SURFACE ( 'NONE', #2319, 0.08090551181102362266, 0.9599310885968742602 ) ;
#34498=VERTEX_POINT ( 'NONE', #6408 ) ;
#34506=FACE_OUTER_BOUND ( 'NONE', #40914, .T. ) ;
#34507=CIRCLE ( 'NONE', #40593, 0.09842519685039370636 ) ;
#34534=FACE_OUTER_BOUND ( 'NONE', #45717, .T. ) ;
#34547=CARTESIAN_POINT ( 'NONE',  ( 0.3906197235759846786, -0.09842519685039370636, 0.000000000000000000 ) ) ;
#34577=CARTESIAN_POINT ( 'NONE',  ( 0.005401850751814351800, 0.1458776762658619275, 0.02292264490054247289 ) ) ;
#34589=CIRCLE ( 'NONE', #13921, 0.08090551181102362266 ) ;
#34630=ORIENTED_EDGE ( 'NONE', *, *, #6163, .F. ) ;
#34637=ORIENTED_EDGE ( 'NONE', *, *, #14309, .T. ) ;
#34641=ORIENTED_EDGE ( 'NONE', *, *, #5235, .T. ) ;
#34646=VECTOR ( 'NONE', #42694, 39.37007874015748143 ) ;
#34649=EDGE_CURVE ( 'NONE', #5875, #39913, #6356, .T. ) ;
#34657=B_SPLINE_CURVE_WITH_KNOTS ( 'NONE', 3,
 ( #44423, #15004, #4894, #15235, #4177, #26260, #15473, #18802, #1294, #40822, #40354, #37253, #19278, #44197, #11396, #11872, #26012, #29655, #4405, #40591, #7546, #19034 ),
 .UNSPECIFIED., .F., .F.,
 ( 4, 2, 2, 2, 2, 2, 2, 2, 2, 2, 4 ),
 ( 0.000000000000000000, 0.1250000000000007494, 0.1875000000000009714, 0.2187500000000011102, 0.2500000000000012212, 0.5000000000000013323, 0.6250000000000015543, 0.6875000000000015543, 0.7187500000000014433, 0.7500000000000012212, 1.000000000000000000 ),
 .UNSPECIFIED. ) ;
#34663=LINE ( 'NONE', #20259, #2960 ) ;
#34683=LINE ( 'NONE', #27753, #29885 ) ;
#34702=FACE_OUTER_BOUND ( 'NONE', #6138, .T. ) ;
#34710=DIRECTION ( 'NONE',  ( 0.5735764363510447161, -0.8191520442889925757, 1.003171929053525486E-16 ) ) ;
#34738=CARTESIAN_POINT ( 'NONE',  ( 0.1498753904841986506, 5.122214988120487988E-17, 0.1377952755905511861 ) ) ;
#34755=CIRCLE ( 'NONE', #41557, 0.09842519685039370636 ) ;
#34786=DIRECTION ( 'NONE',  ( -1.000000000000000000, 0.000000000000000000, 0.000000000000000000 ) ) ;
#34795=CARTESIAN_POINT ( 'NONE',  ( 0.2642359194686346169, 0.09842519685039370636, 0.000000000000000000 ) ) ;
#34819=CONICAL_SURFACE ( 'NONE', #32531, 0.08090551181102362266, 0.9599310885968742602 ) ;
#34829=CARTESIAN_POINT ( 'NONE',  ( 0.002094777259500726820, 0.1352690037935440348, 0.04129845016539761271 ) ) ;
#34847=AXIS2_PLACEMENT_3D ( 'NONE', #19116, #33782, #34459 ) ;
#34856=DIRECTION ( 'NONE',  ( -1.000000000000000000, 0.000000000000000000, 0.000000000000000000 ) ) ;
#34863=ORIENTED_EDGE ( 'NONE', *, *, #24215, .T. ) ;
#34874=ORIENTED_EDGE ( 'NONE', *, *, #27486, .F. ) ;
#34877=B_SPLINE_CURVE_WITH_KNOTS ( 'NONE', 3,
 ( #9670, #21380, #43173, #31481, #6758, #17790, #32437, #28126, #20906, #32188, #46068, #17316, #24985, #6998, #47014, #24286, #31718 ),
 .UNSPECIFIED., .F., .F.,
 ( 4, 2, 2, 2, 2, 1, 2, 2, 4 ),
 ( 0.000000000000000000, 0.2499999999999797384, 0.3749999999999609201, 0.4999999999999420464, 0.6249999999999232836, 0.6874999999999268363, 0.7187499999999351630, 0.7499999999999434896, 1.000000000000000000 ),
 .UNSPECIFIED. ) ;
#34885=DIRECTION ( 'NONE',  ( -1.000000000000000000, 0.000000000000000000, 0.000000000000000000 ) ) ;
#34889=VERTEX_POINT ( 'NONE', #8258 ) ;
#34906=DIRECTION ( 'NONE',  ( 0.5735764363510447161, 0.8191520442889925757, 0.000000000000000000 ) ) ;
#34921=DIRECTION ( 'NONE',  ( 0.000000000000000000, 1.000000000000000000, 0.000000000000000000 ) ) ;
#34946=ADVANCED_FACE ( 'NONE', ( #30352 ), #33897, .T. ) ;
#34961=DIRECTION ( 'NONE',  ( 0.000000000000000000, -1.000000000000000000, 0.000000000000000000 ) ) ;
#34981=CARTESIAN_POINT ( 'NONE',  ( 0.1588150004738602128, 0.1472798737662930069, -0.02049432688553750465 ) ) ;
#34982=EDGE_CURVE ( 'NONE', #12359, #20645, #7082, .T. ) ;
#34986=ORIENTED_EDGE ( 'NONE', *, *, #4041, .T. ) ;
#34989=CARTESIAN_POINT ( 'NONE',  ( 0.5113546317124669782, -3.032960542342102697E-32, 0.09842519685039370636 ) ) ;
#35001=AXIS2_PLACEMENT_3D ( 'NONE', #15105, #39353, #36900 ) ;
#35015=EDGE_CURVE ( 'NONE', #18113, #6083, #46799, .T. ) ;
#35056=CARTESIAN_POINT ( 'NONE',  ( 0.5966535433070866423, 0.000000000000000000, 0.09842519685039370636 ) ) ;
#35074=EDGE_CURVE ( 'NONE', #5428, #13158, #3270, .T. ) ;
#35090=ORIENTED_EDGE ( 'NONE', *, *, #8384, .F. ) ;
#35095=DIRECTION ( 'NONE',  ( -1.000000000000000000, 0.000000000000000000, 0.000000000000000000 ) ) ;
#35101=EDGE_LOOP ( 'NONE', ( #27225, #19394, #3775, #35108, #35626 ) ) ;
#35108=ORIENTED_EDGE ( 'NONE', *, *, #9960, .F. ) ;
#35133=EDGE_CURVE ( 'NONE', #19079, #19636, #40740, .T. ) ;
#35154=DIRECTION ( 'NONE',  ( -1.000000000000000000, 0.000000000000000000, 0.000000000000000000 ) ) ;
#35156=CIRCLE ( 'NONE', #14484, 0.09842519685039370636 ) ;
#35165=DIRECTION ( 'NONE',  ( 0.000000000000000000, 0.000000000000000000, 1.000000000000000000 ) ) ;
#35166=CARTESIAN_POINT ( 'NONE',  ( 0.0002862075950689860768, 0.01346164328476122732, -0.1377991285521767972 ) ) ;
#35172=DIRECTION ( 'NONE',  ( -1.000000000000000000, 0.000000000000000000, 0.000000000000000000 ) ) ;
#35175=VERTEX_POINT ( 'NONE', #22338 ) ;
#35178=EDGE_CURVE ( 'NONE', #20867, #39669, #13222, .T. ) ;
#35180=SURFACE_STYLE_FILL_AREA ( #17189 ) ;
#35185=EDGE_CURVE ( 'NONE', #17524, #42489, #10171, .T. ) ;
#35189=ORIENTED_EDGE ( 'NONE', *, *, #16146, .T. ) ;
#35192=B_SPLINE_CURVE_WITH_KNOTS ( 'NONE', 3,
 ( #35988, #21609, #10364, #47244, #17300, #46997, #21124, #3393, #3149, #24970, #14191, #13481, #29078, #17063, #10118, #24271 ),
 .UNSPECIFIED., .F., .F.,
 ( 4, 2, 2, 2, 2, 2, 2, 4 ),
 ( 0.000000000000000000, 0.1249999999999663325, 0.1874999999999494849, 0.2187499999999465983, 0.2499999999999437117, 0.3749999999999585332, 0.4999999999999734657, 1.000000000000000000 ),
 .UNSPECIFIED. ) ;
#35210=DIRECTION ( 'NONE',  ( 1.000000000000000000, 0.000000000000000000, 0.000000000000000000 ) ) ;
#35215=CARTESIAN_POINT ( 'NONE',  ( 0.1559665883013252041, 0.1473510212940076780, -0.02037109575271764048 ) ) ;
#35258=CARTESIAN_POINT ( 'NONE',  ( 0.1631207519397703531, -0.1587913448376755687, -0.006047451551306580811 ) ) ;
#35262=ORIENTED_EDGE ( 'NONE', *, *, #38476, .F. ) ;
#35265=CIRCLE ( 'NONE', #4604, 0.09842519685039370636 ) ;
#35293=CIRCLE ( 'NONE', #30719, 0.09842519685039370636 ) ;
#35317=ORIENTED_EDGE ( 'NONE', *, *, #24044, .F. ) ;
#35330=AXIS2_PLACEMENT_3D ( 'NONE', #4673, #19302, #5388 ) ;
#35340=DIRECTION ( 'NONE',  ( -1.000000000000000000, 0.000000000000000000, 0.000000000000000000 ) ) ;
#35342=B_SPLINE_CURVE_WITH_KNOTS ( 'NONE', 3,
 ( #44141, #36507, #3662, #40531, #18517, #18285, #32927, #48, #29369, #11111, #25731, #40302, #33169, #7720, #33400, #517, #33873, #22811, #1704, #22579, #26671, #41707 ),
 .UNSPECIFIED., .F., .F.,
 ( 4, 2, 2, 2, 2, 2, 2, 2, 2, 2, 4 ),
 ( 0.000000000000000000, 0.1250000000000000555, 0.1875000000000000833, 0.2187500000000001943, 0.2500000000000002776, 0.5000000000000004441, 0.6250000000000005551, 0.6875000000000006661, 0.7187500000000006661, 0.7500000000000006661, 1.000000000000000000 ),
 .UNSPECIFIED. ) ;
#35350=ORIENTED_EDGE ( 'NONE', *, *, #32490, .F. ) ;
#35378=DIRECTION ( 'NONE',  ( -1.000000000000000000, 0.000000000000000000, 0.000000000000000000 ) ) ;
#35399=ORIENTED_EDGE ( 'NONE', *, *, #7041, .T. ) ;
#35409=EDGE_CURVE ( 'NONE', #17977, #16297, #25468, .T. ) ;
#35437=ORIENTED_EDGE ( 'NONE', *, *, #46459, .F. ) ;
#35439=CARTESIAN_POINT ( 'NONE',  ( 0.002794899976010023664, 0.1008940036866861484, -0.1008370195738217678 ) ) ;
#35446=CARTESIAN_POINT ( 'NONE',  ( 0.1586955767088463476, 0.09170575825942825499, -0.1167515185291642249 ) ) ;
#35456=AXIS2_PLACEMENT_3D ( 'NONE', #13029, #12563, #27188 ) ;
#35481=ORIENTED_EDGE ( 'NONE', *, *, #44446, .F. ) ;
#35491=ORIENTED_EDGE ( 'NONE', *, *, #18190, .T. ) ;
#35512=EDGE_LOOP ( 'NONE', ( #30816, #44428 ) ) ;
#35549=APPLICATION_CONTEXT ( 'automotive_design' ) ;
#35567=FACE_OUTER_BOUND ( 'NONE', #39985, .T. ) ;
#35572=DIRECTION ( 'NONE',  ( -1.000000000000000000, 0.000000000000000000, 0.000000000000000000 ) ) ;
#35590=VECTOR ( 'NONE', #26585, 39.37007874015748854 ) ;
#35599=CARTESIAN_POINT ( 'NONE',  ( 0.1645760504121570877, -0.08210179070116299660, 0.1405695446656931025 ) ) ;
#35626=ORIENTED_EDGE ( 'NONE', *, *, #42705, .F. ) ;
#35636=B_SPLINE_CURVE_WITH_KNOTS ( 'NONE', 3,
 ( #12975, #38828, #30725, #45295, #20141, #19671, #34312, #23995, #1688, #23279, #42409, #5285 ),
 .UNSPECIFIED., .F., .F.,
 ( 4, 2, 2, 2, 2, 4 ),
 ( 0.000000000000000000, 0.2499999999999993339, 0.3749999999999991118, 0.4374999999999991118, 0.4999999999999991118, 1.000000000000000000 ),
 .UNSPECIFIED. ) ;
#35650=DIRECTION ( 'NONE',  ( -0.5735764363510518216, -0.8191520442889876907, 0.000000000000000000 ) ) ;
#35663=FACE_OUTER_BOUND ( 'NONE', #46812, .T. ) ;
#35671=CARTESIAN_POINT ( 'NONE',  ( 0.1634876958472368524, 0.08035653198460006308, 0.1391823568175673820 ) ) ;
#35673=CARTESIAN_POINT ( 'NONE',  ( 0.1598936088129072619, 0.05389714384562859645, -0.1404773021332343941 ) ) ;
#35684=ORIENTED_EDGE ( 'NONE', *, *, #26743, .T. ) ;
#35692=CARTESIAN_POINT ( 'NONE',  ( 0.5660731898098425585, 4.766607801171850497E-17, 0.000000000000000000 ) ) ;
#35696=DIMENSIONAL_EXPONENTS ( 1.000000000000000000, 0.000000000000000000, 0.000000000000000000, 0.000000000000000000, 0.000000000000000000, 0.000000000000000000, 0.000000000000000000 ) ;
#35705=CARTESIAN_POINT ( 'NONE',  ( 0.4453382816733590377, -0.09842519685039370636, 1.205361022782828805E-17 ) ) ;
#35717=CARTESIAN_POINT ( 'NONE',  ( 0.1564256176496392203, -0.1180751491311568813, -0.07625914551943928366 ) ) ;
#35720=EDGE_CURVE ( 'NONE', #6499, #35936, #17061, .T. ) ;
#35729=ORIENTED_EDGE ( 'NONE', *, *, #38229, .T. ) ;
#35733=DIRECTION ( 'NONE',  ( -1.000000000000000000, 0.000000000000000000, 0.000000000000000000 ) ) ;
#35763=FACE_OUTER_BOUND ( 'NONE', #13315, .T. ) ;
#35774=ORIENTED_EDGE ( 'NONE', *, *, #25272, .F. ) ;
#35809=VERTEX_POINT ( 'NONE', #43942 ) ;
#35811=CARTESIAN_POINT ( 'NONE',  ( 0.003062405574132101051, -0.1386494127070022064, -0.03544276884525298515 ) ) ;
#35815=EDGE_CURVE ( 'NONE', #649, #19819, #31600, .T. ) ;
#35817=CIRCLE ( 'NONE', #9041, 0.09842519685039370636 ) ;
#35828=CARTESIAN_POINT ( 'NONE',  ( 0.5839895013123354017, 0.08090551181102362266, 0.000000000000000000 ) ) ;
#35845=CARTESIAN_POINT ( 'NONE',  ( 0.1594617487093093755, -0.04893254358511540947, -0.1404675734346159666 ) ) ;
#35856=CONICAL_SURFACE ( 'NONE', #9865, 0.08090551181102362266, 0.9599310885968742602 ) ;
#35860=ORIENTED_EDGE ( 'NONE', *, *, #42398, .T. ) ;
#35865=CARTESIAN_POINT ( 'NONE',  ( 0.1822895153388602307, 0.000000000000000000, 0.000000000000000000 ) ) ;
#35869=VERTEX_POINT ( 'NONE', #32722 ) ;
#35890=ORIENTED_EDGE ( 'NONE', *, *, #21536, .F. ) ;
#35891=CARTESIAN_POINT ( 'NONE',  ( 0.1642909309750750502, 0.08091905466946164305, 0.1401559438098464727 ) ) ;
#35900=AXIS2_PLACEMENT_3D ( 'NONE', #11412, #10716, #6848 ) ;
#35901=DIRECTION ( 'NONE',  ( 0.000000000000000000, 0.000000000000000000, 1.000000000000000000 ) ) ;
#35919=CIRCLE ( 'NONE', #17585, 0.09842519685039370636 ) ;
#35927=CARTESIAN_POINT ( 'NONE',  ( 0.3906197235759846786, 4.466152701071653354E-17, 0.000000000000000000 ) ) ;
#35929=B_SPLINE_CURVE_WITH_KNOTS ( 'NONE', 3,
 ( #11965, #20074, #8574, #26817, #37825, #5209, #4981, #16496, #19603, #27542, #16031, #45455, #4735, #19837, #12677, #41854, #8105 ),
 .UNSPECIFIED., .F., .F.,
 ( 4, 2, 2, 2, 2, 1, 2, 2, 4 ),
 ( 0.000000000000000000, 0.2500000000000096034, 0.3750000000000056621, 0.5000000000000017764, 0.6249999999999978906, 0.6874999999999988898, 0.7187500000000009992, 0.7500000000000029976, 1.000000000000000000 ),
 .UNSPECIFIED. ) ;
#35933=VECTOR ( 'NONE', #47348, 39.37007874015748854 ) ;
#35936=VERTEX_POINT ( 'NONE', #29147 ) ;
#35988=CARTESIAN_POINT ( 'NONE',  ( 0.1644020957507539848, -0.1623118080249112138, 7.560884646099310910E-18 ) ) ;
#35992=AXIS2_PLACEMENT_3D ( 'NONE', #24056, #12333, #19964 ) ;
#35994=DIRECTION ( 'NONE',  ( -1.000000000000000000, 0.000000000000000000, 0.000000000000000000 ) ) ;
#35997=AXIS2_PLACEMENT_3D ( 'NONE', #470, #15125, #37371 ) ;
#36000=LINE ( 'NONE', #3158, #11653 ) ;
#36016=CARTESIAN_POINT ( 'NONE',  ( 0.5962569168439626477, 4.766607801171850497E-17, 0.000000000000000000 ) ) ;
#36024=DIRECTION ( 'NONE',  ( 0.000000000000000000, -1.000000000000000000, 0.000000000000000000 ) ) ;
#36044=ADVANCED_FACE ( 'NONE', ( #4615 ), #11754, .T. ) ;
#36052=CIRCLE ( 'NONE', #17683, 0.09842519685039370636 ) ;
#36066=CARTESIAN_POINT ( 'NONE',  ( 0.2204724409448818867, 0.07955613945526338049, -0.1377952755905511861 ) ) ;
#36075=ORIENTED_EDGE ( 'NONE', *, *, #41625, .F. ) ;
#36100=ORIENTED_EDGE ( 'NONE', *, *, #25382, .T. ) ;
#36108=EDGE_CURVE ( 'NONE', #24890, #10722, #4060, .T. ) ;
#36151=AXIS2_PLACEMENT_3D ( 'NONE', #12148, #23405, #16450 ) ;
#36169=CARTESIAN_POINT ( 'NONE',  ( 0.1822895153388602307, 2.589602477342551251E-17, 0.2114570894355444486 ) ) ;
#36196=CARTESIAN_POINT ( 'NONE',  ( 0.1566053014577344915, -0.1147315712536507021, -0.08204192511022338763 ) ) ;
#36200=ORIENTED_EDGE ( 'NONE', *, *, #24908, .T. ) ;
#36220=AXIS2_PLACEMENT_3D ( 'NONE', #22864, #33211, #25994 ) ;
#36235=ADVANCED_FACE ( 'NONE', ( #6040 ), #8701, .T. ) ;
#36243=CARTESIAN_POINT ( 'NONE',  ( 0.2204724409448818867, 0.000000000000000000, 0.000000000000000000 ) ) ;
#36262=CARTESIAN_POINT ( 'NONE',  ( 0.1645760587280559184, -0.1627877146821092580, -0.0008175030223465492218 ) ) ;
#36299=ORIENTED_EDGE ( 'NONE', *, *, #4702, .F. ) ;
#36301=CARTESIAN_POINT ( 'NONE',  ( 0.0003553830333943102347, -0.1260611533335281031, -0.05724849586115477590 ) ) ;
#36308=DIRECTION ( 'NONE',  ( 0.5735764363510447161, -0.8191520442889925757, 1.003171929053525486E-16 ) ) ;
#36313=EDGE_CURVE ( 'NONE', #40174, #38091, #34589, .T. ) ;
#36317=DIRECTION ( 'NONE',  ( 0.000000000000000000, 0.8660254037844384856, -0.5000000000000003331 ) ) ;
#36329=ADVANCED_FACE ( 'NONE', ( #32182 ), #20889, .T. ) ;
#36353=LINE ( 'NONE', #28454, #6524 ) ;
#36355=FACE_OUTER_BOUND ( 'NONE', #15328, .T. ) ;
#36359=ORIENTED_EDGE ( 'NONE', *, *, #20013, .T. ) ;
#36390=AXIS2_PLACEMENT_3D ( 'NONE', #30657, #45690, #23450 ) ;
#36404=CARTESIAN_POINT ( 'NONE',  ( 0.1592646090380165913, 0.04727201993825761589, 0.1404638620642217617 ) ) ;
#36414=ORIENTED_EDGE ( 'NONE', *, *, #3693, .F. ) ;
#36418=CARTESIAN_POINT ( 'NONE',  ( 0.3246033735368759610, 4.766607801171850497E-17, 0.000000000000000000 ) ) ;
#36456=CARTESIAN_POINT ( 'NONE',  ( 0.01230737760510393873, -0.07955613945526318620, 0.1377952755905511861 ) ) ;
#36487=DIRECTION ( 'NONE',  ( 0.000000000000000000, 0.000000000000000000, -1.000000000000000000 ) ) ;
#36491=EDGE_CURVE ( 'NONE', #18854, #35809, #36000, .T. ) ;
#36497=CARTESIAN_POINT ( 'NONE',  ( 0.1630380177252895857, 0.08011815157765787843, -0.1387688440578072890 ) ) ;
#36507=CARTESIAN_POINT ( 'NONE',  ( 0.1631207519397802896, 0.08463291909039739880, -0.1344936127549162252 ) ) ;
#36523=VERTEX_POINT ( 'NONE', #493 ) ;
#36528=CARTESIAN_POINT ( 'NONE',  ( 0.002317115957654733525, -0.1361028492805151369, -0.03985382897137078329 ) ) ;
#36529=DIRECTION ( 'NONE',  ( -1.000000000000000000, 0.000000000000000000, 0.000000000000000000 ) ) ;
#36542=CARTESIAN_POINT ( 'NONE',  ( 0.1637370781294386346, 0.08228090712086977287, 0.1377952755905510474 ) ) ;
#36549=FACE_OUTER_BOUND ( 'NONE', #33364, .T. ) ;
#36552=ORIENTED_EDGE ( 'NONE', *, *, #30584, .F. ) ;
#36558=CARTESIAN_POINT ( 'NONE',  ( 0.0003577594938017307079, 0.01348597669578762911, 0.1377974493690218849 ) ) ;
#36575=CARTESIAN_POINT ( 'NONE',  ( 0.01230737760510407577, 0.1591122789105269553, -1.502406898952441074E-18 ) ) ;
#36589=EDGE_CURVE ( 'NONE', #20673, #9638, #4731, .T. ) ;
#36591=CIRCLE ( 'NONE', #42669, 0.09842519685039370636 ) ;
#36639=ADVANCED_FACE ( 'NONE', ( #34534 ), #20069, .T. ) ;
#36645=DIRECTION ( 'NONE',  ( 0.000000000000000000, -1.000000000000000000, 0.000000000000000000 ) ) ;
#36662=DIRECTION ( 'NONE',  ( -1.000000000000000000, 0.000000000000000000, 0.000000000000000000 ) ) ;
#36687=FACE_OUTER_BOUND ( 'NONE', #7680, .T. ) ;
#36690=ORIENTED_EDGE ( 'NONE', *, *, #30763, .F. ) ;
#36692=EDGE_CURVE ( 'NONE', #28921, #40494, #35636, .T. ) ;
#36697=EDGE_CURVE ( 'NONE', #6075, #32411, #44167, .T. ) ;
#36732=CARTESIAN_POINT ( 'NONE',  ( 0.1644020957507537628, 0.08115590401245550978, 0.1405661490837558925 ) ) ;
#36755=EDGE_CURVE ( 'NONE', #12403, #43186, #15485, .T. ) ;
#36756=AXIS2_PLACEMENT_3D ( 'NONE', #5915, #42078, #5680 ) ;
#36772=CARTESIAN_POINT ( 'NONE',  ( 0.1498753904841984286, -1.109813247426106378E-16, -0.1377952755905511861 ) ) ;
#36811=DIRECTION ( 'NONE',  ( 0.000000000000000000, 1.000000000000000000, 0.000000000000000000 ) ) ;
#36822=EDGE_CURVE ( 'NONE', #20918, #42760, #46384, .T. ) ;
#36858=CARTESIAN_POINT ( 'NONE',  ( 0.1571284080983731402, 0.02678626661725594035, 0.1404155760989011514 ) ) ;
#36897=EDGE_CURVE ( 'NONE', #3732, #5428, #29308, .T. ) ;
#36900=DIRECTION ( 'NONE',  ( 0.000000000000000000, -1.000000000000000000, 0.000000000000000000 ) ) ;
#36948=CIRCLE ( 'NONE', #16319, 0.09842519685039370636 ) ;
#36952=CARTESIAN_POINT ( 'NONE',  ( 0.1566053014577290792, 0.1147315712536952914, 0.08204192511013554123 ) ) ;
#36966=DIRECTION ( 'NONE',  ( -1.000000000000000000, 0.000000000000000000, 0.000000000000000000 ) ) ;
#36985=CONICAL_SURFACE ( 'NONE', #33190, 0.08090551181102362266, 0.9599310885968742602 ) ;
#36993=PRODUCT_CONTEXT ( 'NONE', #35549, 'mechanical' ) ;
#37003=CARTESIAN_POINT ( 'NONE',  ( 0.3246033735368759610, 0.09842519685039370636, 0.000000000000000000 ) ) ;
#37009=EDGE_CURVE ( 'NONE', #1825, #9117, #44816, .T. ) ;
#37055=EDGE_CURVE ( 'NONE', #21725, #44147, #43081, .T. ) ;
#37064=CARTESIAN_POINT ( 'NONE',  ( 0.000000000000000000, 0.000000000000000000, 0.000000000000000000 ) ) ;
#37088=DIRECTION ( 'NONE',  ( 0.000000000000000000, -1.000000000000000000, 0.000000000000000000 ) ) ;
#37097=ADVANCED_FACE ( 'NONE', ( #20373 ), #40776, .T. ) ;
#37117=DIRECTION ( 'NONE',  ( 0.5735764363510447161, 0.8191520442889925757, 0.000000000000000000 ) ) ;
#37120=CARTESIAN_POINT ( 'NONE',  ( 0.1564632978426661603, 0.02849706681272137429, -0.1403868342279277759 ) ) ;
#37153=AXIS2_PLACEMENT_3D ( 'NONE', #21608, #32890, #24969 ) ;
#37156=ORIENTED_EDGE ( 'NONE', *, *, #43215, .T. ) ;
#37158=EDGE_CURVE ( 'NONE', #33098, #7386, #30118, .T. ) ;
#37165=ADVANCED_FACE ( 'NONE', ( #13439 ), #9842, .T. ) ;
#37168=VECTOR ( 'NONE', #31852, 39.37007874015748143 ) ;
#37178=CIRCLE ( 'NONE', #30361, 0.09842519685039370636 ) ;
#37180=DIRECTION ( 'NONE',  ( -1.000000000000000000, 0.000000000000000000, 0.000000000000000000 ) ) ;
#37182=CARTESIAN_POINT ( 'NONE',  ( 0.1631207519397589456, 0.1587913448376443715, 0.006047451551359922690 ) ) ;
#37185=CARTESIAN_POINT ( 'NONE',  ( 0.1644020957507537628, 0.08115590401245532937, -0.1405661490837558925 ) ) ;
#37187=EDGE_LOOP ( 'NONE', ( #11125, #14158, #9233, #39781, #35090, #33804 ) ) ;
#37200=CARTESIAN_POINT ( 'NONE',  ( 0.3302522695077432791, -0.09842519685039370636, 0.000000000000000000 ) ) ;
#37213=ORIENTED_EDGE ( 'NONE', *, *, #28604, .F. ) ;
#37217=EDGE_CURVE ( 'NONE', #1825, #6014, #3587, .T. ) ;
#37218=LINE ( 'NONE', #19476, #47063 ) ;
#37253=CARTESIAN_POINT ( 'NONE',  ( 0.1564256176496319206, -0.1250799318561882090, 0.06412650594366478551 ) ) ;
#37267=ORIENTED_EDGE ( 'NONE', *, *, #37055, .F. ) ;
#37290=CARTESIAN_POINT ( 'NONE',  ( 0.1595442748538399846, 0.1490840454108145752, 0.02272210951950409674 ) ) ;
#37304=ORIENTED_EDGE ( 'NONE', *, *, #31995, .T. ) ;
#37341=CARTESIAN_POINT ( 'NONE',  ( 0.3547871005709968273, 4.766607801171850497E-17, 0.000000000000000000 ) ) ;
#37349=CARTESIAN_POINT ( 'NONE',  ( 0.1595439659404218613, -0.05486241767500590893, -0.1404716193513352585 ) ) ;
#37371=DIRECTION ( 'NONE',  ( 0.000000000000000000, -1.000000000000000000, 0.000000000000000000 ) ) ;
#37384=VECTOR ( 'NONE', #3471, 39.37007874015748854 ) ;
#37389=AXIS2_PLACEMENT_3D ( 'NONE', #35692, #417, #37088 ) ;
#37412=CIRCLE ( 'NONE', #42759, 0.1377952755905511861 ) ;
#37444=CARTESIAN_POINT ( 'NONE',  ( 0.1563805530828667190, -0.1352584698612838698, -0.04649480693109527690 ) ) ;
#37464=CIRCLE ( 'NONE', #24476, 0.08090551181102362266 ) ;
#37467=CARTESIAN_POINT ( 'NONE',  ( 0.1822895153388602307, 0.000000000000000000, 0.000000000000000000 ) ) ;
#37491=CARTESIAN_POINT ( 'NONE',  ( 0.000000000000000000, 1.478656101119254046E-17, 0.1377952755905511861 ) ) ;
#37499=CIRCLE ( 'NONE', #16825, 0.09842519685039370636 ) ;
#37505=ORIENTED_EDGE ( 'NONE', *, *, #25382, .F. ) ;
#37507=AXIS2_PLACEMENT_3D ( 'NONE', #22466, #7390, #37558 ) ;
#37510=DIRECTION ( 'NONE',  ( -0.5735764363510518216, -0.8191520442889876907, 0.000000000000000000 ) ) ;
#37516=CARTESIAN_POINT ( 'NONE',  ( 0.003562681675963810801, -0.04170475804576580930, 0.1377952202815972693 ) ) ;
#37528=VECTOR ( 'NONE', #21756, 39.37007874015748143 ) ;
#37558=DIRECTION ( 'NONE',  ( 0.000000000000000000, -1.000000000000000000, 0.000000000000000000 ) ) ;
#37559=CARTESIAN_POINT ( 'NONE',  ( 0.3123359580052492146, 4.616380251121755931E-17, 0.000000000000000000 ) ) ;
#37570=LINE ( 'NONE', #16026, #8037 ) ;
#37594=CARTESIAN_POINT ( 'NONE',  ( 0.3547871005709968273, -0.09842519685039370636, 1.205361022782828805E-17 ) ) ;
#37603=AXIS2_PLACEMENT_3D ( 'NONE', #33264, #15266, #30384 ) ;
#37609=ORIENTED_EDGE ( 'NONE', *, *, #19244, .F. ) ;
#37616=DIRECTION ( 'NONE',  ( 0.000000000000000000, -1.000000000000000000, 0.000000000000000000 ) ) ;
#37630=DIRECTION ( 'NONE',  ( -0.5735764363510518216, 0.8191520442889876907, 1.003171929053519693E-16 ) ) ;
#37678=DIRECTION ( 'NONE',  ( 0.000000000000000000, -1.000000000000000000, 0.000000000000000000 ) ) ;
#37685=EDGE_LOOP ( 'NONE', ( #42617, #33463, #42128, #34070, #36690 ) ) ;
#37697=AXIS2_PLACEMENT_3D ( 'NONE', #24532, #27697, #9460 ) ;
#37731=ORIENTED_EDGE ( 'NONE', *, *, #623, .T. ) ;
#37744=AXIS2_PLACEMENT_3D ( 'NONE', #37467, #41260, #19249 ) ;
#37750=CIRCLE ( 'NONE', #41649, 0.08090551181102362266 ) ;
#37760=CARTESIAN_POINT ( 'NONE',  ( 0.008612976559017233164, -0.06611238040515819703, 0.1377923257425126835 ) ) ;
#37773=VECTOR ( 'NONE', #16032, 39.37007874015748143 ) ;
#37787=ORIENTED_EDGE ( 'NONE', *, *, #22998, .T. ) ;
#37789=CARTESIAN_POINT ( 'NONE',  ( 0.3302522695077432791, -3.032960542342102697E-32, 0.09842519685039370636 ) ) ;
#37796=CARTESIAN_POINT ( 'NONE',  ( 0.1555687797274980522, 0.09281549603114055969, -0.1148293963254594513 ) ) ;
#37805=DIRECTION ( 'NONE',  ( -1.000000000000000000, 0.000000000000000000, 0.000000000000000000 ) ) ;
#37825=CARTESIAN_POINT ( 'NONE',  ( 0.1619802298358933301, -0.07975797990935330761, 0.1381390393564600749 ) ) ;
#37844=AXIS2_PLACEMENT_3D ( 'NONE', #5687, #20299, #2087 ) ;
#37845=VERTEX_POINT ( 'NONE', #10806 ) ;
#37850=EDGE_LOOP ( 'NONE', ( #40699, #38487, #46550, #11399, #29360 ) ) ;
#37856=CARTESIAN_POINT ( 'NONE',  ( 0.2698848154395015464, 4.466152701071653354E-17, 0.000000000000000000 ) ) ;
#37858=ORIENTED_EDGE ( 'NONE', *, *, #34649, .T. ) ;
#37880=ORIENTED_EDGE ( 'NONE', *, *, #12646, .T. ) ;
#37881=CONICAL_SURFACE ( 'NONE', #34847, 0.09842519685039370636, 0.9599310885968824758 ) ;
#37882=VECTOR ( 'NONE', #35650, 39.37007874015748143 ) ;
#37893=DIRECTION ( 'NONE',  ( -0.5735764363510518216, -0.8191520442889876907, 0.000000000000000000 ) ) ;
#37928=CARTESIAN_POINT ( 'NONE',  ( 0.1595442748538421218, -0.1490840454108204871, -0.02272210951951406099 ) ) ;
#37939=FACE_OUTER_BOUND ( 'NONE', #23669, .T. ) ;
#37969=EDGE_LOOP ( 'NONE', ( #16528, #10217, #6244, #22305, #30593 ) ) ;
#37976=CARTESIAN_POINT ( 'NONE',  ( 0.5717220857807087109, 4.466152701071653354E-17, 0.000000000000000000 ) ) ;
#37991=EDGE_LOOP ( 'NONE', ( #2660, #15614, #40308, #2721, #30457, #27926 ) ) ;
#38017=DIRECTION ( 'NONE',  ( -1.000000000000000000, 0.000000000000000000, 0.000000000000000000 ) ) ;
#38025=AXIS2_PLACEMENT_3D ( 'NONE', #25653, #36662, #452 ) ;
#38053=CIRCLE ( 'NONE', #43376, 0.1377952755905511861 ) ;
#38062=CARTESIAN_POINT ( 'NONE',  ( 0.000000000000000000, 0.000000000000000000, 0.000000000000000000 ) ) ;
#38067=DIRECTION ( 'NONE',  ( -1.000000000000000000, 0.000000000000000000, 0.000000000000000000 ) ) ;
#38071=DIRECTION ( 'NONE',  ( -1.000000000000000000, 0.000000000000000000, 0.000000000000000000 ) ) ;
#38091=VERTEX_POINT ( 'NONE', #15582 ) ;
#38096=CIRCLE ( 'NONE', #31198, 0.09842519685039370636 ) ;
#38103=DIRECTION ( 'NONE',  ( -1.000000000000000000, 0.000000000000000000, 0.000000000000000000 ) ) ;
#38124=VECTOR ( 'NONE', #47281, 39.37007874015748143 ) ;
#38126=CARTESIAN_POINT ( 'NONE',  ( 0.003457534521343444064, 0.09882139917205609581, 0.1044452803223061832 ) ) ;
#38129=CARTESIAN_POINT ( 'NONE',  ( 0.1645805237892203066, -0.08067386790044646372, 0.1414080254031224448 ) ) ;
#38136=DIRECTION ( 'NONE',  ( -1.000000000000000000, 0.000000000000000000, 0.000000000000000000 ) ) ;
#38145=ORIENTED_EDGE ( 'NONE', *, *, #23938, .T. ) ;
#38160=CARTESIAN_POINT ( 'NONE',  ( 1.111591794296983909E-20, 0.1210185251471166540, 0.06598031696924452905 ) ) ;
#38190=CARTESIAN_POINT ( 'NONE',  ( 0.000000000000000000, 0.000000000000000000, 0.000000000000000000 ) ) ;
#38228=FACE_OUTER_BOUND ( 'NONE', #15368, .T. ) ;
#38229=EDGE_CURVE ( 'NONE', #40935, #26601, #31149, .T. ) ;
#38231=AXIS2_PLACEMENT_3D ( 'NONE', #12164, #27515, #23181 ) ;
#38286=( BOUNDED_SURFACE ( )  B_SPLINE_SURFACE ( 3, 2, ( 
 ( #20573, #28034, #9806 ),
 ( #35215, #34981, #24414 ),
 ( #27815, #20103, #16295 ),
 ( #30923, #39017, #20806 ),
 ( #23485, #35446, #45484 ),
 ( #2586, #27093, #16755 ) ),
 .UNSPECIFIED., .F., .F., .T. ) 
 B_SPLINE_SURFACE_WITH_KNOTS ( ( 4, 2, 4 ),
 ( 3, 3 ),
 ( 0.01651999345535504898, 0.01858032176739835006, 0.02064065007944164767 ),
 ( 0.000000000000000000, 1.000000000000000000 ),
 .UNSPECIFIED. ) 
 GEOMETRIC_REPRESENTATION_ITEM ( )  RATIONAL_B_SPLINE_SURFACE ( (
 ( 1.000000000000000000, 0.8047781103519390244, 1.000000000000000000),
 ( 1.000000000000000000, 0.8123785825612319655, 1.000000000000000000),
 ( 1.000000000000000000, 0.8190671539777679699, 1.000000000000000000),
 ( 1.000000000000000000, 0.8192352254845469695, 1.000000000000000000),
 ( 1.000000000000000000, 0.8126129677203649537, 1.000000000000000000),
 ( 1.000000000000000000, 0.8047712537969730073, 1.000000000000000000) ) ) 
 REPRESENTATION_ITEM ( '' )  SURFACE ( )  ) ;
#38298=ADVANCED_FACE ( 'NONE', ( #6653 ), #18801, .T. ) ;
#38305=CARTESIAN_POINT ( 'NONE',  ( 0.5717220857807087109, 4.466152701071653354E-17, 0.000000000000000000 ) ) ;
#38336=CARTESIAN_POINT ( 'NONE',  ( 0.3849708276051176936, -0.09842519685039370636, 1.205361022782828805E-17 ) ) ;
#38339=ORIENTED_EDGE ( 'NONE', *, *, #14890, .T. ) ;
#38354=DIRECTION ( 'NONE',  ( 1.000000000000000000, 0.000000000000000000, 0.000000000000000000 ) ) ;
#38377=DIRECTION ( 'NONE',  ( 1.000000000000000000, 0.000000000000000000, 0.000000000000000000 ) ) ;
#38384=CONICAL_SURFACE ( 'NONE', #42973, 0.09842519685039370636, 0.9599310885968824758 ) ;
#38396=ORIENTED_EDGE ( 'NONE', *, *, #2845, .F. ) ;
#38398=CARTESIAN_POINT ( 'NONE',  ( 0.002794899976025624899, 0.1377744224362131009, 0.03695826049526609869 ) ) ;
#38422=VECTOR ( 'NONE', #20419, 39.37007874015748854 ) ;
#38424=VERTEX_POINT ( 'NONE', #14810 ) ;
#38476=EDGE_CURVE ( 'NONE', #39669, #46509, #41728, .T. ) ;
#38487=ORIENTED_EDGE ( 'NONE', *, *, #5365, .T. ) ;
#38490=CIRCLE ( 'NONE', #36220, 0.09842519685039370636 ) ;
#38491=LINE ( 'NONE', #45654, #5281 ) ;
#38500=AXIS2_PLACEMENT_3D ( 'NONE', #20323, #33611, #3285 ) ;
#38515=CARTESIAN_POINT ( 'NONE',  ( 0.4453382816733590377, 4.766607801171850497E-17, 0.000000000000000000 ) ) ;
#38524=AXIS2_PLACEMENT_3D ( 'NONE', #336, #25769, #22381 ) ;
#38535=CARTESIAN_POINT ( 'NONE',  ( 0.000000000000000000, 0.000000000000000000, -0.1377952755905511861 ) ) ;
#38541=CARTESIAN_POINT ( 'NONE',  ( 0.3123359580052492146, 4.616380251121755931E-17, 0.000000000000000000 ) ) ;
#38554=ORIENTED_EDGE ( 'NONE', *, *, #2323, .T. ) ;
#38571=CARTESIAN_POINT ( 'NONE',  ( 0.2944196465027555387, 0.09842519685039370636, 0.000000000000000000 ) ) ;
#38596=CARTESIAN_POINT ( 'NONE',  ( 0.4934383202099732468, 4.616380251121755931E-17, 0.000000000000000000 ) ) ;
#38624=ORIENTED_EDGE ( 'NONE', *, *, #35185, .F. ) ;
#38653=AXIS2_PLACEMENT_3D ( 'NONE', #16813, #31451, #42431 ) ;
#38659=AXIS2_PLACEMENT_3D ( 'NONE', #45680, #35172, #41361 ) ;
#38682=FACE_OUTER_BOUND ( 'NONE', #26249, .T. ) ;
#38692=ORIENTED_EDGE ( 'NONE', *, *, #28549, .T. ) ;
#38704=EDGE_LOOP ( 'NONE', ( #39560, #6258, #23960, #31697, #37609 ) ) ;
#38721=CARTESIAN_POINT ( 'NONE',  ( 0.4330708661417322913, 4.616380251121755931E-17, 0.000000000000000000 ) ) ;
#38731=CARTESIAN_POINT ( 'NONE',  ( 0.2397010884053811242, 4.466152701071653354E-17, 0.000000000000000000 ) ) ;
#38739=DIRECTION ( 'NONE',  ( 0.000000000000000000, -1.000000000000000000, 0.000000000000000000 ) ) ;
#38764=CARTESIAN_POINT ( 'NONE',  ( 0.1822895153388602307, 0.000000000000000000, 0.000000000000000000 ) ) ;
#38778=EDGE_CURVE ( 'NONE', #6083, #22780, #1208, .T. ) ;
#38819=LINE ( 'NONE', #6449, #32500 ) ;
#38821=CARTESIAN_POINT ( 'NONE',  ( 0.4151545546392377273, 4.766607801171850497E-17, 0.000000000000000000 ) ) ;
#38826=ADVANCED_FACE ( 'NONE', ( #20742 ), #28042, .T. ) ;
#38827=CARTESIAN_POINT ( 'NONE',  ( 0.4755220087074803481, 4.766607801171850497E-17, 0.000000000000000000 ) ) ;
#38828=CARTESIAN_POINT ( 'NONE',  ( 0.1564216623530369221, -0.006801955215180027596, 0.1403857474672648431 ) ) ;
#38847=CYLINDRICAL_SURFACE ( 'NONE', #29102, 0.09842519685039370636 ) ;
#38858=ORIENTED_EDGE ( 'NONE', *, *, #25159, .F. ) ;
#38894=DIRECTION ( 'NONE',  ( -1.000000000000000000, 0.000000000000000000, 0.000000000000000000 ) ) ;
#38906=CARTESIAN_POINT ( 'NONE',  ( 0.000000000000000000, 0.1591122789105269553, 0.000000000000000000 ) ) ;
#38911=AXIS2_PLACEMENT_3D ( 'NONE', #16545, #38103, #19410 ) ;
#38912=CARTESIAN_POINT ( 'NONE',  ( 0.5839895013123354017, 4.616380251121755931E-17, 0.000000000000000000 ) ) ;
#38926=CONICAL_SURFACE ( 'NONE', #47366, 0.08090551181102362266, 0.9599310885968742602 ) ;
#38936=DIRECTION ( 'NONE',  ( -1.000000000000000000, 0.000000000000000000, 0.000000000000000000 ) ) ;
#38974=ORIENTED_EDGE ( 'NONE', *, *, #43046, .T. ) ;
#38975=CARTESIAN_POINT ( 'NONE',  ( 0.000000000000000000, 0.000000000000000000, 0.09842519685039370636 ) ) ;
#38991=DIRECTION ( 'NONE',  ( 0.000000000000000000, 0.000000000000000000, 1.000000000000000000 ) ) ;
#38998=CIRCLE ( 'NONE', #27555, 0.2114570894355444486 ) ;
#39008=CARTESIAN_POINT ( 'NONE',  ( 0.001132063567019381744, 0.1075630933946142148, -0.08929056810493603280 ) ) ;
#39017=CARTESIAN_POINT ( 'NONE',  ( 0.1554371429169570662, 0.1056204263327887305, -0.09265060645563602537 ) ) ;
#39023=CYLINDRICAL_SURFACE ( 'NONE', #43472, 0.09842519685039370636 ) ;
#39034=CIRCLE ( 'NONE', #37507, 0.09842519685039370636 ) ;
#39052=CARTESIAN_POINT ( 'NONE',  ( 0.1573602050224812976, -0.1080344010929237403, -0.09369282772939586945 ) ) ;
#39055=EDGE_LOOP ( 'NONE', ( #4771, #26516, #9709, #10939, #17938, #31333 ) ) ;
#39057=DIRECTION ( 'NONE',  ( -1.000000000000000000, 0.000000000000000000, 0.000000000000000000 ) ) ;
#39066=CARTESIAN_POINT ( 'NONE',  ( 0.4811709046783464450, 4.466152701071653354E-17, 0.000000000000000000 ) ) ;
#39070=CARTESIAN_POINT ( 'NONE',  ( 0.3604359965418638123, -3.032960542342102697E-32, 0.09842519685039370636 ) ) ;
#39078=ORIENTED_EDGE ( 'NONE', *, *, #17173, .T. ) ;
#39094=EDGE_CURVE ( 'NONE', #38424, #14831, #19594, .T. ) ;
#39125=DIRECTION ( 'NONE',  ( 0.000000000000000000, -1.000000000000000000, 0.000000000000000000 ) ) ;
#39137=ORIENTED_EDGE ( 'NONE', *, *, #35178, .T. ) ;
#39156=EDGE_CURVE ( 'NONE', #40494, #20918, #34657, .T. ) ;
#39177=ORIENTED_EDGE ( 'NONE', *, *, #42560, .F. ) ;
#39193=CONICAL_SURFACE ( 'NONE', #5543, 0.08090551181102362266, 0.9599310885968742602 ) ;
#39227=DIRECTION ( 'NONE',  ( -1.000000000000000000, 0.000000000000000000, 0.000000000000000000 ) ) ;
#39245=CARTESIAN_POINT ( 'NONE',  ( 0.000000000000000000, 0.000000000000000000, 0.000000000000000000 ) ) ;
#39248=ORIENTED_EDGE ( 'NONE', *, *, #43557, .F. ) ;
#39286=CARTESIAN_POINT ( 'NONE',  ( 0.1571168540705020489, -0.1349219317375998928, -0.04713923310949922479 ) ) ;
#39288=VECTOR ( 'NONE', #29966, 39.37007874015748143 ) ;
#39307=DIRECTION ( 'NONE',  ( -1.000000000000000000, 0.000000000000000000, 0.000000000000000000 ) ) ;
#39308=ORIENTED_EDGE ( 'NONE', *, *, #2635, .T. ) ;
#39323=AXIS2_PLACEMENT_3D ( 'NONE', #34018, #41142, #1143 ) ;
#39343=ORIENTED_EDGE ( 'NONE', *, *, #46836, .T. ) ;
#39353=DIRECTION ( 'NONE',  ( -1.000000000000000000, 0.000000000000000000, 0.000000000000000000 ) ) ;
#39356=CIRCLE ( 'NONE', #39461, 0.09842519685039370636 ) ;
#39359=AXIS2_PLACEMENT_3D ( 'NONE', #45164, #41551, #8759 ) ;
#39382=EDGE_CURVE ( 'NONE', #8358, #37845, #15379, .T. ) ;
#39418=B_SPLINE_CURVE_WITH_KNOTS ( 'NONE', 3,
 ( #21330, #33760, #25836, #15529, #40639 ),
 .UNSPECIFIED., .F., .F.,
 ( 4, 1, 4 ),
 ( 0.000000000000000000, 0.002020725942163689639, 0.004041451884327379278 ),
 .UNSPECIFIED. ) ;
#39439=CARTESIAN_POINT ( 'NONE',  ( 0.003620633035317427639, 0.04207376041596044836, -0.1377952987789565764 ) ) ;
#39448=VERTEX_POINT ( 'NONE', #30028 ) ;
#39460=VECTOR ( 'NONE', #13023, 39.37007874015748854 ) ;
#39461=AXIS2_PLACEMENT_3D ( 'NONE', #31761, #10181, #7045 ) ;
#39469=CARTESIAN_POINT ( 'NONE',  ( 0.000000000000000000, 0.000000000000000000, 0.000000000000000000 ) ) ;
#39471=CARTESIAN_POINT ( 'NONE',  ( 0.1611065205440928294, 0.07958672989228716965, 0.1378549147581101531 ) ) ;
#39472=CARTESIAN_POINT ( 'NONE',  ( 0.002094777259473996466, 0.1034000088769234660, -0.09649716854706523461 ) ) ;
#39521=CARTESIAN_POINT ( 'NONE',  ( 0.000000000000000000, 0.000000000000000000, 0.000000000000000000 ) ) ;
#39522=CARTESIAN_POINT ( 'NONE',  ( 0.1582120475477764854, -0.1029568672337116270, -0.1025480767803625959 ) ) ;
#39524=ORIENTED_EDGE ( 'NONE', *, *, #29107, .F. ) ;
#39560=ORIENTED_EDGE ( 'NONE', *, *, #25397, .F. ) ;
#39561=CARTESIAN_POINT ( 'NONE',  ( 0.2821522309711287368, 4.616380251121755931E-17, 0.000000000000000000 ) ) ;
#39571=DIRECTION ( 'NONE',  ( 0.000000000000000000, -1.000000000000000000, 0.000000000000000000 ) ) ;
#39621=CARTESIAN_POINT ( 'NONE',  ( 0.4509871776442260227, 1.205361022782824954E-17, -0.09842519685039370636 ) ) ;
#39633=AXIS2_PLACEMENT_3D ( 'NONE', #44324, #3847, #244 ) ;
#39641=VERTEX_POINT ( 'NONE', #33377 ) ;
#39668=AXIS2_PLACEMENT_3D ( 'NONE', #32066, #46654, #5469 ) ;
#39669=VERTEX_POINT ( 'NONE', #3873 ) ;
#39671=CARTESIAN_POINT ( 'NONE',  ( 0.2204724409448818867, -0.07955613945526357478, -0.1377952755905511861 ) ) ;
#39674=DIRECTION ( 'NONE',  ( -1.000000000000000000, 0.000000000000000000, 0.000000000000000000 ) ) ;
#39677=CARTESIAN_POINT ( 'NONE',  ( 0.001443311806748592266, -0.02661417251542722018, -0.1377865128822150786 ) ) ;
#39693=ADVANCED_FACE ( 'NONE', ( #21859 ), #38926, .T. ) ;
#39704=CIRCLE ( 'NONE', #45833, 0.09842519685039370636 ) ;
#39734=CARTESIAN_POINT ( 'NONE',  ( 0.1602931993194442739, -0.07955613945526357478, -0.1377952755905511861 ) ) ;
#39749=CARTESIAN_POINT ( 'NONE',  ( 0.1594510458733890690, -0.1460701887064284055, -0.02793386226024194632 ) ) ;
#39781=ORIENTED_EDGE ( 'NONE', *, *, #7511, .F. ) ;
#39787=ADVANCED_FACE ( 'NONE', ( #24174 ), #44277, .T. ) ;
#39795=EDGE_CURVE ( 'NONE', #16297, #17977, #22858, .T. ) ;
#39804=CARTESIAN_POINT ( 'NONE',  ( 0.3000685424736224127, 4.466152701071653354E-17, 0.000000000000000000 ) ) ;
#39846=CIRCLE ( 'NONE', #26087, 0.09842519685039370636 ) ;
#39868=AXIS2_PLACEMENT_3D ( 'NONE', #29446, #33956, #12616 ) ;
#39871=CARTESIAN_POINT ( 'NONE',  ( 0.1586958850898451678, 0.05525856355904548017, 0.1377952755905512694 ) ) ;
#39873=CARTESIAN_POINT ( 'NONE',  ( 0.1555687797274980522, -0.05303742630350904985, -0.1377952755905511861 ) ) ;
#39896=CARTESIAN_POINT ( 'NONE',  ( 0.1564216623530368111, -8.910440797025414093E-13, -0.1403857474672218497 ) ) ;
#39913=VERTEX_POINT ( 'NONE', #42357 ) ;
#39917=CONICAL_SURFACE ( 'NONE', #25407, 0.09842519685039370636, 0.9599310885968824758 ) ;
#39920=DIRECTION ( 'NONE',  ( 0.000000000000000000, 0.000000000000000000, 1.000000000000000000 ) ) ;
#39945=CARTESIAN_POINT ( 'NONE',  ( 0.1582007246420325530, 0.03721045995875260637, -0.1404371117717378159 ) ) ;
#39959=CARTESIAN_POINT ( 'NONE',  ( 0.1644020957507537628, 0.08115590401245550978, 0.1405661490837558925 ) ) ;
#39979=CARTESIAN_POINT ( 'NONE',  ( 0.4208034506101054895, 4.466152701071653354E-17, 0.000000000000000000 ) ) ;
#39981=AXIS2_PLACEMENT_3D ( 'NONE', #36243, #42673, #24729 ) ;
#39985=EDGE_LOOP ( 'NONE', ( #10816, #41864, #34392, #45620, #17153, #15425 ) ) ;
#40019=CYLINDRICAL_SURFACE ( 'NONE', #39633, 0.09842519685039370636 ) ;
#40020=ADVANCED_FACE ( 'NONE', ( #35663 ), #17430, .T. ) ;
#40023=ADVANCED_FACE ( 'NONE', ( #27553 ), #45792, .T. ) ;
#40046=CARTESIAN_POINT ( 'NONE',  ( 0.4151545546392377273, 4.766607801171850497E-17, 0.000000000000000000 ) ) ;
#40052=CARTESIAN_POINT ( 'NONE',  ( 0.1582120475477748200, 0.1029568672337303342, 0.1025480767803373799 ) ) ;
#40079=EDGE_CURVE ( 'NONE', #23379, #23076, #34663, .T. ) ;
#40139=EDGE_CURVE ( 'NONE', #8724, #9638, #46125, .T. ) ;
#40146=ORIENTED_EDGE ( 'NONE', *, *, #22825, .F. ) ;
#40147=VECTOR ( 'NONE', #6139, 39.37007874015748143 ) ;
#40156=CARTESIAN_POINT ( 'NONE',  ( 0.4151545546392377273, -0.09842519685039370636, 1.205361022782828805E-17 ) ) ;
#40170=DIRECTION ( 'NONE',  ( -1.000000000000000000, 0.000000000000000000, 0.000000000000000000 ) ) ;
#40174=VERTEX_POINT ( 'NONE', #13543 ) ;
#40196=CARTESIAN_POINT ( 'NONE',  ( 0.5962569168439626477, 0.09842519685039370636, 0.000000000000000000 ) ) ;
#40218=ORIENTED_EDGE ( 'NONE', *, *, #28266, .T. ) ;
#40219=CARTESIAN_POINT ( 'NONE',  ( 0.3123359580052492146, -0.08090551181102362266, 1.098083891755157578E-17 ) ) ;
#40221=DIRECTION ( 'NONE',  ( -0.5735764363510518216, 0.8191520442889876907, 1.003171929053519693E-16 ) ) ;
#40224=DIRECTION ( 'NONE',  ( 0.000000000000000000, -1.000000000000000000, 0.000000000000000000 ) ) ;
#40233=FACE_OUTER_BOUND ( 'NONE', #2009, .T. ) ;
#40249=ADVANCED_FACE ( 'NONE', ( #21684 ), #1604, .F. ) ;
#40258=DIRECTION ( 'NONE',  ( 0.000000000000000000, -1.000000000000000000, 0.000000000000000000 ) ) ;
#40282=DIRECTION ( 'NONE',  ( 0.000000000000000000, -1.000000000000000000, 0.000000000000000000 ) ) ;
#40285=CARTESIAN_POINT ( 'NONE',  ( 0.1555213372790489601, -0.1336203177416374344, 0.04415337192907527186 ) ) ;
#40297=B_SPLINE_CURVE_WITH_KNOTS ( 'NONE', 3,
 ( #36575, #40839, #15021, #44211, #3966, #592, #30367, #3738, #7561, #14773, #15488, #30131, #18358 ),
 .UNSPECIFIED., .F., .F.,
 ( 4, 2, 2, 1, 2, 2, 4 ),
 ( 0.000000000000000000, 0.2499999999999984457, 0.3749999999999975020, 0.4374999999999972244, 0.4687499999999971134, 0.4999999999999971134, 1.000000000000000000 ),
 .UNSPECIFIED. ) ;
#40302=CARTESIAN_POINT ( 'NONE',  ( 0.1564256176496426898, 0.1250799318563151907, -0.06412650594350359501 ) ) ;
#40308=ORIENTED_EDGE ( 'NONE', *, *, #960, .T. ) ;
#40353=CARTESIAN_POINT ( 'NONE',  ( 0.000000000000000000, 0.000000000000000000, 0.000000000000000000 ) ) ;
#40354=CARTESIAN_POINT ( 'NONE',  ( 0.1564139474901095617, -0.1149079234233351815, 0.08174552760832223819 ) ) ;
#40358=EDGE_LOOP ( 'NONE', ( #21653, #46919, #46804 ) ) ;
#40359=AXIS2_PLACEMENT_3D ( 'NONE', #20569, #35210, #28251 ) ;
#40380=CARTESIAN_POINT ( 'NONE',  ( 0.01034490908492528144, -0.07275794908485518075, 0.1377952755905511306 ) ) ;
#40385=AXIS2_PLACEMENT_3D ( 'NONE', #7268, #22104, #29599 ) ;
#40386=( BOUNDED_SURFACE ( )  B_SPLINE_SURFACE ( 3, 2, ( 
 ( #19464, #8679, #1245 ),
 ( #15422, #22829, #1475 ),
 ( #44608, #4352, #34117 ),
 ( #4595, #41012, #37444 ),
 ( #8203, #11824, #37928 ),
 ( #16133, #1007, #30764 ) ),
 .UNSPECIFIED., .F., .F., .T. ) 
 B_SPLINE_SURFACE_WITH_KNOTS ( ( 4, 2, 4 ),
 ( 3, 3 ),
 ( 0.01651999345535504898, 0.01858032176739835006, 0.02064065007944164767 ),
 ( 0.000000000000000000, 1.000000000000000000 ),
 .UNSPECIFIED. ) 
 GEOMETRIC_REPRESENTATION_ITEM ( )  RATIONAL_B_SPLINE_SURFACE ( (
 ( 1.000000000000000000, 0.8047781103519390244, 1.000000000000000000),
 ( 1.000000000000000000, 0.8123785825609349809, 1.000000000000000000),
 ( 1.000000000000000000, 0.8190671539781639865, 1.000000000000000000),
 ( 1.000000000000000000, 0.8192352254841480663, 1.000000000000000000),
 ( 1.000000000000000000, 0.8126129677206639368, 1.000000000000000000),
 ( 1.000000000000000000, 0.8047712537969730073, 1.000000000000000000) ) ) 
 REPRESENTATION_ITEM ( '' )  SURFACE ( )  ) ;
#40395=EDGE_CURVE ( 'NONE', #1067, #46509, #29863, .T. ) ;
#40406=CARTESIAN_POINT ( 'NONE',  ( 0.1617601974881476001, 0.07970274315509767726, 0.1380562389070501550 ) ) ;
#40411=CARTESIAN_POINT ( 'NONE',  ( 0.3604359965418638123, 0.09842519685039370636, 1.205361022782828805E-17 ) ) ;
#40438=ORIENTED_EDGE ( 'NONE', *, *, #36589, .T. ) ;
#40461=ORIENTED_EDGE ( 'NONE', *, *, #6163, .T. ) ;
#40473=ORIENTED_EDGE ( 'NONE', *, *, #2802, .T. ) ;
#40483=AXIS2_PLACEMENT_3D ( 'NONE', #500, #10623, #25225 ) ;
#40487=ORIENTED_EDGE ( 'NONE', *, *, #46473, .F. ) ;
#40493=CONICAL_SURFACE ( 'NONE', #32884, 0.09842519685039370636, 0.9599310885968824758 ) ;
#40494=VERTEX_POINT ( 'NONE', #12091 ) ;
#40512=DIRECTION ( 'NONE',  ( -0.5735764363510518216, 0.8191520442889876907, 1.003171929053519693E-16 ) ) ;
#40513=DIRECTION ( 'NONE',  ( 0.000000000000000000, -1.000000000000000000, 0.000000000000000000 ) ) ;
#40531=CARTESIAN_POINT ( 'NONE',  ( 0.1605229034655568932, 0.09306627081908142030, -0.1197794644538782011 ) ) ;
#40545=FACE_OUTER_BOUND ( 'NONE', #37969, .T. ) ;
#40569=LINE ( 'NONE', #32961, #10779 ) ;
#40572=CARTESIAN_POINT ( 'NONE',  ( 0.3906197235759846786, 0.09842519685039370636, 1.205361022782828805E-17 ) ) ;
#40588=CONICAL_SURFACE ( 'NONE', #35992, 0.08090551181102362266, 0.9599310885968742602 ) ;
#40589=CARTESIAN_POINT ( 'NONE',  ( 0.001140081640800088593, 0.02362312937809664393, 0.1377990287693362237 ) ) ;
#40591=CARTESIAN_POINT ( 'NONE',  ( 0.1599045142067893333, -0.1486426375326765359, 0.02349808476896642767 ) ) ;
#40593=AXIS2_PLACEMENT_3D ( 'NONE', #44593, #29814, #7955 ) ;
#40605=CARTESIAN_POINT ( 'NONE',  ( 0.000000000000000000, 0.000000000000000000, 0.000000000000000000 ) ) ;
#40610=VERTEX_POINT ( 'NONE', #46314 ) ;
#40618=( LENGTH_UNIT ( ) NAMED_UNIT ( * ) SI_UNIT ( $, .METRE. ) ) ;
#40627=DIRECTION ( 'NONE',  ( -1.000000000000000000, 0.000000000000000000, 0.000000000000000000 ) ) ;
#40629=CARTESIAN_POINT ( 'NONE',  ( 0.1526809758745832635, 0.1331472126641763676, 0.04497281396057103281 ) ) ;
#40639=CARTESIAN_POINT ( 'NONE',  ( 0.1602931993194444682, -0.1591122789105269553, 0.000000000000000000 ) ) ;
#40644=AXIS2_PLACEMENT_3D ( 'NONE', #29901, #44448, #1078 ) ;
#40699=ORIENTED_EDGE ( 'NONE', *, *, #36313, .F. ) ;
#40700=ORIENTED_EDGE ( 'NONE', *, *, #20068, .T. ) ;
#40701=ORIENTED_EDGE ( 'NONE', *, *, #30492, .T. ) ;
#40726=ORIENTED_EDGE ( 'NONE', *, *, #4010, .T. ) ;
#40736=CARTESIAN_POINT ( 'NONE',  ( 0.000000000000000000, 0.000000000000000000, 0.09842519685039370636 ) ) ;
#40740=CIRCLE ( 'NONE', #37697, 0.08090551181102362266 ) ;
#40743=CARTESIAN_POINT ( 'NONE',  ( 0.000000000000000000, 0.000000000000000000, 0.000000000000000000 ) ) ;
#40752=CARTESIAN_POINT ( 'NONE',  ( 0.1605229034655247800, 0.1502651944781876470, 0.02070802253799618881 ) ) ;
#40755=CARTESIAN_POINT ( 'NONE',  ( 0.1643592525017875672, 0.08109370453517872335, -0.1404553931991618931 ) ) ;
#40769=ORIENTED_EDGE ( 'NONE', *, *, #41303, .T. ) ;
#40776=CONICAL_SURFACE ( 'NONE', #5610, 0.09842519685039370636, 0.9599310885968824758 ) ;
#40819=CARTESIAN_POINT ( 'NONE',  ( 0.0005771639294482186966, 0.01692329920547855360, 0.1377992204327473935 ) ) ;
#40822=CARTESIAN_POINT ( 'NONE',  ( 0.1571168540705163430, -0.1082847392565217393, 0.09327620385775631240 ) ) ;
#40839=CARTESIAN_POINT ( 'NONE',  ( 0.01035225325193033126, 0.1557259041957147483, -0.005865373059513411674 ) ) ;
#40849=CIRCLE ( 'NONE', #302, 0.08090551181102362266 ) ;
#40852=LINE ( 'NONE', #30600, #9564 ) ;
#40856=VECTOR ( 'NONE', #41193, 39.37007874015748143 ) ;
#40865=CARTESIAN_POINT ( 'NONE',  ( 0.1645760587280559184, 0.08068587895603188120, 0.1413870478498926997 ) ) ;
#40874=CARTESIAN_POINT ( 'NONE',  ( 0.1498753904841986506, 0.1193342091828950846, -0.06889763779527559306 ) ) ;
#40876=EDGE_LOOP ( 'NONE', ( #21601, #11934, #24158, #19706, #41104 ) ) ;
#40877=VECTOR ( 'NONE', #7104, 39.37007874015748854 ) ;
#40884=AXIS2_PLACEMENT_3D ( 'NONE', #1087, #33734, #8524 ) ;
#40906=CARTESIAN_POINT ( 'NONE',  ( 0.5962569168439626477, -0.09842519685039370636, 1.205361022782828805E-17 ) ) ;
#40909=CARTESIAN_POINT ( 'NONE',  ( 0.5415383587465882886, -3.032960542342102697E-32, 0.09842519685039370636 ) ) ;
#40914=EDGE_LOOP ( 'NONE', ( #30678, #37731, #2763, #19745, #21278 ) ) ;
#40917=EDGE_CURVE ( 'NONE', #43186, #29608, #35156, .T. ) ;
#40925=CARTESIAN_POINT ( 'NONE',  ( 0.1558455157293398008, -0.05538006030750638325, -0.1377952755905511861 ) ) ;
#40935=VERTEX_POINT ( 'NONE', #18266 ) ;
#40950=ORIENTED_EDGE ( 'NONE', *, *, #30763, .T. ) ;
#40960=CIRCLE ( 'NONE', #28009, 0.09842519685039370636 ) ;
#40989=CARTESIAN_POINT ( 'NONE',  ( 0.1644020957507537628, 0.08115590401245550978, 0.1405661490837558925 ) ) ;
#41010=ORIENTED_EDGE ( 'NONE', *, *, #29238, .F. ) ;
#41012=CARTESIAN_POINT ( 'NONE',  ( 0.1554371429169570384, -0.1330479920330144283, -0.04514466913491271133 ) ) ;
#41021=DIRECTION ( 'NONE',  ( -1.000000000000000000, 0.000000000000000000, 0.000000000000000000 ) ) ;
#41027=SHAPE_DEFINITION_REPRESENTATION ( #20868, #20643 ) ;
#41070=CIRCLE ( 'NONE', #16613, 0.09842519685039370636 ) ;
#41072=CARTESIAN_POINT ( 'NONE',  ( 0.5962569168439626477, 4.766607801171850497E-17, 0.000000000000000000 ) ) ;
#41086=CARTESIAN_POINT ( 'NONE',  ( 0.5236220472440944462, 4.616380251121755931E-17, 0.000000000000000000 ) ) ;
#41104=ORIENTED_EDGE ( 'NONE', *, *, #41843, .F. ) ;
#41132=CARTESIAN_POINT ( 'NONE',  ( 0.4811709046783464450, 1.205361022782824954E-17, -0.09842519685039370636 ) ) ;
#41133=ORIENTED_EDGE ( 'NONE', *, *, #39382, .T. ) ;
#41142=DIRECTION ( 'NONE',  ( -1.000000000000000000, 0.000000000000000000, 0.000000000000000000 ) ) ;
#41193=DIRECTION ( 'NONE',  ( -0.5735764363510518216, -0.8191520442889876907, 0.000000000000000000 ) ) ;
#41213=ORIENTED_EDGE ( 'NONE', *, *, #28604, .T. ) ;
#41222=DIRECTION ( 'NONE',  ( -1.000000000000000000, 0.000000000000000000, 0.000000000000000000 ) ) ;
#41231=DIRECTION ( 'NONE',  ( 0.000000000000000000, 0.000000000000000000, 1.000000000000000000 ) ) ;
#41232=VERTEX_POINT ( 'NONE', #18833 ) ;
#41245=EDGE_CURVE ( 'NONE', #18563, #5973, #30255, .T. ) ;
#41248=CIRCLE ( 'NONE', #23678, 0.08090551181102362266 ) ;
#41256=ORIENTED_EDGE ( 'NONE', *, *, #24253, .F. ) ;
#41260=DIRECTION ( 'NONE',  ( 1.000000000000000000, 0.000000000000000000, 0.000000000000000000 ) ) ;
#41281=ORIENTED_EDGE ( 'NONE', *, *, #35409, .F. ) ;
#41283=ORIENTED_EDGE ( 'NONE', *, *, #35409, .T. ) ;
#41295=CONICAL_SURFACE ( 'NONE', #1533, 0.09842519685039370636, 0.9599310885968824758 ) ;
#41303=EDGE_CURVE ( 'NONE', #5973, #4993, #40852, .T. ) ;
#41313=EDGE_CURVE ( 'NONE', #8358, #6083, #23308, .T. ) ;
#41354=ADVANCED_FACE ( 'NONE', ( #23396 ), #11072, .T. ) ;
#41361=DIRECTION ( 'NONE',  ( 0.000000000000000000, 0.000000000000000000, 1.000000000000000000 ) ) ;
#41376=DIRECTION ( 'NONE',  ( 0.000000000000000000, -1.073081856240829922E-16, -1.000000000000000000 ) ) ;
#41408=ORIENTED_EDGE ( 'NONE', *, *, #28056, .F. ) ;
#41411=ORIENTED_EDGE ( 'NONE', *, *, #38778, .F. ) ;
#41432=EDGE_CURVE ( 'NONE', #23848, #12702, #1879, .T. ) ;
#41438=CYLINDRICAL_SURFACE ( 'NONE', #15666, 0.09842519685039370636 ) ;
#41460=CIRCLE ( 'NONE', #6287, 0.09842519685039370636 ) ;
#41469=DIRECTION ( 'NONE',  ( -1.000000000000000000, 0.000000000000000000, 0.000000000000000000 ) ) ;
#41485=CARTESIAN_POINT ( 'NONE',  ( 0.003583035186828842367, -0.09844385435685996943, -0.1050988454126300514 ) ) ;
#41512=DIRECTION ( 'NONE',  ( 0.000000000000000000, 0.000000000000000000, 1.000000000000000000 ) ) ;
#41519=ORIENTED_EDGE ( 'NONE', *, *, #23278, .F. ) ;
#41526=CARTESIAN_POINT ( 'NONE',  ( 0.5839895013123354017, 4.616380251121755931E-17, 0.000000000000000000 ) ) ;
#41551=DIRECTION ( 'NONE',  ( -1.000000000000000000, 0.000000000000000000, 0.000000000000000000 ) ) ;
#41557=AXIS2_PLACEMENT_3D ( 'NONE', #39979, #22019, #36645 ) ;
#41605=CIRCLE ( 'NONE', #42410, 0.09842519685039370636 ) ;
#41625=EDGE_CURVE ( 'NONE', #6499, #24890, #8202, .T. ) ;
#41631=CIRCLE ( 'NONE', #20986, 0.09842519685039370636 ) ;
#41632=ORIENTED_EDGE ( 'NONE', *, *, #23227, .F. ) ;
#41649=AXIS2_PLACEMENT_3D ( 'NONE', #2470, #10155, #42701 ) ;
#41663=CARTESIAN_POINT ( 'NONE',  ( 0.5660731898098425585, 0.09842519685039370636, 0.000000000000000000 ) ) ;
#41666=CARTESIAN_POINT ( 'NONE',  ( 0.3849708276051176936, 4.766607801171850497E-17, 0.000000000000000000 ) ) ;
#41685=B_SPLINE_CURVE_WITH_KNOTS ( 'NONE', 3,
 ( #33388, #37182, #33, #40752, #15396, #7948, #22092, #22567, #4326, #7252, #3881, #47266, #36952, #278, #29805, #18959, #18500, #40052, #14923, #33157, #18270, #40989 ),
 .UNSPECIFIED., .F., .F.,
 ( 4, 2, 2, 2, 2, 2, 2, 2, 2, 2, 4 ),
 ( 0.000000000000000000, 0.1250000000000002776, 0.1875000000000003331, 0.2187500000000003053, 0.2500000000000002776, 0.5000000000000002220, 0.6250000000000002220, 0.6875000000000003331, 0.7187500000000002220, 0.7500000000000002220, 1.000000000000000000 ),
 .UNSPECIFIED. ) ;
#41707=CARTESIAN_POINT ( 'NONE',  ( 0.1644020957507539848, 0.1623118080249112138, 1.367956046207553540E-19 ) ) ;
#41728=CIRCLE ( 'NONE', #24932, 0.09842519685039370636 ) ;
#41729=CARTESIAN_POINT ( 'NONE',  ( 0.000000000000000000, 0.1193342091828950846, 0.06889763779527559306 ) ) ;
#41734=CIRCLE ( 'NONE', #37844, 0.08090551181102362266 ) ;
#41750=ORIENTED_EDGE ( 'NONE', *, *, #45207, .T. ) ;
#41756=EDGE_CURVE ( 'NONE', #5495, #32411, #13363, .T. ) ;
#41782=AXIS2_PLACEMENT_3D ( 'NONE', #18870, #22007, #29720 ) ;
#41785=LINE ( 'NONE', #12838, #3110 ) ;
#41791=ORIENTED_EDGE ( 'NONE', *, *, #27486, .T. ) ;
#41802=CARTESIAN_POINT ( 'NONE',  ( 0.5538057742782149795, 4.616380251121755931E-17, 0.000000000000000000 ) ) ;
#41805=CYLINDRICAL_SURFACE ( 'NONE', #19907, 0.09842519685039370636 ) ;
#41843=EDGE_CURVE ( 'NONE', #4993, #28970, #7290, .T. ) ;
#41854=CARTESIAN_POINT ( 'NONE',  ( 0.1643927466631365242, -0.08114304634203027555, 0.1405438789450154657 ) ) ;
#41857=DIRECTION ( 'NONE',  ( 0.000000000000000000, -1.000000000000000000, 1.073081856240829922E-16 ) ) ;
#41864=ORIENTED_EDGE ( 'NONE', *, *, #21660, .F. ) ;
#41883=EDGE_LOOP ( 'NONE', ( #42530, #40218, #47182, #39248, #3000 ) ) ;
#41907=EDGE_CURVE ( 'NONE', #30831, #9904, #34098, .T. ) ;
#41920=CARTESIAN_POINT ( 'NONE',  ( 0.001106411046829902005, 0.1060985490482350690, 0.09184399599020635907 ) ) ;
#41943=DIRECTION ( 'NONE',  ( 0.000000000000000000, 0.000000000000000000, 1.000000000000000000 ) ) ;
#41945=EDGE_LOOP ( 'NONE', ( #46252, #44892, #34641, #14397, #12780 ) ) ;
#41962=CARTESIAN_POINT ( 'NONE',  ( 7.107660667885992191E-05, 0.1226968624037449579, 0.06307306040125523761 ) ) ;
#41982=EDGE_LOOP ( 'NONE', ( #522, #35189, #15093, #23183, #13554, #25045 ) ) ;
#42028=ADVANCED_FACE ( 'NONE', ( #31116 ), #42335, .T. ) ;
#42030=CIRCLE ( 'NONE', #10665, 0.09842519685039370636 ) ;
#42034=AXIS2_PLACEMENT_3D ( 'NONE', #9027, #23424, #38739 ) ;
#42065=DIRECTION ( 'NONE',  ( -1.000000000000000000, 0.000000000000000000, 0.000000000000000000 ) ) ;
#42078=DIRECTION ( 'NONE',  ( -1.000000000000000000, 0.000000000000000000, 0.000000000000000000 ) ) ;
#42089=ORIENTED_EDGE ( 'NONE', *, *, #36108, .T. ) ;
#42105=CARTESIAN_POINT ( 'NONE',  ( 0.000000000000000000, 0.000000000000000000, 0.000000000000000000 ) ) ;
#42122=AXIS2_PLACEMENT_3D ( 'NONE', #45594, #6293, #45835 ) ;
#42124=ORIENTED_EDGE ( 'NONE', *, *, #24724, .F. ) ;
#42128=ORIENTED_EDGE ( 'NONE', *, *, #22625, .F. ) ;
#42171=DIRECTION ( 'NONE',  ( 0.000000000000000000, -0.8660254037844384856, -0.5000000000000003331 ) ) ;
#42173=ADVANCED_FACE ( 'NONE', ( #28217 ), #6490, .T. ) ;
#42192=FACE_OUTER_BOUND ( 'NONE', #22545, .T. ) ;
#42254=ORIENTED_EDGE ( 'NONE', *, *, #23599, .T. ) ;
#42258=EDGE_CURVE ( 'NONE', #5428, #46578, #27992, .T. ) ;
#42299=CARTESIAN_POINT ( 'NONE',  ( 0.5660731898098425585, 0.09842519685039370636, 0.000000000000000000 ) ) ;
#42307=ORIENTED_EDGE ( 'NONE', *, *, #29035, .F. ) ;
#42322=ORIENTED_EDGE ( 'NONE', *, *, #46459, .T. ) ;
#42335=CYLINDRICAL_SURFACE ( 'NONE', #38659, 0.09842519685039370636 ) ;
#42338=CARTESIAN_POINT ( 'NONE',  ( 0.4811709046783464450, 4.466152701071653354E-17, 0.000000000000000000 ) ) ;
#42339=ORIENTED_EDGE ( 'NONE', *, *, #4497, .F. ) ;
#42357=CARTESIAN_POINT ( 'NONE',  ( 0.1822895153388602307, 0.000000000000000000, -0.2114570894355444486 ) ) ;
#42361=ADVANCED_FACE ( 'NONE', ( #4475 ), #37881, .T. ) ;
#42363=DIRECTION ( 'NONE',  ( 0.000000000000000000, 0.000000000000000000, 1.000000000000000000 ) ) ;
#42375=ORIENTED_EDGE ( 'NONE', *, *, #20352, .F. ) ;
#42392=CARTESIAN_POINT ( 'NONE',  ( 0.5415383587465882886, 1.205361022782824954E-17, -0.09842519685039370636 ) ) ;
#42394=VERTEX_POINT ( 'NONE', #41132 ) ;
#42398=EDGE_CURVE ( 'NONE', #46714, #8724, #17213, .T. ) ;
#42409=CARTESIAN_POINT ( 'NONE',  ( 0.1618465483937499283, -0.06719994080176183715, 0.1405161193130591291 ) ) ;
#42410=AXIS2_PLACEMENT_3D ( 'NONE', #35927, #2613, #14132 ) ;
#42415=EDGE_LOOP ( 'NONE', ( #11991, #7554, #27469, #45670, #25904, #41408 ) ) ;
#42425=EDGE_LOOP ( 'NONE', ( #30371, #24637, #17120, #21764, #29520 ) ) ;
#42431=DIRECTION ( 'NONE',  ( 0.000000000000000000, -1.000000000000000000, 0.000000000000000000 ) ) ;
#42449=EDGE_CURVE ( 'NONE', #43974, #15794, #37570, .T. ) ;
#42471=DIRECTION ( 'NONE',  ( 0.000000000000000000, -1.000000000000000000, 0.000000000000000000 ) ) ;
#42489=VERTEX_POINT ( 'NONE', #26520 ) ;
#42513=EDGE_CURVE ( 'NONE', #25167, #4886, #37218, .T. ) ;
#42530=ORIENTED_EDGE ( 'NONE', *, *, #1541, .F. ) ;
#42533=ORIENTED_EDGE ( 'NONE', *, *, #36897, .T. ) ;
#42553=CARTESIAN_POINT ( 'NONE',  ( 0.001144830380275972063, 0.02367899979687082546, -0.1377991226254607904 ) ) ;
#42560=EDGE_CURVE ( 'NONE', #18221, #34218, #45497, .T. ) ;
#42582=DIRECTION ( 'NONE',  ( -1.000000000000000000, 0.000000000000000000, 0.000000000000000000 ) ) ;
#42588=FACE_OUTER_BOUND ( 'NONE', #13050, .T. ) ;
#42606=CARTESIAN_POINT ( 'NONE',  ( 0.2642359194686346169, -0.09842519685039370636, 1.205361022782828805E-17 ) ) ;
#42617=ORIENTED_EDGE ( 'NONE', *, *, #2373, .T. ) ;
#42624=( LENGTH_UNIT ( ) NAMED_UNIT ( * ) SI_UNIT ( $, .METRE. ) ) ;
#42642=VERTEX_POINT ( 'NONE', #35056 ) ;
#42668=DIRECTION ( 'NONE',  ( -1.000000000000000000, 0.000000000000000000, 0.000000000000000000 ) ) ;
#42669=AXIS2_PLACEMENT_3D ( 'NONE', #30001, #44786, #37616 ) ;
#42673=DIRECTION ( 'NONE',  ( -1.000000000000000000, 0.000000000000000000, 0.000000000000000000 ) ) ;
#42694=DIRECTION ( 'NONE',  ( -0.5735764363510518216, 0.8191520442889876907, 1.003171929053519693E-16 ) ) ;
#42701=DIRECTION ( 'NONE',  ( 0.000000000000000000, -1.000000000000000000, 0.000000000000000000 ) ) ;
#42705=EDGE_CURVE ( 'NONE', #6499, #21404, #20890, .T. ) ;
#42719=CARTESIAN_POINT ( 'NONE',  ( 0.3906197235759846786, 4.466152701071653354E-17, 0.000000000000000000 ) ) ;
#42759=AXIS2_PLACEMENT_3D ( 'NONE', #16399, #26716, #8471 ) ;
#42760=VERTEX_POINT ( 'NONE', #27885 ) ;
#42774=CARTESIAN_POINT ( 'NONE',  ( 0.005709509457931655034, 0.05322596569711288833, -0.1377927287266135781 ) ) ;
#42778=AXIS2_PLACEMENT_3D ( 'NONE', #38731, #1580, #27270 ) ;
#42801=CIRCLE ( 'NONE', #6843, 0.09842519685039370636 ) ;
#42811=CARTESIAN_POINT ( 'NONE',  ( 0.1577476715125368523, 0.03207557811201351694, -0.1404216743935784162 ) ) ;
#42827=CARTESIAN_POINT ( 'NONE',  ( 0.000000000000000000, 0.000000000000000000, 0.000000000000000000 ) ) ;
#42841=VECTOR ( 'NONE', #45740, 39.37007874015748854 ) ;
#42873=VERTEX_POINT ( 'NONE', #46522 ) ;
#42883=EDGE_CURVE ( 'NONE', #32338, #9031, #21867, .T. ) ;
#42969=AXIS2_PLACEMENT_3D ( 'NONE', #20664, #27666, #2445 ) ;
#42971=VECTOR ( 'NONE', #34313, 39.37007874015748143 ) ;
#42973=AXIS2_PLACEMENT_3D ( 'NONE', #8933, #12315, #34353 ) ;
#42974=CONICAL_SURFACE ( 'NONE', #46820, 0.1377952755905511861, 1.047197551196598297 ) ;
#43020=ORIENTED_EDGE ( 'NONE', *, *, #37217, .T. ) ;
#43023=DIRECTION ( 'NONE',  ( -0.5735764363510518216, -0.8191520442889876907, 0.000000000000000000 ) ) ;
#43037=DIRECTION ( 'NONE',  ( 0.000000000000000000, 0.000000000000000000, 1.000000000000000000 ) ) ;
#43046=EDGE_CURVE ( 'NONE', #19079, #39641, #5510, .T. ) ;
#43081=CIRCLE ( 'NONE', #10193, 0.08090551181102362266 ) ;
#43096=ORIENTED_EDGE ( 'NONE', *, *, #2428, .F. ) ;
#43145=ORIENTED_EDGE ( 'NONE', *, *, #46836, .F. ) ;
#43162=CARTESIAN_POINT ( 'NONE',  ( 0.01230737760510395781, 0.07955613945526338049, -0.1377952755905511861 ) ) ;
#43173=CARTESIAN_POINT ( 'NONE',  ( 0.1611065205447556881, 0.1591792231633174792, 3.327488133692118618E-06 ) ) ;
#43186=VERTEX_POINT ( 'NONE', #45453 ) ;
#43215=EDGE_CURVE ( 'NONE', #21269, #9918, #12909, .T. ) ;
#43219=CIRCLE ( 'NONE', #36390, 0.09842519685039370636 ) ;
#43235=DIRECTION ( 'NONE',  ( -1.000000000000000000, 0.000000000000000000, 0.000000000000000000 ) ) ;
#43258=ORIENTED_EDGE ( 'NONE', *, *, #41313, .T. ) ;
#43286=EDGE_LOOP ( 'NONE', ( #42124, #43096, #42322, #15831, #2252 ) ) ;
#43289=PRESENTATION_STYLE_ASSIGNMENT (( #6629 ) ) ;
#43303=CARTESIAN_POINT ( 'NONE',  ( 0.3547871005709968273, 4.766607801171850497E-17, 0.000000000000000000 ) ) ;
#43317=CARTESIAN_POINT ( 'NONE',  ( 0.5057057357416000487, 4.766607801171850497E-17, 0.000000000000000000 ) ) ;
#43320=CARTESIAN_POINT ( 'NONE',  ( 0.3000685424736224127, -3.032960542342102697E-32, 0.09842519685039370636 ) ) ;
#43336=EDGE_CURVE ( 'NONE', #39913, #9031, #15016, .T. ) ;
#43350=VERTEX_POINT ( 'NONE', #13829 ) ;
#43353=DIRECTION ( 'NONE',  ( 0.000000000000000000, -1.000000000000000000, 0.000000000000000000 ) ) ;
#43364=CARTESIAN_POINT ( 'NONE',  ( 0.4509871776442260227, 4.466152701071653354E-17, 0.000000000000000000 ) ) ;
#43376=AXIS2_PLACEMENT_3D ( 'NONE', #4589, #1003, #44848 ) ;
#43396=B_SPLINE_CURVE_WITH_KNOTS ( 'NONE', 3,
 ( #37185, #3884, #40755, #737, #3653, #281, #43661, #33391, #44132, #26187, #33622, #14926, #36497, #11330, #25942, #37 ),
 .UNSPECIFIED., .F., .F.,
 ( 4, 2, 2, 2, 2, 2, 2, 4 ),
 ( 0.000000000000000000, 0.1250000000000263956, 0.1875000000000336675, 0.2187500000000319467, 0.2500000000000301981, 0.3750000000000279776, 0.5000000000000257572, 1.000000000000000000 ),
 .UNSPECIFIED. ) ;
#43430=CARTESIAN_POINT ( 'NONE',  ( 0.4330708661417322913, -0.08090551181102362266, 0.000000000000000000 ) ) ;
#43447=AXIS2_PLACEMENT_3D ( 'NONE', #38906, #6067, #2711 ) ;
#43452=ORIENTED_EDGE ( 'NONE', *, *, #1193, .T. ) ;
#43460=VECTOR ( 'NONE', #23937, 39.37007874015748143 ) ;
#43461=DIRECTION ( 'NONE',  ( 0.000000000000000000, -1.000000000000000000, 0.000000000000000000 ) ) ;
#43472=AXIS2_PLACEMENT_3D ( 'NONE', #42827, #23963, #17230 ) ;
#43515=DIRECTION ( 'NONE',  ( 0.000000000000000000, 0.000000000000000000, -1.000000000000000000 ) ) ;
#43518=EDGE_LOOP ( 'NONE', ( #5777, #21006, #16516, #45393, #34986 ) ) ;
#43532=CARTESIAN_POINT ( 'NONE',  ( 0.000000000000000000, 0.000000000000000000, 0.000000000000000000 ) ) ;
#43544=DIRECTION ( 'NONE',  ( -1.000000000000000000, 0.000000000000000000, 0.000000000000000000 ) ) ;
#43557=EDGE_CURVE ( 'NONE', #32653, #18221, #46007, .T. ) ;
#43566=DIRECTION ( 'NONE',  ( -1.000000000000000000, 0.000000000000000000, 0.000000000000000000 ) ) ;
#43578=FACE_OUTER_BOUND ( 'NONE', #7101, .T. ) ;
#43599=CARTESIAN_POINT ( 'NONE',  ( 0.000000000000000000, 0.000000000000000000, 0.000000000000000000 ) ) ;
#43602=DIRECTION ( 'NONE',  ( 0.000000000000000000, -1.000000000000000000, 0.000000000000000000 ) ) ;
#43634=CONICAL_SURFACE ( 'NONE', #46709, 0.08090551181102362266, 0.9599310885968742602 ) ;
#43661=CARTESIAN_POINT ( 'NONE',  ( 0.1639941273279659495, 0.08071998019771058075, -0.1398093569819856552 ) ) ;
#43670=DIRECTION ( 'NONE',  ( -1.000000000000000000, 0.000000000000000000, 0.000000000000000000 ) ) ;
#43676=ORIENTED_EDGE ( 'NONE', *, *, #6760, .F. ) ;
#43683=AXIS2_PLACEMENT_3D ( 'NONE', #17150, #38017, #46374 ) ;
#43694=CARTESIAN_POINT ( 'NONE',  ( -9.866766664128584110E-18, -0.1210185251470264484, -0.06598031696940066804 ) ) ;
#43697=B_SPLINE_CURVE_WITH_KNOTS ( 'NONE', 3,
 ( #4672, #40380, #37760, #11898, #8275, #22902, #15972, #375, #37516, #25807, #33955, #29679, #19539 ),
 .UNSPECIFIED., .F., .F.,
 ( 4, 2, 2, 1, 2, 2, 4 ),
 ( 0.000000000000000000, 0.2500000000000000000, 0.3750000000000000000, 0.4374999999999998335, 0.4687499999999997780, 0.4999999999999997224, 1.000000000000000000 ),
 .UNSPECIFIED. ) ;
#43727=CARTESIAN_POINT ( 'NONE',  ( 0.002110188122406738646, 0.03198543007710048791, 0.1377961241629048206 ) ) ;
#43747=AXIS2_PLACEMENT_3D ( 'NONE', #18023, #47258, #36487 ) ;
#43750=DIRECTION ( 'NONE',  ( 0.000000000000000000, 0.000000000000000000, 1.000000000000000000 ) ) ;
#43793=EDGE_LOOP ( 'NONE', ( #45956, #38339, #21665, #250, #25945 ) ) ;
#43809=ORIENTED_EDGE ( 'NONE', *, *, #11577, .F. ) ;
#43812=ORIENTED_EDGE ( 'NONE', *, *, #729, .F. ) ;
#43825=ORIENTED_EDGE ( 'NONE', *, *, #42398, .F. ) ;
#43828=LINE ( 'NONE', #916, #14898 ) ;
#43831=DIRECTION ( 'NONE',  ( 0.000000000000000000, -1.000000000000000000, 0.000000000000000000 ) ) ;
#43868=EDGE_CURVE ( 'NONE', #12246, #12116, #37178, .T. ) ;
#43895=CARTESIAN_POINT ( 'NONE',  ( 0.1526809758745832635, -0.1055212057016147592, 0.09282246162997874472 ) ) ;
#43900=CARTESIAN_POINT ( 'NONE',  ( 0.3727034120734909473, -0.08090551181102362266, 0.000000000000000000 ) ) ;
#43902=EDGE_LOOP ( 'NONE', ( #36552, #17402, #15776, #20031, #40950, #37858, #13450 ) ) ;
#43923=B_SPLINE_CURVE_WITH_KNOTS ( 'NONE', 3,
 ( #21557, #17957, #14381, #44064, #915, #18429, #5707, #5402, #27496, #24568, #20727, #31781, #13326, #6340, #13775, #28419 ),
 .UNSPECIFIED., .F., .F.,
 ( 4, 2, 2, 2, 2, 2, 2, 4 ),
 ( 0.000000000000000000, 0.1250000000000247302, 0.1875000000000333900, 0.2187500000000407174, 0.2500000000000480171, 0.3750000000000456302, 0.5000000000000432987, 1.000000000000000000 ),
 .UNSPECIFIED. ) ;
#43925=EDGE_CURVE ( 'NONE', #29529, #32777, #17305, .T. ) ;
#43936=LINE ( 'NONE', #7508, #33282 ) ;
#43942=CARTESIAN_POINT ( 'NONE',  ( 0.4755220087074803481, 0.09842519685039370636, 0.000000000000000000 ) ) ;
#43948=CIRCLE ( 'NONE', #40884, 0.09842519685039370636 ) ;
#43950=DIRECTION ( 'NONE',  ( -1.000000000000000000, 0.000000000000000000, 0.000000000000000000 ) ) ;
#43956=CARTESIAN_POINT ( 'NONE',  ( 0.4028871391076110364, 4.616380251121755931E-17, 0.000000000000000000 ) ) ;
#43971=DIRECTION ( 'NONE',  ( -1.000000000000000000, 0.000000000000000000, 0.000000000000000000 ) ) ;
#43974=VERTEX_POINT ( 'NONE', #27663 ) ;
#43995=CARTESIAN_POINT ( 'NONE',  ( 0.3000685424736224127, 1.205361022782824954E-17, -0.09842519685039370636 ) ) ;
#44013=CARTESIAN_POINT ( 'NONE',  ( 0.1644020957507537628, 0.08115590401245550978, 0.1405661490837558925 ) ) ;
#44014=CARTESIAN_POINT ( 'NONE',  ( 0.003457534521343483096, -0.1398629656505342711, 0.03335920195936160210 ) ) ;
#44058=APPLICATION_CONTEXT ( 'automotive_design' ) ;
#44060=DIRECTION ( 'NONE',  ( -1.000000000000000000, 0.000000000000000000, 0.000000000000000000 ) ) ;
#44064=CARTESIAN_POINT ( 'NONE',  ( 0.1642211331208078551, -0.08093396052748196012, -0.1401860130076740540 ) ) ;
#44068=DIRECTION ( 'NONE',  ( 0.000000000000000000, -1.000000000000000000, 0.000000000000000000 ) ) ;
#44082=ORIENTED_EDGE ( 'NONE', *, *, #13330, .T. ) ;
#44109=ORIENTED_EDGE ( 'NONE', *, *, #24244, .F. ) ;
#44118=DIRECTION ( 'NONE',  ( 0.000000000000000000, -1.000000000000000000, 0.000000000000000000 ) ) ;
#44119=CARTESIAN_POINT ( 'NONE',  ( 0.5358894627757212481, 4.766607801171850497E-17, 0.000000000000000000 ) ) ;
#44129=CARTESIAN_POINT ( 'NONE',  ( 0.5962569168439626477, 0.09842519685039370636, 0.000000000000000000 ) ) ;
#44132=CARTESIAN_POINT ( 'NONE',  ( 0.1638066842825940672, 0.08057053547025881668, -0.1395522881968654649 ) ) ;
#44141=CARTESIAN_POINT ( 'NONE',  ( 0.1644020957507537628, 0.08115590401245532937, -0.1405661490837558925 ) ) ;
#44147=VERTEX_POINT ( 'NONE', #45989 ) ;
#44148=DIRECTION ( 'NONE',  ( 0.000000000000000000, 0.000000000000000000, 1.000000000000000000 ) ) ;
#44167=B_SPLINE_CURVE_WITH_KNOTS ( 'NONE', 3,
 ( #45524, #12748, #15863, #5769, #45049, #20374, #27611, #9612, #23521, #38126, #41920, #26886, #9129 ),
 .UNSPECIFIED., .F., .F.,
 ( 4, 2, 2, 1, 2, 2, 4 ),
 ( 0.000000000000000000, 0.2499999999999980016, 0.3749999999999974465, 0.4374999999999968914, 0.4687499999999968359, 0.4999999999999968914, 1.000000000000000000 ),
 .UNSPECIFIED. ) ;
#44182=DIRECTION ( 'NONE',  ( 0.000000000000000000, -1.000000000000000000, 0.000000000000000000 ) ) ;
#44186=ORIENTED_EDGE ( 'NONE', *, *, #11662, .T. ) ;
#44189=EDGE_LOOP ( 'NONE', ( #38396, #29097, #6058, #32684, #39137 ) ) ;
#44196=DIRECTION ( 'NONE',  ( 0.000000000000000000, 0.000000000000000000, 1.000000000000000000 ) ) ;
#44197=CARTESIAN_POINT ( 'NONE',  ( 0.1571385178022373375, -0.1334669528785105419, 0.04962495032677907009 ) ) ;
#44203=ORIENTED_EDGE ( 'NONE', *, *, #11607, .F. ) ;
#44211=CARTESIAN_POINT ( 'NONE',  ( 0.006378642920472008850, 0.1475107277141399220, -0.02009854774567082850 ) ) ;
#44223=DIRECTION ( 'NONE',  ( 0.5735764363510447161, -0.8191520442889925757, 1.003171929053525486E-16 ) ) ;
#44234=CARTESIAN_POINT ( 'NONE',  ( 0.3123359580052492146, 4.616380251121755931E-17, 0.000000000000000000 ) ) ;
#44237=CARTESIAN_POINT ( 'NONE',  ( 0.1596650774283338570, 0.09389790430995964554, 0.1183119828675037455 ) ) ;
#44247=CARTESIAN_POINT ( 'NONE',  ( 0.1555687797274982465, 0.1458529223346496095, -0.02296587926509184932 ) ) ;
#44248=AXIS2_PLACEMENT_3D ( 'NONE', #25540, #36317, #43950 ) ;
#44277=CONICAL_SURFACE ( 'NONE', #18280, 0.09842519685039370636, 0.9599310885968824758 ) ;
#44282=ORIENTED_EDGE ( 'NONE', *, *, #3693, .T. ) ;
#44306=ORIENTED_EDGE ( 'NONE', *, *, #21420, .F. ) ;
#44324=CARTESIAN_POINT ( 'NONE',  ( 0.000000000000000000, 0.000000000000000000, 0.000000000000000000 ) ) ;
#44341=EDGE_CURVE ( 'NONE', #30008, #22975, #11240, .T. ) ;
#44350=CARTESIAN_POINT ( 'NONE',  ( 0.1595442748538452582, -0.09421994677688858011, 0.1177495158649726342 ) ) ;
#44383=ORIENTED_EDGE ( 'NONE', *, *, #6701, .T. ) ;
#44423=CARTESIAN_POINT ( 'NONE',  ( 0.1644020957507537628, -0.08115590401245532937, 0.1405661490837558925 ) ) ;
#44428=ORIENTED_EDGE ( 'NONE', *, *, #22234, .F. ) ;
#44446=EDGE_CURVE ( 'NONE', #32777, #9016, #12650, .T. ) ;
#44448=DIRECTION ( 'NONE',  ( -1.000000000000000000, 0.000000000000000000, 0.000000000000000000 ) ) ;
#44451=CARTESIAN_POINT ( 'NONE',  ( 0.2204724409448818867, 0.000000000000000000, 0.000000000000000000 ) ) ;
#44467=CARTESIAN_POINT ( 'NONE',  ( 0.4632545931758527691, 0.08090551181102362266, 9.908067607274841931E-18 ) ) ;
#44482=VECTOR ( 'NONE', #36529, 39.37007874015748143 ) ;
#44489=CARTESIAN_POINT ( 'NONE',  ( 0.1631243713103937287, 0.07417819129889609286, 0.1405411351623389871 ) ) ;
#44506=AXIS2_PLACEMENT_3D ( 'NONE', #46009, #1928, #12511 ) ;
#44550=CARTESIAN_POINT ( 'NONE',  ( 0.2944196465027555387, 4.766607801171850497E-17, 0.000000000000000000 ) ) ;
#44565=ORIENTED_EDGE ( 'NONE', *, *, #15725, .T. ) ;
#44591=CIRCLE ( 'NONE', #39981, 0.09842519685039370636 ) ;
#44593=CARTESIAN_POINT ( 'NONE',  ( 0.3849708276051176936, 4.766607801171850497E-17, 0.000000000000000000 ) ) ;
#44607=ADVANCED_FACE ( 'NONE', ( #34702 ), #8817, .T. ) ;
#44608=CARTESIAN_POINT ( 'NONE',  ( 0.1527640389977631963, -0.1049476924225413443, -0.09381581576814961021 ) ) ;
#44651=CARTESIAN_POINT ( 'NONE',  ( 0.002815489457238504883, 0.03701807430643332120, 0.1377953632175518695 ) ) ;
#44680=CYLINDRICAL_SURFACE ( 'NONE', #28462, 0.09842519685039370636 ) ;
#44717=EDGE_CURVE ( 'NONE', #29582, #20867, #24152, .T. ) ;
#44727=( BOUNDED_SURFACE ( )  B_SPLINE_SURFACE ( 3, 2, ( 
 ( #19861, #22504, #447 ),
 ( #30444, #29747, #11744 ),
 ( #34034, #7883, #37120 ),
 ( #15816, #33556, #26364 ),
 ( #40925, #8119, #37349 ),
 ( #15581, #4502, #922 ) ),
 .UNSPECIFIED., .F., .F., .F. ) 
 B_SPLINE_SURFACE_WITH_KNOTS ( ( 4, 2, 4 ),
 ( 3, 3 ),
 ( 0.01652267773200355103, 0.01858309280828994783, 0.02064350788457639668 ),
 ( 0.000000000000000000, 1.000000000000000000 ),
 .UNSPECIFIED. ) 
 GEOMETRIC_REPRESENTATION_ITEM ( )  RATIONAL_B_SPLINE_SURFACE ( (
 ( 1.000000000000000000, 0.8047780975688290095, 1.000000000000000000),
 ( 1.000000000000000000, 0.8123789546321300570, 1.000000000000000000),
 ( 1.000000000000000000, 0.8190677982993119777, 1.000000000000000000),
 ( 1.000000000000000000, 0.8192346069547790099, 1.000000000000000000),
 ( 1.000000000000000000, 0.8126126759772189789, 1.000000000000000000),
 ( 1.000000000000000000, 0.8047712639312000205, 1.000000000000000000) ) ) 
 REPRESENTATION_ITEM ( '' )  SURFACE ( )  ) ;
#44730=CARTESIAN_POINT ( 'NONE',  ( 0.5236220472440944462, 0.08090551181102362266, 0.000000000000000000 ) ) ;
#44731=CARTESIAN_POINT ( 'NONE',  ( 0.3604359965418638123, -0.09842519685039370636, 0.000000000000000000 ) ) ;
#44745=CARTESIAN_POINT ( 'NONE',  ( 0.4028871391076110364, 4.616380251121755931E-17, 0.000000000000000000 ) ) ;
#44747=VECTOR ( 'NONE', #32043, 39.37007874015748143 ) ;
#44748=AXIS2_PLACEMENT_3D ( 'NONE', #7677, #32648, #29067 ) ;
#44749=FACE_OUTER_BOUND ( 'NONE', #9529, .T. ) ;
#44754=( GEOMETRIC_REPRESENTATION_CONTEXT ( 3 ) GLOBAL_UNCERTAINTY_ASSIGNED_CONTEXT ( ( #18675 ) ) GLOBAL_UNIT_ASSIGNED_CONTEXT ( ( #33257, #3271, #18134 ) ) REPRESENTATION_CONTEXT ( 'NONE', 'WORKASPACE' ) ) ;
#44786=DIRECTION ( 'NONE',  ( -1.000000000000000000, 0.000000000000000000, 0.000000000000000000 ) ) ;
#44792=AXIS2_PLACEMENT_3D ( 'NONE', #25077, #20295, #27774 ) ;
#44803=VERTEX_POINT ( 'NONE', #46401 ) ;
#44804=ORIENTED_EDGE ( 'NONE', *, *, #4041, .F. ) ;
#44816=LINE ( 'NONE', #968, #7857 ) ;
#44825=DIRECTION ( 'NONE',  ( -1.000000000000000000, 0.000000000000000000, 0.000000000000000000 ) ) ;
#44838=ADVANCED_FACE ( 'NONE', ( #10478 ), #15759, .T. ) ;
#44848=DIRECTION ( 'NONE',  ( 0.000000000000000000, 0.000000000000000000, -1.000000000000000000 ) ) ;
#44854=ORIENTED_EDGE ( 'NONE', *, *, #10694, .F. ) ;
#44877=ORIENTED_EDGE ( 'NONE', *, *, #35015, .T. ) ;
#44885=CARTESIAN_POINT ( 'NONE',  ( 0.2642359194686346169, 4.766607801171850497E-17, 0.000000000000000000 ) ) ;
#44892=ORIENTED_EDGE ( 'NONE', *, *, #39795, .T. ) ;
#44901=DIRECTION ( 'NONE',  ( -1.000000000000000000, 0.000000000000000000, 0.000000000000000000 ) ) ;
#44933=CARTESIAN_POINT ( 'NONE',  ( 0.2204724409448818867, 0.07955613945526338049, -0.1377952755905511861 ) ) ;
#44940=CARTESIAN_POINT ( 'NONE',  ( 0.3727034120734909473, 0.08090551181102362266, 0.000000000000000000 ) ) ;
#44947=DIRECTION ( 'NONE',  ( 0.000000000000000000, 0.000000000000000000, -1.000000000000000000 ) ) ;
#44953=FACE_OUTER_BOUND ( 'NONE', #24314, .T. ) ;
#44960=LINE ( 'NONE', #34448, #16108 ) ;
#44967=DIRECTION ( 'NONE',  ( 0.000000000000000000, -1.000000000000000000, 0.000000000000000000 ) ) ;
#44972=DIRECTION ( 'NONE',  ( -1.000000000000000000, 0.000000000000000000, 0.000000000000000000 ) ) ;
#45002=EDGE_LOOP ( 'NONE', ( #14002, #4791, #10898, #38145, #7624 ) ) ;
#45025=DIRECTION ( 'NONE',  ( -1.000000000000000000, 0.000000000000000000, 0.000000000000000000 ) ) ;
#45031=CIRCLE ( 'NONE', #22096, 0.09842519685039370636 ) ;
#45037=AXIS2_PLACEMENT_3D ( 'NONE', #40605, #47112, #43750 ) ;
#45049=CARTESIAN_POINT ( 'NONE',  ( 0.005686768416191418166, 0.09278660394097182351, 0.1148867573884606030 ) ) ;
#45052=ORIENTED_EDGE ( 'NONE', *, *, #9903, .F. ) ;
#45054=CARTESIAN_POINT ( 'NONE',  ( 0.000000000000000000, 0.000000000000000000, 0.09842519685039370636 ) ) ;
#45079=CIRCLE ( 'NONE', #42778, 0.09842519685039370636 ) ;
#45095=AXIS2_PLACEMENT_3D ( 'NONE', #38596, #39057, #6226 ) ;
#45128=CARTESIAN_POINT ( 'NONE',  ( 0.01230737760510393873, -0.07955613945526318620, 0.1377952755905511861 ) ) ;
#45152=DIRECTION ( 'NONE',  ( -1.000000000000000000, 0.000000000000000000, 0.000000000000000000 ) ) ;
#45164=CARTESIAN_POINT ( 'NONE',  ( 0.2698848154395015464, 4.466152701071653354E-17, 0.000000000000000000 ) ) ;
#45195=ORIENTED_EDGE ( 'NONE', *, *, #41432, .T. ) ;
#45207=EDGE_CURVE ( 'NONE', #31651, #46614, #3140, .T. ) ;
#45270=ADVANCED_FACE ( 'NONE', ( #24612 ), #13142, .T. ) ;
#45280=AXIS2_PLACEMENT_3D ( 'NONE', #38190, #34856, #41512 ) ;
#45295=CARTESIAN_POINT ( 'NONE',  ( 0.1571288672381034868, -0.02360035419889824210, 0.1403980133540951303 ) ) ;
#45358=EDGE_LOOP ( 'NONE', ( #12853, #8983, #25742, #16296, #46937 ) ) ;
#45387=VECTOR ( 'NONE', #36308, 39.37007874015748854 ) ;
#45393=ORIENTED_EDGE ( 'NONE', *, *, #13885, .T. ) ;
#45394=AXIS2_PLACEMENT_3D ( 'NONE', #11234, #15292, #15541 ) ;
#45395=ADVANCED_FACE ( 'NONE', ( #28955 ), #18825, .T. ) ;
#45398=LINE ( 'NONE', #22897, #32108 ) ;
#45400=ORIENTED_EDGE ( 'NONE', *, *, #23850, .T. ) ;
#45405=CARTESIAN_POINT ( 'NONE',  ( 0.000000000000000000, 0.000000000000000000, 0.000000000000000000 ) ) ;
#45424=DIRECTION ( 'NONE',  ( -0.5735764363510518216, 0.8191520442889876907, 1.003171929053519693E-16 ) ) ;
#45437=VERTEX_POINT ( 'NONE', #47121 ) ;
#45453=CARTESIAN_POINT ( 'NONE',  ( 0.4151545546392377273, -3.032960542342102697E-32, 0.09842519685039370636 ) ) ;
#45455=CARTESIAN_POINT ( 'NONE',  ( 0.1636082376614000078, -0.08043368169713546734, 0.1393148943341546153 ) ) ;
#45472=CARTESIAN_POINT ( 'NONE',  ( 0.000000000000000000, -0.1193342091828950846, -0.06889763779527559306 ) ) ;
#45484=CARTESIAN_POINT ( 'NONE',  ( 0.1595442748538490330, 0.09421994677690039011, -0.1177495158649775608 ) ) ;
#45485=ADVANCED_FACE ( 'NONE', ( #132 ), #11583, .T. ) ;
#45494=CARTESIAN_POINT ( 'NONE',  ( 0.000000000000000000, 1.205361022782826802E-17, -0.09842519685039370636 ) ) ;
#45497=B_SPLINE_CURVE_WITH_KNOTS ( 'NONE', 3,
 ( #11601, #22843, #26222, #1489, #29624, #12316, #30084, #26933, #41485, #4366, #11363, #33898, #33657 ),
 .UNSPECIFIED., .F., .F.,
 ( 4, 2, 2, 1, 2, 2, 4 ),
 ( 0.000000000000000000, 0.2500000000000000000, 0.3750000000000002776, 0.4375000000000008327, 0.4687500000000012768, 0.5000000000000016653, 1.000000000000000000 ),
 .UNSPECIFIED. ) ;
#45506=LINE ( 'NONE', #38336, #20311 ) ;
#45524=CARTESIAN_POINT ( 'NONE',  ( 0.01230737760510397689, 0.07955613945526338049, 0.1377952755905511861 ) ) ;
#45538=VECTOR ( 'NONE', #27178, 39.37007874015748143 ) ;
#45568=CIRCLE ( 'NONE', #12618, 0.09842519685039370636 ) ;
#45572=ADVANCED_FACE ( 'NONE', ( #8515 ), #832, .T. ) ;
#45573=CARTESIAN_POINT ( 'NONE',  ( 0.003168982538894474926, -0.03928607229653706401, -0.1377952867935988979 ) ) ;
#45586=ORIENTED_EDGE ( 'NONE', *, *, #23278, .T. ) ;
#45594=CARTESIAN_POINT ( 'NONE',  ( 0.5962569168439626477, 4.766607801171850497E-17, 0.000000000000000000 ) ) ;
#45620=ORIENTED_EDGE ( 'NONE', *, *, #28549, .F. ) ;
#45629=DIRECTION ( 'NONE',  ( -1.000000000000000000, 0.000000000000000000, 0.000000000000000000 ) ) ;
#45642=ADVANCED_FACE ( 'NONE', ( #26288 ), #44680, .T. ) ;
#45654=CARTESIAN_POINT ( 'NONE',  ( 0.000000000000000000, 1.205361022782826802E-17, -0.09842519685039370636 ) ) ;
#45663=DIRECTION ( 'NONE',  ( 0.000000000000000000, 0.000000000000000000, 1.000000000000000000 ) ) ;
#45670=ORIENTED_EDGE ( 'NONE', *, *, #13172, .F. ) ;
#45680=CARTESIAN_POINT ( 'NONE',  ( 0.000000000000000000, 0.000000000000000000, 0.000000000000000000 ) ) ;
#45688=AXIS2_PLACEMENT_3D ( 'NONE', #18791, #21692, #25998 ) ;
#45690=DIRECTION ( 'NONE',  ( -1.000000000000000000, 0.000000000000000000, 0.000000000000000000 ) ) ;
#45700=ORIENTED_EDGE ( 'NONE', *, *, #4497, .T. ) ;
#45709=CARTESIAN_POINT ( 'NONE',  ( 0.4811709046783464450, -3.032960542342102697E-32, 0.09842519685039370636 ) ) ;
#45715=CARTESIAN_POINT ( 'NONE',  ( 0.5538057742782149795, 4.616380251121755931E-17, 0.000000000000000000 ) ) ;
#45717=EDGE_LOOP ( 'NONE', ( #40726, #39343, #19930, #1970 ) ) ;
#45736=ADVANCED_FACE ( 'NONE', ( #38228 ), #1639, .T. ) ;
#45740=DIRECTION ( 'NONE',  ( 0.5735764363510447161, 0.8191520442889925757, 0.000000000000000000 ) ) ;
#45763=DIRECTION ( 'NONE',  ( 0.000000000000000000, -1.000000000000000000, 0.000000000000000000 ) ) ;
#45769=DIRECTION ( 'NONE',  ( -0.5735764363510518216, -0.8191520442889876907, 0.000000000000000000 ) ) ;
#45778=CARTESIAN_POINT ( 'NONE',  ( 0.4330708661417322913, 4.616380251121755931E-17, 0.000000000000000000 ) ) ;
#45792=CONICAL_SURFACE ( 'NONE', #5273, 0.1377952755905511861, 1.047197551196598297 ) ;
#45802=FACE_OUTER_BOUND ( 'NONE', #19462, .T. ) ;
#45818=CIRCLE ( 'NONE', #27513, 0.09842519685039370636 ) ;
#45820=DIRECTION ( 'NONE',  ( 0.000000000000000000, -1.000000000000000000, 0.000000000000000000 ) ) ;
#45833=AXIS2_PLACEMENT_3D ( 'NONE', #20937, #34885, #13756 ) ;
#45835=DIRECTION ( 'NONE',  ( 0.000000000000000000, 1.000000000000000000, 0.000000000000000000 ) ) ;
#45905=CARTESIAN_POINT ( 'NONE',  ( 0.4811709046783464450, 4.466152701071653354E-17, 0.000000000000000000 ) ) ;
#45909=ORIENTED_EDGE ( 'NONE', *, *, #43336, .F. ) ;
#45911=CIRCLE ( 'NONE', #16114, 0.09842519685039370636 ) ;
#45925=EDGE_CURVE ( 'NONE', #8667, #16843, #7748, .T. ) ;
#45956=ORIENTED_EDGE ( 'NONE', *, *, #26743, .F. ) ;
#45959=DIRECTION ( 'NONE',  ( 0.000000000000000000, 0.000000000000000000, 1.000000000000000000 ) ) ;
#45973=CARTESIAN_POINT ( 'NONE',  ( 0.2698848154395015464, 4.466152701071653354E-17, 0.000000000000000000 ) ) ;
#45989=CARTESIAN_POINT ( 'NONE',  ( 0.3727034120734909473, -0.08090551181102362266, 1.098083891755157578E-17 ) ) ;
#46007=B_SPLINE_CURVE_WITH_KNOTS ( 'NONE', 3,
 ( #17657, #46881, #47129, #28718, #39677, #4149, #14317, #1739, #12321, #45573, #12076, #15913, #19245 ),
 .UNSPECIFIED., .F., .F.,
 ( 4, 2, 2, 1, 2, 2, 4 ),
 ( 0.000000000000000000, 0.2499999999999993339, 0.3749999999999990008, 0.4374999999999988343, 0.4687499999999987788, 0.4999999999999987788, 1.000000000000000000 ),
 .UNSPECIFIED. ) ;
#46009=CARTESIAN_POINT ( 'NONE',  ( 0.2007874015748031815, 0.000000000000000000, 0.000000000000000000 ) ) ;
#46028=CIRCLE ( 'NONE', #43747, 0.1377952755905511861 ) ;
#46038=AXIS2_PLACEMENT_3D ( 'NONE', #39469, #10752, #25359 ) ;
#46046=CARTESIAN_POINT ( 'NONE',  ( 0.3246033735368759610, -3.032960542342102697E-32, 0.09842519685039370636 ) ) ;
#46068=CARTESIAN_POINT ( 'NONE',  ( 0.1634876958473884812, 0.1607137227551046210, 3.803501547868341211E-07 ) ) ;
#46079=CARTESIAN_POINT ( 'NONE',  ( 0.4632545931758527691, 4.616380251121755931E-17, 0.000000000000000000 ) ) ;
#46096=DIRECTION ( 'NONE',  ( 0.000000000000000000, -1.000000000000000000, 0.000000000000000000 ) ) ;
#46116=AXIS2_PLACEMENT_3D ( 'NONE', #30375, #8041, #4199 ) ;
#46125=LINE ( 'NONE', #13325, #18941 ) ;
#46145=CARTESIAN_POINT ( 'NONE',  ( 0.1822895153388602307, 0.000000000000000000, -0.2114570894355444486 ) ) ;
#46153=CARTESIAN_POINT ( 'NONE',  ( 0.3246033735368759610, 1.205361022782824954E-17, -0.09842519685039370636 ) ) ;
#46176=VERTEX_POINT ( 'NONE', #30775 ) ;
#46190=CARTESIAN_POINT ( 'NONE',  ( 0.3604359965418638123, 1.205361022782824954E-17, -0.09842519685039370636 ) ) ;
#46191=FACE_OUTER_BOUND ( 'NONE', #19573, .T. ) ;
#46196=ADVANCED_FACE ( 'NONE', ( #37939 ), #38384, .T. ) ;
#46252=ORIENTED_EDGE ( 'NONE', *, *, #16324, .F. ) ;
#46256=VERTEX_POINT ( 'NONE', #33426 ) ;
#46276=COLOUR_RGB ( '', 0.72549020, 0.75294118, 0.79215686) ;
#46314=CARTESIAN_POINT ( 'NONE',  ( 0.5717220857807087109, -0.09842519685039370636, 0.000000000000000000 ) ) ;
#46374=DIRECTION ( 'NONE',  ( 0.000000000000000000, -1.000000000000000000, 0.000000000000000000 ) ) ;
#46384=B_SPLINE_CURVE_WITH_KNOTS ( 'NONE', 3,
 ( #10073, #35258, #24929, #6461, #3102, #39749, #24688, #28071, #21078, #39286, #9843, #35717, #36196, #47204, #39052, #2853, #32377, #39522, #6938, #6222, #21560, #20846 ),
 .UNSPECIFIED., .F., .F.,
 ( 4, 2, 2, 2, 2, 2, 2, 2, 2, 2, 4 ),
 ( 0.000000000000000000, 0.1249999999999998890, 0.1874999999999999167, 0.2187499999999999167, 0.2499999999999999445, 0.4999999999999994449, 0.6249999999999992228, 0.6874999999999991118, 0.7187499999999990008, 0.7499999999999990008, 1.000000000000000000 ),
 .UNSPECIFIED. ) ;
#46388=ORIENTED_EDGE ( 'NONE', *, *, #7247, .T. ) ;
#46401=CARTESIAN_POINT ( 'NONE',  ( 0.6141732283464567121, 0.000000000000000000, 0.08090551181102362266 ) ) ;
#46429=CARTESIAN_POINT ( 'NONE',  ( 0.008396861977877295019, 0.08632935120539782237, -0.1260637287088791914 ) ) ;
#46459=EDGE_CURVE ( 'NONE', #9934, #9904, #5810, .T. ) ;
#46473=EDGE_CURVE ( 'NONE', #35175, #35809, #9325, .T. ) ;
#46477=EDGE_CURVE ( 'NONE', #18563, #46176, #31464, .T. ) ;
#46498=CARTESIAN_POINT ( 'NONE',  ( 0.4208034506101054895, 0.09842519685039370636, 1.205361022782828805E-17 ) ) ;
#46509=VERTEX_POINT ( 'NONE', #46046 ) ;
#46522=CARTESIAN_POINT ( 'NONE',  ( 0.3302522695077432791, 0.09842519685039370636, 1.205361022782828805E-17 ) ) ;
#46540=ORIENTED_EDGE ( 'NONE', *, *, #29916, .T. ) ;
#46550=ORIENTED_EDGE ( 'NONE', *, *, #36755, .T. ) ;
#46558=DIRECTION ( 'NONE',  ( -0.5735764363510518216, 0.8191520442889876907, 1.003171929053519693E-16 ) ) ;
#46578=VERTEX_POINT ( 'NONE', #10603 ) ;
#46611=DIRECTION ( 'NONE',  ( 0.3420201433256624401, 0.000000000000000000, -0.9396926207859106484 ) ) ;
#46612=EDGE_CURVE ( 'NONE', #42489, #41232, #21604, .T. ) ;
#46614=VERTEX_POINT ( 'NONE', #18001 ) ;
#46634=CONICAL_SURFACE ( 'NONE', #42034, 0.08090551181102362266, 0.9599310885968742602 ) ;
#46654=DIRECTION ( 'NONE',  ( -1.000000000000000000, 0.000000000000000000, 0.000000000000000000 ) ) ;
#46656=AXIS2_PLACEMENT_3D ( 'NONE', #32402, #39307, #3612 ) ;
#46658=EDGE_CURVE ( 'NONE', #18113, #43974, #29276, .T. ) ;
#46662=ORIENTED_EDGE ( 'NONE', *, *, #46658, .T. ) ;
#46704=ORIENTED_EDGE ( 'NONE', *, *, #14961, .F. ) ;
#46709=AXIS2_PLACEMENT_3D ( 'NONE', #29094, #4998, #32436 ) ;
#46714=VERTEX_POINT ( 'NONE', #46994 ) ;
#46738=CARTESIAN_POINT ( 'NONE',  ( 0.5966535433070866423, 0.000000000000000000, 0.000000000000000000 ) ) ;
#46768=DIRECTION ( 'NONE',  ( -1.000000000000000000, 0.000000000000000000, 0.000000000000000000 ) ) ;
#46771=DIRECTION ( 'NONE',  ( -0.7071067811865454633, 8.659560562354952580E-17, -0.7071067811865494601 ) ) ;
#46798=CARTESIAN_POINT ( 'NONE',  ( 0.000000000000000000, 0.000000000000000000, 0.000000000000000000 ) ) ;
#46799=LINE ( 'NONE', #13514, #13256 ) ;
#46804=ORIENTED_EDGE ( 'NONE', *, *, #22284, .F. ) ;
#46810=DIRECTION ( 'NONE',  ( 1.000000000000000000, 0.000000000000000000, 0.000000000000000000 ) ) ;
#46812=EDGE_LOOP ( 'NONE', ( #11452, #8247, #16632, #17185, #23142, #15733 ) ) ;
#46815=CARTESIAN_POINT ( 'NONE',  ( 0.0005737749932938826774, -0.1277779173642346333, -0.05427780112423363085 ) ) ;
#46820=AXIS2_PLACEMENT_3D ( 'NONE', #37064, #8294, #23166 ) ;
#46830=CARTESIAN_POINT ( 'NONE',  ( 0.1559668151880143627, -0.05603484930530078928, 0.1377952755905511861 ) ) ;
#46836=EDGE_CURVE ( 'NONE', #35869, #39913, #16273, .T. ) ;
#46847=EDGE_CURVE ( 'NONE', #8667, #40494, #35929, .T. ) ;
#46875=ORIENTED_EDGE ( 'NONE', *, *, #17489, .T. ) ;
#46881=CARTESIAN_POINT ( 'NONE',  ( -9.829250441071060444E-18, -0.006719043512062446329, -0.1377952755905511861 ) ) ;
#46891=CIRCLE ( 'NONE', #3279, 0.09842519685039370636 ) ;
#46902=CARTESIAN_POINT ( 'NONE',  ( 0.1636882031745370836, 0.08048648106634784249, 0.1394067746907973471 ) ) ;
#46906=EDGE_CURVE ( 'NONE', #32919, #30008, #14812, .T. ) ;
#46914=EDGE_LOOP ( 'NONE', ( #42375, #18352, #16917, #24488, #38858 ) ) ;
#46919=ORIENTED_EDGE ( 'NONE', *, *, #36697, .T. ) ;
#46933=CIRCLE ( 'NONE', #31648, 0.09842519685039370636 ) ;
#46937=ORIENTED_EDGE ( 'NONE', *, *, #28652, .F. ) ;
#46952=DIRECTION ( 'NONE',  ( -1.000000000000000000, 0.000000000000000000, 0.000000000000000000 ) ) ;
#46953=B_SPLINE_CURVE_WITH_KNOTS ( 'NONE', 3,
 ( #21266, #17914, #39471, #40406, #21024, #25602, #21503, #29468, #21987, #6649, #35671, #25362, #46902, #10508, #35891, #32566, #44013 ),
 .UNSPECIFIED., .F., .F.,
 ( 4, 2, 2, 2, 2, 1, 2, 2, 4 ),
 ( 0.000000000000000000, 0.2500000000000179301, 0.3750000000000189293, 0.5000000000000199840, 0.6250000000000210942, 0.6875000000000186517, 0.7187500000000174305, 0.7500000000000162093, 1.000000000000000000 ),
 .UNSPECIFIED. ) ;
#46994=CARTESIAN_POINT ( 'NONE',  ( 0.5415383587465882886, 0.09842519685039370636, 1.205361022782828805E-17 ) ) ;
#46997=CARTESIAN_POINT ( 'NONE',  ( 0.1640397255806962662, -0.1615187269478208787, -1.214557857170256269E-06 ) ) ;
#47014=CARTESIAN_POINT ( 'NONE',  ( 0.1642909309817496277, 0.1618381351750143859, 1.491082269536694323E-08 ) ) ;
#47039=CARTESIAN_POINT ( 'NONE',  ( 0.3246033735368759610, 4.766607801171850497E-17, 0.000000000000000000 ) ) ;
#47061=CIRCLE ( 'NONE', #38653, 0.09842519685039370636 ) ;
#47063=VECTOR ( 'NONE', #34128, 39.37007874015748143 ) ;
#47074=CARTESIAN_POINT ( 'NONE',  ( 0.1588152253974371431, -0.05589252443383686819, 0.1377952755905511029 ) ) ;
#47095=EDGE_LOOP ( 'NONE', ( #41283, #19509, #273, #4421, #25597 ) ) ;
#47102=ORIENTED_EDGE ( 'NONE', *, *, #9607, .T. ) ;
#47112=DIRECTION ( 'NONE',  ( -1.000000000000000000, 0.000000000000000000, 0.000000000000000000 ) ) ;
#47116=ORIENTED_EDGE ( 'NONE', *, *, #39382, .F. ) ;
#47121=CARTESIAN_POINT ( 'NONE',  ( 0.5839895013123354017, -0.08090551181102362266, 1.098083891755157578E-17 ) ) ;
#47129=CARTESIAN_POINT ( 'NONE',  ( 0.0002749165346187715567, -0.01333023677889469405, -0.1377841106655355030 ) ) ;
#47182=ORIENTED_EDGE ( 'NONE', *, *, #6804, .T. ) ;
#47204=CARTESIAN_POINT ( 'NONE',  ( 0.1571385178022482731, -0.1097099440836124123, -0.09077329659535897377 ) ) ;
#47210=DIRECTION ( 'NONE',  ( -1.000000000000000000, 0.000000000000000000, 0.000000000000000000 ) ) ;
#47213=CARTESIAN_POINT ( 'NONE',  ( 0.3302522695077432791, 1.205361022782824954E-17, -0.09842519685039370636 ) ) ;
#47234=ORIENTED_EDGE ( 'NONE', *, *, #22625, .T. ) ;
#47235=ADVANCED_FACE ( 'NONE', ( #45802 ), #39193, .T. ) ;
#47244=CARTESIAN_POINT ( 'NONE',  ( 0.1642211665447064484, -0.1618716989613354917, -2.141082140707521260E-06 ) ) ;
#47258=DIRECTION ( 'NONE',  ( 1.000000000000000000, 0.000000000000000000, 0.000000000000000000 ) ) ;
#47266=CARTESIAN_POINT ( 'NONE',  ( 0.1564256176496356399, 0.1180751491311807649, 0.07625914551937829078 ) ) ;
#47281=DIRECTION ( 'NONE',  ( -0.5735764363510518216, -0.8191520442889876907, 0.000000000000000000 ) ) ;
#47288=VECTOR ( 'NONE', #33914, 39.37007874015748143 ) ;
#47308=ADVANCED_BREP_SHAPE_REPRESENTATION ( 'ISO 4162 M5x10 Hex Flange Bolt', ( #5351, #20860 ), #30086 ) ;
#47320=CARTESIAN_POINT ( 'NONE',  ( 0.1596653045507425150, -0.05551344951183716930, 0.1404739663221734325 ) ) ;
#47348=DIRECTION ( 'NONE',  ( 0.5735764363510447161, -0.8191520442889925757, 1.003171929053525486E-16 ) ) ;
#47349=FACE_OUTER_BOUND ( 'NONE', #40876, .T. ) ;
#47353=EDGE_LOOP ( 'NONE', ( #47234, #27238, #37787, #43809 ) ) ;
#47366=AXIS2_PLACEMENT_3D ( 'NONE', #15152, #18489, #724 ) ;
#47369=LINE ( 'NONE', #39671, #23415 ) ;
#47370=AXIS2_PLACEMENT_3D ( 'NONE', #882, #34232, #23664 ) ;
#47396=DIRECTION ( 'NONE',  ( 0.000000000000000000, -1.000000000000000000, 0.000000000000000000 ) ) ;
ENDSEC;
END-ISO-10303-21;
